ISO-10303-21;
HEADER;
FILE_DESCRIPTION (('STEP AP214'),
    '1' );
FILE_NAME ('Wheel Axle Bolt.step',
    '2026-10-09T12:05:53',
    ( '' ),
    ( '' ),
    'SwSTEP 2.0',
    'SolidWorks 2026',
    '' );
FILE_SCHEMA (( 'AUTOMOTIVE_DESIGN' ));
ENDSEC;

DATA;
#34=CARTESIAN_POINT ( 'NONE',  ( 63.30967889250540992, 1.328674444234379859, -68.76626720283900340 ) ) ;
#37=DIRECTION ( 'NONE',  ( 0.000000000000000000, -0.7071067811865292541, 0.7071067811865656694 ) ) ;
#47=CARTESIAN_POINT ( 'NONE',  ( 71.33582579397329937, 0.9940695285616559795, -70.71491496446259362 ) ) ;
#58=CARTESIAN_POINT ( 'NONE',  ( 71.48394854028050815, 1.096932441169200079, -60.71856768636379797 ) ) ;
#60=CARTESIAN_POINT ( 'NONE',  ( 72.18036885542301206, 1.274155933524790063, -61.30553710256390332 ) ) ;
#96=CARTESIAN_POINT ( 'NONE',  ( 63.43393739769620510, 1.883811055320669947, -62.44999999999999574 ) ) ;
#103=CARTESIAN_POINT ( 'NONE',  ( 63.10556452593170462, 0.9234936569010840923, -62.37649816534809588 ) ) ;
#114=CARTESIAN_POINT ( 'NONE',  ( 63.48718924516480655, 1.369286338574360107, -62.31365646596000119 ) ) ;
#131=EDGE_CURVE ( 'NONE', #41228, #12484, #43567, .T. ) ;
#147=CARTESIAN_POINT ( 'NONE',  ( 72.11830705158430987, 1.407740700961940039, -69.90489258341499124 ) ) ;
#149=AXIS2_PLACEMENT_3D ( 'NONE', #32880, #41030, #5146 ) ;
#166=CARTESIAN_POINT ( 'NONE',  ( 71.29447239804829906, 1.393731187554809958, -70.25064478522961053 ) ) ;
#181=EDGE_LOOP ( 'NONE', ( #10169, #38470, #47423, #39238 ) ) ;
#192=CARTESIAN_POINT ( 'NONE',  ( 64.43393739769619799, 11.38381105532079829, -62.44999999999999574 ) ) ;
#233=ORIENTED_EDGE ( 'NONE', *, *, #50630, .F. ) ;
#263=AXIS2_PLACEMENT_3D ( 'NONE', #1040, #23378, #35460 ) ;
#270=CARTESIAN_POINT ( 'NONE',  ( 71.19761362482960010, 1.388189907116970101, -61.01613942410280345 ) ) ;
#279=CARTESIAN_POINT ( 'NONE',  ( 63.07039345372018602, 1.099973129953850215, -68.78515728267289830 ) ) ;
#292=CARTESIAN_POINT ( 'NONE',  ( 71.23944111523938716, 1.270877794983130027, -70.57718306158270138 ) ) ;
#302=CARTESIAN_POINT ( 'NONE',  ( 71.36299175555980412, 1.264791438333819906, -60.78603624114159487 ) ) ;
#305=CARTESIAN_POINT ( 'NONE',  ( 72.21022460378770802, 1.195685806282509978, -61.28382422308500566 ) ) ;
#307=CARTESIAN_POINT ( 'NONE',  ( 64.99878011502339348, 1.099973129953850215, -70.71354394397609155 ) ) ;
#309=VERTEX_POINT ( 'NONE', #6067 ) ;
#346=CARTESIAN_POINT ( 'NONE',  ( 63.44018392888030178, 1.383811055320669947, -62.77287342953649585 ) ) ;
#348=PLANE ( 'NONE',  #1400 ) ;
#357=CARTESIAN_POINT ( 'NONE',  ( 65.02936113742819657, 1.390208944942409985, -61.02997314496759884 ) ) ;
#361=CARTESIAN_POINT ( 'NONE',  ( 63.57044994947320760, 1.402336724397559964, -62.38137791222469986 ) ) ;
#400=CARTESIAN_POINT ( 'NONE',  ( 72.40616118569840864, 1.406831506490830108, -69.61258613051629141 ) ) ;
#422=ORIENTED_EDGE ( 'NONE', *, *, #26234, .F. ) ;
#523=DIRECTION ( 'NONE',  ( -0.5193766129849238800, 0.000000000000000000, -0.8545454545454611583 ) ) ;
#529=CARTESIAN_POINT ( 'NONE',  ( 63.47971227208819300, 1.385888765344509999, -68.65207957385619864 ) ) ;
#542=CARTESIAN_POINT ( 'NONE',  ( 71.19443613848248731, 1.370118064600909902, -70.39245762607309587 ) ) ;
#543=DIRECTION ( 'NONE',  ( 0.000000000000000000, -1.000000000000000000, 0.000000000000000000 ) ) ;
#551=CARTESIAN_POINT ( 'NONE',  ( 71.17905174416029013, 1.387412027389909985, -61.00994802092580471 ) ) ;
#553=CARTESIAN_POINT ( 'NONE',  ( 72.06056480500649286, 1.091560265417830022, -61.11985751463939920 ) ) ;
#556=CARTESIAN_POINT ( 'NONE',  ( 65.07343865691001383, 1.370118064600889918, -70.39245762607309587 ) ) ;
#557=ORIENTED_EDGE ( 'NONE', *, *, #33185, .T. ) ;
#598=CARTESIAN_POINT ( 'NONE',  ( 63.40852617131290003, 1.383411777981069957, -62.75344103383148564 ) ) ;
#606=CARTESIAN_POINT ( 'NONE',  ( 64.89668540611299363, 1.325715844996850024, -60.88145737504000010 ) ) ;
#633=ORIENTED_EDGE ( 'NONE', *, *, #50882, .T. ) ;
#656=CARTESIAN_POINT ( 'NONE',  ( 72.26841818567149289, 1.277726347179370059, -69.91422003724520096 ) ) ;
#666=CARTESIAN_POINT ( 'NONE',  ( 64.29895108830758943, 1.258806274519160162, -61.13074064017239806 ) ) ;
#671=AXIS2_PLACEMENT_3D ( 'NONE', #41968, #6064, #19398 ) ;
#702=ADVANCED_FACE ( 'NONE', ( #11811 ), #36152, .F. ) ;
#703=DIRECTION ( 'NONE',  ( 1.000000000000000000, 0.000000000000000000, 0.000000000000000000 ) ) ;
#710=CARTESIAN_POINT ( 'NONE',  ( 63.77506981661740326, 1.028299550205570068, -69.77396888106839867 ) ) ;
#755=ORIENTED_EDGE ( 'NONE', *, *, #1133, .T. ) ;
#776=DIRECTION ( 'NONE',  ( 0.8545454545454587159, -1.845195999999999228E-15, -0.5193766129849277657 ) ) ;
#781=CARTESIAN_POINT ( 'NONE',  ( 64.93393739769619799, 1.883811055320669947, -68.84999999999999432 ) ) ;
#784=CARTESIAN_POINT ( 'NONE',  ( 63.13475262569159696, 0.9955677559369519036, -68.95442834019429768 ) ) ;
#795=CARTESIAN_POINT ( 'NONE',  ( 71.07527734533519492, 1.384447124000270035, -70.32375107525380997 ) ) ;
#803=CARTESIAN_POINT ( 'NONE',  ( 72.97593009921529017, 1.263903724274369811, -68.92034810279041324 ) ) ;
#807=CARTESIAN_POINT ( 'NONE',  ( 71.22849534471220068, 1.384708701328909886, -60.99162623037230446 ) ) ;
#809=CARTESIAN_POINT ( 'NONE',  ( 71.33393739769628894, 11.23736444591397543, -61.59644660940672622 ) ) ;
#810=CARTESIAN_POINT ( 'NONE',  ( 71.79351670693411336, 0.9755120847784399807, -60.89440987841059894 ) ) ;
#813=CARTESIAN_POINT ( 'NONE',  ( 64.99546124159368787, 0.9209567800143640959, -70.76376997076650355 ) ) ;
#816=CARTESIAN_POINT ( 'NONE',  ( 72.33393739769579156, 10.88381105532070059, -62.44999999999859597 ) ) ;
#854=( GEOMETRIC_REPRESENTATION_CONTEXT ( 3 ) GLOBAL_UNCERTAINTY_ASSIGNED_CONTEXT ( ( #8008 ) ) GLOBAL_UNIT_ASSIGNED_CONTEXT ( ( #10591, #23128, #47273 ) ) REPRESENTATION_CONTEXT ( 'NONE', 'WORKASPACE' ) );
#863=CARTESIAN_POINT ( 'NONE',  ( 63.13551795786779053, 1.096291039689149871, -62.40636042108670267 ) ) ;
#872=CARTESIAN_POINT ( 'NONE',  ( 64.73967613295080525, 1.000225705806889964, -60.71075825745960231 ) ) ;
#887=EDGE_LOOP ( 'NONE', ( #17457, #46801, #27829, #39812, #47372, #27144, #12308, #24981 ) ) ;
#920=CARTESIAN_POINT ( 'NONE',  ( 72.29200328562438926, 1.409763019284750118, -69.74012879731020575 ) ) ;
#921=EDGE_CURVE ( 'NONE', #8004, #33885, #26864, .T. ) ;
#934=CARTESIAN_POINT ( 'NONE',  ( 64.34567283584411257, 1.332297898506040079, -61.16569568407510360 ) ) ;
#939=DIRECTION ( 'NONE',  ( 6.938893903907222067E-15, 0.000000000000000000, -1.000000000000000000 ) ) ;
#976=CARTESIAN_POINT ( 'NONE',  ( 64.23018683434881382, 1.404169013718219894, -69.96877364398430643 ) ) ;
#1025=CARTESIAN_POINT ( 'NONE',  ( 72.06663613036050720, 1.456055805561079941, -69.85592311231539497 ) ) ;
#1028=DIRECTION ( 'NONE',  ( 0.5193766129849327617, -1.517977999999999440E-15, 0.8545454545454557183 ) ) ;
#1040=CARTESIAN_POINT ( 'NONE',  ( 64.93393739769619799, 11.38381105532070059, -62.44999999999999574 ) ) ;
#1050=CYLINDRICAL_SURFACE ( 'NONE', #23550, 0.4999999999999994449 ) ;
#1065=CARTESIAN_POINT ( 'NONE',  ( 71.03049636386479904, 1.383411777981069957, -70.37541122638330648 ) ) ;
#1071=CARTESIAN_POINT ( 'NONE',  ( 73.02743803608620965, 1.099344084866040072, -69.05806188122140554 ) ) ;
#1074=CARTESIAN_POINT ( 'NONE',  ( 73.00373354607030763, 1.334812829108570131, -62.63859554625260273 ) ) ;
#1078=CARTESIAN_POINT ( 'NONE',  ( 72.23968433060379368, 1.026088617261680103, -61.27424404961239901 ) ) ;
#1080=CARTESIAN_POINT ( 'NONE',  ( 65.07863563811220331, 1.331842543267529821, -70.50106597067950531 ) ) ;
#1115=DIRECTION ( 'NONE',  ( 1.000000000000000000, 0.000000000000000000, 0.000000000000000000 ) ) ;
#1124=CARTESIAN_POINT ( 'NONE',  ( 63.50390619396998915, 1.388715606738730068, -62.57493595107060713 ) ) ;
#1129=CARTESIAN_POINT ( 'NONE',  ( 71.83998266832981017, 1.442158793902750036, -61.28605443723469648 ) ) ;
#1133=EDGE_CURVE ( 'NONE', #17335, #39508, #35624, .T. ) ;
#1151=CARTESIAN_POINT ( 'NONE',  ( 64.83819905826869956, 1.404650034021960092, -61.09597217184949614 ) ) ;
#1158=LINE ( 'NONE', #41768, #48093 ) ;
#1178=CIRCLE ( 'NONE', #11219, 5.999999999999998224 ) ;
#1181=CARTESIAN_POINT ( 'NONE',  ( 72.54418616719020463, 1.434949534324099885, -69.27291511353429598 ) ) ;
#1195=CARTESIAN_POINT ( 'NONE',  ( 64.45537117179310371, 1.245299373075330118, -61.01735943755249991 ) ) ;
#1196=VERTEX_POINT ( 'NONE', #34146 ) ;
#1232=FACE_OUTER_BOUND ( 'NONE', #36716, .T. ) ;
#1236=CARTESIAN_POINT ( 'NONE',  ( 72.31745269033760337, 1.031856533264720266, -61.34884692546020091 ) ) ;
#1240=CARTESIAN_POINT ( 'NONE',  ( 64.07670260090860381, 1.019777262794749895, -70.07076857027371375 ) ) ;
#1262=CARTESIAN_POINT ( 'NONE',  ( 65.07026117056290104, 1.388189907116970101, -61.01613942410280345 ) ) ;
#1268=CARTESIAN_POINT ( 'NONE',  ( 72.72759757326660690, 1.395196698723390138, -68.83033655198650536 ) ) ;
#1270=DIRECTION ( 'NONE',  ( 1.000000000000000000, 0.000000000000000000, 0.000000000000000000 ) ) ;
#1310=CARTESIAN_POINT ( 'NONE',  ( 65.07261215712630076, 1.274277262446069869, -60.70118609097839624 ) ) ;
#1330=CARTESIAN_POINT ( 'NONE',  ( 71.41555540048999262, 0.9948723650351710690, -70.66407068423170301 ) ) ;
#1333=TOROIDAL_SURFACE ( 'NONE', #50715, 1.499999999742110068, 0.4999999999874650269 ) ;
#1336=CARTESIAN_POINT ( 'NONE',  ( 73.05279713336409486, 1.186856010528209993, -68.92285061280580294 ) ) ;
#1343=CARTESIAN_POINT ( 'NONE',  ( 71.81752115780599866, 1.390572245144489960, -61.18038351632199578 ) ) ;
#1345=CARTESIAN_POINT ( 'NONE',  ( 64.95336252238109864, 1.097895768572089814, -70.68669971647908312 ) ) ;
#1349=DIRECTION ( 'NONE',  ( 1.000000000000000000, 0.000000000000000000, 0.000000000000000000 ) ) ;
#1370=EDGE_CURVE ( 'NONE', #38406, #50553, #31003, .T. ) ;
#1379=DIRECTION ( 'NONE',  ( 0.7071067811865475727, 0.000000000000000000, 0.7071067811865475727 ) ) ;
#1386=CARTESIAN_POINT ( 'NONE',  ( 63.23977555071240175, 1.186515949276300219, -62.33540229050490211 ) ) ;
#1391=CARTESIAN_POINT ( 'NONE',  ( 72.04429487089811346, 1.454949836291180132, -61.42720652002459758 ) ) ;
#1395=CARTESIAN_POINT ( 'NONE',  ( 63.33722961565180043, 1.138495159512730170, -69.18058936015049198 ) ) ;
#1400=AXIS2_PLACEMENT_3D ( 'NONE', #16334, #9264, #32287 ) ;
#1426=CARTESIAN_POINT ( 'NONE',  ( 73.23379646625190276, 0.8840451408750739093, -68.81103260973570457 ) ) ;
#1441=CARTESIAN_POINT ( 'NONE',  ( 73.04443511092439678, 0.9036513197889539661, -62.20214363597960272 ) ) ;
#1442=CARTESIAN_POINT ( 'NONE',  ( 63.43393739769620510, 1.883811055320669947, -62.44999999999999574 ) ) ;
#1443=CARTESIAN_POINT ( 'NONE',  ( 72.83009333885370040, 0.9561296872639739597, -69.38553930450309792 ) ) ;
#1453=CARTESIAN_POINT ( 'NONE',  ( 64.52993238696269884, 1.239065815390639980, -60.96725493808969532 ) ) ;
#1454=ORIENTED_EDGE ( 'NONE', *, *, #12920, .T. ) ;
#1496=CARTESIAN_POINT ( 'NONE',  ( 72.97999464611700660, 0.9170823515334789455, -62.11176382508629956 ) ) ;
#1498=CARTESIAN_POINT ( 'NONE',  ( 63.95618934260088650, 1.116860928049330015, -69.95003379205579108 ) ) ;
#1518=CARTESIAN_POINT ( 'NONE',  ( 65.08882305123219680, 1.387412027389909985, -61.00994802092580471 ) ) ;
#1561=CARTESIAN_POINT ( 'NONE',  ( 65.16938214696820353, 1.384887413063060180, -60.98363600610959878 ) ) ;
#1589=CIRCLE ( 'NONE', #30859, 0.5000000000000000000 ) ;
#1591=CARTESIAN_POINT ( 'NONE',  ( 73.04558532727548936, 1.003508719580009867, -69.08444824154609876 ) ) ;
#1594=CARTESIAN_POINT ( 'NONE',  ( 73.13312216970089708, 0.9955677559369568996, -62.34557165980569948 ) ) ;
#1601=CARTESIAN_POINT ( 'NONE',  ( 65.06933737855379718, 1.383922910988889976, -70.31893907080630868 ) ) ;
#1644=CARTESIAN_POINT ( 'NONE',  ( 63.18291598250529262, 1.096305581841160004, -62.33061120451039727 ) ) ;
#1653=CARTESIAN_POINT ( 'NONE',  ( 63.69560517452909920, 1.394111633877010092, -69.38462823658350942 ) ) ;
#1667=CARTESIAN_POINT ( 'NONE',  ( 63.93393739769619089, 1.883811055320669947, -62.44999999999999574 ) ) ;
#1669=ORIENTED_EDGE ( 'NONE', *, *, #47982, .T. ) ;
#1675=CARTESIAN_POINT ( 'NONE',  ( 63.55847417696450208, 1.399433130755639798, -62.41600958228519858 ) ) ;
#1694=CLOSED_SHELL ( 'NONE', ( #12356, #8471, #31755, #13954, #36652, #22567, #45074, #30523, #7885, #702, #2912, #45252, #37723, #9003, #46743, #8402, #4460, #20099, #15266, #34124, #28345, #49575, #27791, #22214, #15863, #26295, #9008, #37449, #17898, #38741, #43411, #42881, #8802, #12110, #8183, #36287, #47763, #3443, #45280, #22229, #29551, #19431, #12834, #5292, #24576, #26528, #15723, #18699, #6950, #13357, #2129, #42108, #44657, #24258, #4602, #2828, #26312, #45212, #9753, #26551 ) ) ;
#1702=CARTESIAN_POINT ( 'NONE',  ( 72.98949351566140820, 0.9150552061895700362, -69.17495778280340346 ) ) ;
#1706=CARTESIAN_POINT ( 'NONE',  ( 64.97340239734430156, 1.393731187554809958, -70.25064478522961053 ) ) ;
#1714=CARTESIAN_POINT ( 'NONE',  ( 64.34763627307550848, 1.432916438945960103, -61.30477097020899890 ) ) ;
#1730=AXIS2_PLACEMENT_3D ( 'NONE', #22923, #38944, #3034 ) ;
#1738=CARTESIAN_POINT ( 'NONE',  ( 64.93393739769619799, 1.383811055320669947, -62.44999999999999574 ) ) ;
#1749=CARTESIAN_POINT ( 'NONE',  ( 64.08748592165750324, 1.274156885185230070, -69.99444499429958455 ) ) ;
#1750=CARTESIAN_POINT ( 'NONE',  ( 68.13393739769620083, -20.61618894467929763, -65.65000000000000568 ) ) ;
#1764=CARTESIAN_POINT ( 'NONE',  ( 63.48611918674540533, 1.385702546077159925, -68.77407799673838440 ) ) ;
#1820=CARTESIAN_POINT ( 'NONE',  ( 65.14310169846920928, 1.336371993404959824, -60.77157093307350522 ) ) ;
#1845=CARTESIAN_POINT ( 'NONE',  ( 64.86358929490590697, 1.263903724274369811, -60.80800729848100161 ) ) ;
#1851=CARTESIAN_POINT ( 'NONE',  ( 72.85248830348810145, 1.369535599030039963, -68.77214795431979155 ) ) ;
#1854=CARTESIAN_POINT ( 'NONE',  ( 72.85976395805219852, 1.369613126987639928, -62.54642937019949755 ) ) ;
#1856=CARTESIAN_POINT ( 'NONE',  ( 71.61023385683570552, 1.007912009470880221, -60.76768544528139415 ) ) ;
#1860=CARTESIAN_POINT ( 'NONE',  ( 64.81454860220668479, 1.096305581841150012, -70.60102141519101338 ) ) ;
#1879=EDGE_LOOP ( 'NONE', ( #23046, #50505, #48861, #755 ) ) ;
#1904=CARTESIAN_POINT ( 'NONE',  ( 63.16328864814500577, 1.096044978595160035, -62.36169201816110075 ) ) ;
#1911=DIRECTION ( 'NONE',  ( -0.000000000000000000, 1.000000000000000000, 0.000000000000000000 ) ) ;
#1913=CARTESIAN_POINT ( 'NONE',  ( 63.64962603492929816, 1.332297187113020032, -69.43825451126340909 ) ) ;
#1920=CARTESIAN_POINT ( 'NONE',  ( 72.71580530985501412, 1.395841836299609895, -62.33173032533499480 ) ) ;
#1945=CARTESIAN_POINT ( 'NONE',  ( 73.01385068780759013, 0.9098571636355720083, -69.14090909090960224 ) ) ;
#1958=CARTESIAN_POINT ( 'NONE',  ( 73.07318775143939149, 0.8986939045430389905, -62.24348040161350326 ) ) ;
#1961=CARTESIAN_POINT ( 'NONE',  ( 72.65863549626330098, 1.000506532484680022, -69.59146369456030357 ) ) ;
#1962=CARTESIAN_POINT ( 'NONE',  ( 71.58179376171669617, 0.9036513197889510796, -60.73950228677190211 ) ) ;
#1965=CARTESIAN_POINT ( 'NONE',  ( 65.19259745005730622, 1.384447124000270035, -70.32375107525380997 ) ) ;
#1973=CARTESIAN_POINT ( 'NONE',  ( 63.71089178726140290, 1.048861872235970161, -61.59523540267399966 ) ) ;
#2006=CARTESIAN_POINT ( 'NONE',  ( 72.23968433060379368, 1.026088617261680103, -61.27424404961239901 ) ) ;
#2008=CARTESIAN_POINT ( 'NONE',  ( 64.75240447675760436, 1.412311545208970065, -70.17188921921470524 ) ) ;
#2017=B_SPLINE_CURVE_WITH_KNOTS ( 'NONE', 3,
 ( #45735, #26048, #1706, #14019, #17942, #41275, #10352, #2481, #49928, #29978, #46001, #5649, #1965, #9831, #22380, #26311 ),
 .UNSPECIFIED., .F., .F.,
 ( 4, 2, 2, 2, 2, 2, 2, 4 ),
 ( 0.000000000000000000, 0.07319275283554199651, 0.1391693187718069935, 0.1804046724819720060, 0.2061767685508260062, 0.2577209606885330073, 0.3401916681088649752, 0.4123535371016520124 ),
 .UNSPECIFIED. ) ;
#2020=DIRECTION ( 'NONE',  ( 0.5193766129849389790, 0.000000000000000000, -0.8545454545454520545 ) ) ;
#2023=CARTESIAN_POINT ( 'NONE',  ( 63.26014808640670140, 1.265401080857980087, -68.86031185997930493 ) ) ;
#2063=EDGE_CURVE ( 'NONE', #25175, #45766, #2640, .T. ) ;
#2081=CARTESIAN_POINT ( 'NONE',  ( 65.04142308672740569, 1.102581332775300016, -60.56179621591489592 ) ) ;
#2110=CARTESIAN_POINT ( 'NONE',  ( 73.01149271009099095, 1.265664290790580182, -62.44691083073610116 ) ) ;
#2112=CARTESIAN_POINT ( 'NONE',  ( 71.56253747416560884, 1.100585178972000033, -60.77016257896750062 ) ) ;
#2117=CARTESIAN_POINT ( 'NONE',  ( 64.91481325068460251, 1.325839985408290067, -70.42711907493250578 ) ) ;
#2129=ADVANCED_FACE ( 'NONE', ( #18871 ), #34593, .T. ) ;
#2130=DIRECTION ( 'NONE',  ( 1.377466541413789929E-11, -1.000000000000000000, 3.637457002807960330E-11 ) ) ;
#2133=CARTESIAN_POINT ( 'NONE',  ( 64.93393739769619799, 1.383811055320669947, -68.84999999999999432 ) ) ;
#2158=ORIENTED_EDGE ( 'NONE', *, *, #34472, .F. ) ;
#2163=CARTESIAN_POINT ( 'NONE',  ( 63.21464875163319874, 1.097545367735379918, -62.28124518314879765 ) ) ;
#2169=CARTESIAN_POINT ( 'NONE',  ( 72.33393739769618946, 1.883811055320669947, -68.84999999999999432 ) ) ;
#2173=CARTESIAN_POINT ( 'NONE',  ( 63.25101889642220954, 0.9479899806831150189, -69.13670813078400101 ) ) ;
#2174=DIRECTION ( 'NONE',  ( -1.000000000000000000, 0.000000000000000000, 0.000000000000000000 ) ) ;
#2182=VERTEX_POINT ( 'NONE', #41961 ) ;
#2192=LINE ( 'NONE', #13737, #42701 ) ;
#2218=CARTESIAN_POINT ( 'NONE',  ( 72.78068555023349973, 1.369286338573830086, -68.98634353402660224 ) ) ;
#2235=CARTESIAN_POINT ( 'NONE',  ( 63.66985334848389044, 1.334524132314560019, -61.83332299293069667 ) ) ;
#2268=CARTESIAN_POINT ( 'NONE',  ( 64.49087712817019735, 1.421946872762799963, -70.08110891980980739 ) ) ;
#2278=CARTESIAN_POINT ( 'NONE',  ( 63.50390619396989678, 1.388715606738730068, -68.72506404892941134 ) ) ;
#2288=CARTESIAN_POINT ( 'NONE',  ( 71.42224537953511287, 1.096044978595170027, -70.62064874955129312 ) ) ;
#2290=CIRCLE ( 'NONE', #19013, 0.5000000000000000000 ) ;
#2302=ORIENTED_EDGE ( 'NONE', *, *, #11741, .T. ) ;
#2311=CARTESIAN_POINT ( 'NONE',  ( 63.93393739769684458, 10.88381105532090487, -69.84999999999980957 ) ) ;
#2313=EDGE_CURVE ( 'NONE', #8182, #45770, #41955, .T. ) ;
#2333=ORIENTED_EDGE ( 'NONE', *, *, #13311, .T. ) ;
#2364=CARTESIAN_POINT ( 'NONE',  ( 72.83834671619840151, 1.382830464309369844, -62.68920552647019662 ) ) ;
#2371=CARTESIAN_POINT ( 'NONE',  ( 64.86108678489050305, 1.186856010528209993, -70.56885973566789971 ) ) ;
#2422=CARTESIAN_POINT ( 'NONE',  ( 63.53378487636381067, 1.392489938374319891, -68.91992234782470916 ) ) ;
#2427=CARTESIAN_POINT ( 'NONE',  ( 72.85979347688879670, 0.9828917932958439740, -61.95210570009940199 ) ) ;
#2436=ORIENTED_EDGE ( 'NONE', *, *, #33166, .T. ) ;
#2447=CIRCLE ( 'NONE', #9145, 5.500000000000005329 ) ;
#2481=CARTESIAN_POINT ( 'NONE',  ( 65.08882305123219680, 1.387412027389909985, -70.29005197907430613 ) ) ;
#2492=CARTESIAN_POINT ( 'NONE',  ( 63.47413392627220219, 1.313759828079400060, -62.14118152289400143 ) ) ;
#2509=ORIENTED_EDGE ( 'NONE', *, *, #26912, .F. ) ;
#2519=EDGE_CURVE ( 'NONE', #19450, #14121, #45321, .T. ) ;
#2536=CARTESIAN_POINT ( 'NONE',  ( 71.62240088300148955, 1.377110276564099900, -70.22675574799650633 ) ) ;
#2541=CARTESIAN_POINT ( 'NONE',  ( 63.51391054266390768, 1.390208944942409985, -68.75457626026799574 ) ) ;
#2552=CARTESIAN_POINT ( 'NONE',  ( 71.32344782937069283, 1.326324093417220240, -70.44093178352299844 ) ) ;
#2602=CARTESIAN_POINT ( 'NONE',  ( 65.05077035654539941, 1.384378348444520013, -60.98758765055369935 ) ) ;
#2606=CARTESIAN_POINT ( 'NONE',  ( 63.43393739769620510, 1.383811055320669947, -62.79342862858290886 ) ) ;
#2619=ORIENTED_EDGE ( 'NONE', *, *, #42232, .F. ) ;
#2633=CARTESIAN_POINT ( 'NONE',  ( 73.08075677931830683, 1.188042061556800144, -62.42534911081870064 ) ) ;
#2640=CIRCLE ( 'NONE', #5149, 6.000000000000005329 ) ;
#2643=CARTESIAN_POINT ( 'NONE',  ( 64.73967613295090473, 1.000225705806889964, -70.58924174254049433 ) ) ;
#2644=ORIENTED_EDGE ( 'NONE', *, *, #14707, .F. ) ;
#2694=PLANE ( 'NONE',  #47024 ) ;
#2696=CARTESIAN_POINT ( 'NONE',  ( 71.33582579397329937, 0.9940695285616559795, -60.58508503553749591 ) ) ;
#2698=CARTESIAN_POINT ( 'NONE',  ( 72.81668245960399588, 1.239065815390979930, -62.04599498926259571 ) ) ;
#2705=EDGE_LOOP ( 'NONE', ( #35832, #27499, #29235, #30784, #22657, #33958 ) ) ;
#2709=CARTESIAN_POINT ( 'NONE',  ( 64.93393739769619799, 10.88381105532070059, -69.84999999999999432 ) ) ;
#2718=EDGE_CURVE ( 'NONE', #33931, #51003, #24364, .T. ) ;
#2720=CYLINDRICAL_SURFACE ( 'NONE', #29707, 0.4999999999999994449 ) ;
#2754=CARTESIAN_POINT ( 'NONE',  ( 63.63571284094848579, 1.261444690199680085, -61.78778606023939091 ) ) ;
#2758=CARTESIAN_POINT ( 'NONE',  ( 73.18782247527531126, 0.8859637708054489691, -68.88406027352149863 ) ) ;
#2785=DIRECTION ( 'NONE',  ( 0.7071067811865475727, 0.000000000000000000, -0.7071067811865475727 ) ) ;
#2798=CARTESIAN_POINT ( 'NONE',  ( 71.62484648860579739, 0.9098571636355720083, -70.52991329011129551 ) ) ;
#2804=CARTESIAN_POINT ( 'NONE',  ( 63.47112272702528912, 1.372372808637209785, -68.90857576278490626 ) ) ;
#2816=CARTESIAN_POINT ( 'NONE',  ( 71.44853510719140388, 1.186515949276290227, -70.54416184698391135 ) ) ;
#2822=EDGE_CURVE ( 'NONE', #14121, #19450, #21628, .T. ) ;
#2828=ADVANCED_FACE ( 'NONE', ( #9860 ), #10125, .T. ) ;
#2857=CARTESIAN_POINT ( 'NONE',  ( 71.13601697155240799, 1.385888765344509999, -70.30422512560809878 ) ) ;
#2862=CARTESIAN_POINT ( 'NONE',  ( 64.86108678489040358, 1.186856010528209993, -60.73114026433219692 ) ) ;
#2865=CARTESIAN_POINT ( 'NONE',  ( 71.33393739769670105, 0.9098571636355720083, -70.12325384926869276 ) ) ;
#2866=DIRECTION ( 'NONE',  ( 2.754761277895425776E-28, -6.290312716002009228E-11, -1.000000000000000000 ) ) ;
#2890=ORIENTED_EDGE ( 'NONE', *, *, #5718, .T. ) ;
#2892=CARTESIAN_POINT ( 'NONE',  ( 73.02919596257699197, 0.9065823421260970072, -69.11945805671248877 ) ) ;
#2894=CARTESIAN_POINT ( 'NONE',  ( 72.93398937763220147, 1.264121749638659864, -62.30317625966389983 ) ) ;
#2900=CARTESIAN_POINT ( 'NONE',  ( 64.91485532786460055, 1.370853092582090094, -70.32939881202800336 ) ) ;
#2912=ADVANCED_FACE ( 'NONE', ( #28371 ), #50372, .T. ) ;
#2917=ORIENTED_EDGE ( 'NONE', *, *, #16683, .T. ) ;
#2932=ADVANCED_BREP_SHAPE_REPRESENTATION ( '', ( #10006, #20940 ), #854 ) ;
#2935=EDGE_LOOP ( 'NONE', ( #27341, #12969, #36013, #4740 ) ) ;
#2939=CARTESIAN_POINT ( 'NONE',  ( 63.54731047306190561, 1.396834109478120034, -62.44999999999999574 ) ) ;
#2953=CARTESIAN_POINT ( 'NONE',  ( 71.27262092911099955, 0.8838110553206759423, -60.53635606803790381 ) ) ;
#2972=ORIENTED_EDGE ( 'NONE', *, *, #46173, .T. ) ;
#3012=CARTESIAN_POINT ( 'NONE',  ( 63.62053861216700312, 1.408710407023049838, -62.16810826758219832 ) ) ;
#3015=CARTESIAN_POINT ( 'NONE',  ( 69.73393739769620936, 10.88381105532070059, -61.94999999999999574 ) ) ;
#3016=CARTESIAN_POINT ( 'NONE',  ( 73.03020225798630349, 1.267233196669030004, -68.81685389259939711 ) ) ;
#3034=DIRECTION ( 'NONE',  ( 1.000000000000000000, 0.000000000000000000, 0.000000000000000000 ) ) ;
#3055=CARTESIAN_POINT ( 'NONE',  ( 71.66453485656519717, 1.138495779907619854, -70.44670231041529007 ) ) ;
#3060=CARTESIAN_POINT ( 'NONE',  ( 63.51397770047800861, 1.389468113695450091, -68.84985728199801258 ) ) ;
#3073=CARTESIAN_POINT ( 'NONE',  ( 71.37448966235888292, 1.264489825601020190, -70.50788383491540401 ) ) ;
#3079=CARTESIAN_POINT ( 'NONE',  ( 68.13393739769620083, 0.8838110553206759423, -65.65000000000000568 ) ) ;
#3099=FACE_OUTER_BOUND ( 'NONE', #13841, .T. ) ;
#3115=CARTESIAN_POINT ( 'NONE',  ( 71.09849264842429761, 1.384887413063060180, -70.31636399389039127 ) ) ;
#3121=CARTESIAN_POINT ( 'NONE',  ( 64.89338513303370348, 1.264489825601020190, -60.79211616508469973 ) ) ;
#3152=CARTESIAN_POINT ( 'NONE',  ( 73.01702207920239118, 1.186614556332920234, -62.31696408872340243 ) ) ;
#3157=EDGE_LOOP ( 'NONE', ( #8378, #16844, #1669, #13148, #19636, #26018 ) ) ;
#3213=CARTESIAN_POINT ( 'NONE',  ( 71.05099032166229733, 1.383136297697689976, -60.93121850368469694 ) ) ;
#3215=CARTESIAN_POINT ( 'NONE',  ( 72.49387005411300322, 1.113948672550079788, -61.53426704495930011 ) ) ;
#3230=ORIENTED_EDGE ( 'NONE', *, *, #3666, .T. ) ;
#3269=CARTESIAN_POINT ( 'NONE',  ( 63.31978766800359892, 1.229084191802120030, -62.25930094257930136 ) ) ;
#3273=CARTESIAN_POINT ( 'NONE',  ( 72.80768847295010460, 1.384447124000270035, -68.59133994763901399 ) ) ;
#3274=VECTOR ( 'NONE', #25563, 1000.000000000000000 ) ;
#3311=CARTESIAN_POINT ( 'NONE',  ( 72.11129086675759936, 1.099201050715699957, -70.13622689935800736 ) ) ;
#3319=CARTESIAN_POINT ( 'NONE',  ( 63.28787718588009881, 0.9170817191178709527, -69.18823203240749820 ) ) ;
#3327=CARTESIAN_POINT ( 'NONE',  ( 71.31427394968270050, 1.395196698723390138, -70.24366017557039754 ) ) ;
#3351=CARTESIAN_POINT ( 'NONE',  ( 71.33393739769670105, 1.396834109478129804, -61.06337307536569625 ) ) ;
#3354=VECTOR ( 'NONE', #19123, 1000.000000000000000 ) ;
#3360=CARTESIAN_POINT ( 'NONE',  ( 64.93393739769609851, 11.38381105532070059, -61.94999999999999574 ) ) ;
#3378=CARTESIAN_POINT ( 'NONE',  ( 64.89029781878299730, 1.096291039689149871, -60.65158056017160249 ) ) ;
#3384=AXIS2_PLACEMENT_3D ( 'NONE', #29488, #44706, #25545 ) ;
#3390=CARTESIAN_POINT ( 'NONE',  ( 72.96483387528870423, 0.9208623934721549276, -69.20867653485849758 ) ) ;
#3409=ORIENTED_EDGE ( 'NONE', *, *, #14707, .T. ) ;
#3412=CARTESIAN_POINT ( 'NONE',  ( 72.81333620972418430, 1.370853092582090094, -62.43091793016829882 ) ) ;
#3443=ADVANCED_FACE ( 'NONE', ( #51539 ), #25754, .T. ) ;
#3453=CARTESIAN_POINT ( 'NONE',  ( 63.02699984107479025, 0.9952464559119579279, -68.78371246661670568 ) ) ;
#3472=DIRECTION ( 'NONE',  ( 0.000000000000000000, 0.000000000000000000, 1.000000000000000000 ) ) ;
#3474=CARTESIAN_POINT ( 'NONE',  ( 71.35858828687760536, 1.188042061556800144, -60.70318061837799917 ) ) ;
#3476=CARTESIAN_POINT ( 'NONE',  ( 72.49279582477680606, 1.028300555801489935, -61.52602141601349928 ) ) ;
#3501=DIRECTION ( 'NONE',  ( 0.000000000000000000, 1.000000000000000000, 0.000000000000000000 ) ) ;
#3505=AXIS2_PLACEMENT_3D ( 'NONE', #31358, #7032, #10962 ) ;
#3539=CARTESIAN_POINT ( 'NONE',  ( 72.92255733887110125, 1.374300485541529948, -68.58542282960749503 ) ) ;
#3540=CARTESIAN_POINT ( 'NONE',  ( 73.24087495431770378, 0.9952464559119579279, -62.51628753338329858 ) ) ;
#3567=VECTOR ( 'NONE', #12251, 1000.000000000000000 ) ;
#3575=CARTESIAN_POINT ( 'NONE',  ( 71.67217357260551580, 0.9170823515327879427, -70.49605724842400889 ) ) ;
#3580=CARTESIAN_POINT ( 'NONE',  ( 63.54731047306190561, 1.396834109478120034, -68.84999999999999432 ) ) ;
#3589=CARTESIAN_POINT ( 'NONE',  ( 71.54590618381259048, 1.188860127980290171, -70.48451794758248923 ) ) ;
#3594=CARTESIAN_POINT ( 'NONE',  ( 72.33393739769618946, 10.88381105532070059, -62.44999999999999574 ) ) ;
#3609=ORIENTED_EDGE ( 'NONE', *, *, #50771, .F. ) ;
#3618=CARTESIAN_POINT ( 'NONE',  ( 63.22343968446809725, 0.9036513197889539661, -69.09785636402048681 ) ) ;
#3635=CARTESIAN_POINT ( 'NONE',  ( 65.00323391584400667, 1.328073773609210084, -60.83220757462540007 ) ) ;
#3643=CARTESIAN_POINT ( 'NONE',  ( 71.71886329086420631, 0.9254890127224479901, -70.46161719983020078 ) ) ;
#3666=EDGE_CURVE ( 'NONE', #45770, #10362, #18922, .T. ) ;
#3669=CARTESIAN_POINT ( 'NONE',  ( 73.11834175676820280, 0.9272522097098119254, -62.30994913869029972 ) ) ;
#3675=CARTESIAN_POINT ( 'NONE',  ( 64.70533732122689230, 1.100585178971990041, -70.52983742103261022 ) ) ;
#3709=CARTESIAN_POINT ( 'NONE',  ( 63.17514626975080461, 1.276058558775509999, -68.69062364193268877 ) ) ;
#3723=EDGE_LOOP ( 'NONE', ( #51692, #50268, #43375, #15101 ) ) ;
#3731=CARTESIAN_POINT ( 'NONE',  ( 71.19525238180870019, 1.198183261254780030, -60.61312937625270081 ) ) ;
#3734=CARTESIAN_POINT ( 'NONE',  ( 72.79984470539690733, 0.9644290104361010751, -61.87674839326469822 ) ) ;
#3739=ORIENTED_EDGE ( 'NONE', *, *, #47152, .F. ) ;
#3746=B_SPLINE_CURVE_WITH_KNOTS ( 'NONE', 3,
 ( #44103, #28353, #16841, #43849, #16569, #27847, #7945, #44614, #36478, #4015, #12141, #13629, #31765, #20234, #16061, #11893, #36222, #39920, #47784, #8720 ),
 .UNSPECIFIED., .F., .F.,
 ( 4, 2, 2, 2, 2, 2, 2, 2, 2, 4 ),
 ( 0.000000000000000000, 0.08842031323028211320, 0.2261927319929608049, 0.3750000000000007216, 0.4999999999999988898, 0.5624999999999988898, 0.6624999999999994227, 0.7986771749361281092, 0.9352917551345886205, 1.000000000000000000 ),
 .UNSPECIFIED. ) ;
#3748=LINE ( 'NONE', #19960, #24289 ) ;
#3779=CARTESIAN_POINT ( 'NONE',  ( 63.24512423172760833, 1.266538207494809942, -62.46861950876320435 ) ) ;
#3789=EDGE_CURVE ( 'NONE', #23989, #16929, #20000, .T. ) ;
#3792=CARTESIAN_POINT ( 'NONE',  ( 63.33916480286269746, 1.229734285826310058, -62.22610693502240053 ) ) ;
#3796=CARTESIAN_POINT ( 'NONE',  ( 72.89060928222170332, 1.370937308141410238, -68.67294022748990301 ) ) ;
#3813=AXIS2_PLACEMENT_3D ( 'NONE', #15544, #31243, #23631 ) ;
#3828=CARTESIAN_POINT ( 'NONE',  ( 72.31796842074359688, 1.033013263524880099, -69.95125361163759692 ) ) ;
#3834=CARTESIAN_POINT ( 'NONE',  ( 63.45453858566830974, 1.370853092582090094, -68.86908206983169123 ) ) ;
#3851=CARTESIAN_POINT ( 'NONE',  ( 72.83393739769620367, 1.883811055320669947, -62.44999999999999574 ) ) ;
#3873=ORIENTED_EDGE ( 'NONE', *, *, #43714, .F. ) ;
#3880=AXIS2_PLACEMENT_3D ( 'NONE', #37818, #1911, #20771 ) ;
#3898=CIRCLE ( 'NONE', #42436, 0.4999999999999962252 ) ;
#3911=AXIS2_PLACEMENT_3D ( 'NONE', #4798, #13457, #29151 ) ;
#3918=EDGE_CURVE ( 'NONE', #4949, #28243, #8141, .T. ) ;
#3927=CARTESIAN_POINT ( 'NONE',  ( 73.11516444234040080, 0.9966178393190270324, -62.31828917185450223 ) ) ;
#3932=CARTESIAN_POINT ( 'NONE',  ( 64.68494473060250982, 1.102139304147779830, -70.51608385812039614 ) ) ;
#3938=CARTESIAN_POINT ( 'NONE',  ( 63.54731047306190561, 1.396834109478129804, -68.84999999999999432 ) ) ;
#3958=CARTESIAN_POINT ( 'NONE',  ( 71.20900144662560649, 1.388715606738720076, -61.01996879627380110 ) ) ;
#3964=CARTESIAN_POINT ( 'NONE',  ( 63.46018632244250313, 1.384447124000270035, -68.59133994763901399 ) ) ;
#3985=CARTESIAN_POINT ( 'NONE',  ( 71.52074786344320501, 0.8966068345641440285, -60.69721413447479819 ) ) ;
#3987=CARTESIAN_POINT ( 'NONE',  ( 72.15626456945139466, 1.443019669817199979, -61.49113342732780296 ) ) ;
#3995=EDGE_LOOP ( 'NONE', ( #51630, #38929, #49640, #34889, #16898, #16657 ) ) ;
#3996=CARTESIAN_POINT ( 'NONE',  ( 68.13393739769620083, 1.383811055320669947, -65.65000000000000568 ) ) ;
#4012=EDGE_CURVE ( 'NONE', #33090, #11777, #1589, .T. ) ;
#4015=CARTESIAN_POINT ( 'NONE',  ( 64.09336526242300636, 1.458407755040209919, -69.75916877191829713 ) ) ;
#4030=CARTESIAN_POINT ( 'NONE',  ( 63.05799534064709633, 1.101170701158060039, -62.53612607382319766 ) ) ;
#4053=AXIS2_PLACEMENT_3D ( 'NONE', #21380, #5423, #32911 ) ;
#4076=CARTESIAN_POINT ( 'NONE',  ( 72.50011317461130034, 1.195685806282509978, -69.72628720609149866 ) ) ;
#4089=CARTESIAN_POINT ( 'NONE',  ( 71.44880243016270072, 1.326666718054990035, -70.38086014838010840 ) ) ;
#4097=CYLINDRICAL_SURFACE ( 'NONE', #8912, 1.000000000000000888 ) ;
#4124=CIRCLE ( 'NONE', #9960, 0.5000000000000004441 ) ;
#4167=DIRECTION ( 'NONE',  ( 0.000000000000000000, 1.000000000000000000, 0.000000000000000000 ) ) ;
#4204=DIRECTION ( 'NONE',  ( 0.000000000000000000, 0.7071067811865492381, -0.7071067811865457964 ) ) ;
#4209=CARTESIAN_POINT ( 'NONE',  ( 63.31614497232158811, 1.328073773609220076, -68.78070348185231353 ) ) ;
#4220=CARTESIAN_POINT ( 'NONE',  ( 71.28940315555229290, 0.9947083095259759977, -70.74365995857920097 ) ) ;
#4221=CARTESIAN_POINT ( 'NONE',  ( 64.93393739769619799, 1.383811055320669947, -69.84999999999999432 ) ) ;
#4222=ORIENTED_EDGE ( 'NONE', *, *, #34472, .T. ) ;
#4231=CARTESIAN_POINT ( 'NONE',  ( 71.44595490529870574, 0.9958340104639651358, -60.65579263520140074 ) ) ;
#4233=CARTESIAN_POINT ( 'NONE',  ( 72.29430833700220660, 1.199410787637519960, -61.36310690539009727 ) ) ;
#4234=VECTOR ( 'NONE', #48785, 1000.000000000000000 ) ;
#4238=CARTESIAN_POINT ( 'NONE',  ( 65.05533261316259086, 1.330484379554840002, -70.49093568668439502 ) ) ;
#4277=CARTESIAN_POINT ( 'NONE',  ( 63.14473109323350286, 1.096110717717199812, -62.39142878032480155 ) ) ;
#4287=CARTESIAN_POINT ( 'NONE',  ( 63.25226693078700180, 1.024253516290730026, -62.17688587085479668 ) ) ;
#4304=CIRCLE ( 'NONE', #41149, 0.5000000000000004441 ) ;
#4332=CARTESIAN_POINT ( 'NONE',  ( 72.51126090687719739, 1.112168069084249922, -69.74683124610460538 ) ) ;
#4340=CARTESIAN_POINT ( 'NONE',  ( 64.64302830678670375, 0.9098571636355720083, -70.52991329011129551 ) ) ;
#4347=CARTESIAN_POINT ( 'NONE',  ( 71.62484648860569791, 0.9098571636355680115, -70.52991329011140920 ) ) ;
#4394=UNCERTAINTY_MEASURE_WITH_UNIT (LENGTH_MEASURE( 1.000000000000000082E-05 ), #23715, 'distance_accuracy_value', 'NONE');
#4408=EDGE_LOOP ( 'NONE', ( #44563, #7907, #15080, #17680 ) ) ;
#4434=CIRCLE ( 'NONE', #5309, 0.5000000000000000000 ) ;
#4436=CARTESIAN_POINT ( 'NONE',  ( 72.35673087767170841, 1.454949836291170140, -69.56035747320190410 ) ) ;
#4437=CARTESIAN_POINT ( 'NONE',  ( 63.50390619396998915, 1.388715606738730068, -62.57493595107060713 ) ) ;
#4460=ADVANCED_FACE ( 'NONE', ( #24627 ), #4828, .T. ) ;
#4465=CARTESIAN_POINT ( 'NONE',  ( 63.21844385136499511, 1.269319268680890067, -68.77895457036579785 ) ) ;
#4477=CARTESIAN_POINT ( 'NONE',  ( 71.15378634064809660, 1.278021359705829862, -70.61864533961639268 ) ) ;
#4486=CARTESIAN_POINT ( 'NONE',  ( 71.31509885739851029, 1.369976237678180109, -60.95504431261769440 ) ) ;
#4489=CARTESIAN_POINT ( 'NONE',  ( 71.39063606569699516, 1.391735898526160087, -61.04516847149080405 ) ) ;
#4492=CARTESIAN_POINT ( 'NONE',  ( 65.16938214696820353, 1.384887413063050188, -70.31636399389039127 ) ) ;
#4529=CARTESIAN_POINT ( 'NONE',  ( 63.35267264707980672, 1.373356196620449943, -62.69406858229250901 ) ) ;
#4537=CARTESIAN_POINT ( 'NONE',  ( 64.99178804968060774, 1.386446979194299933, -61.00873193152619933 ) ) ;
#4543=ORIENTED_EDGE ( 'NONE', *, *, #19788, .T. ) ;
#4584=CARTESIAN_POINT ( 'NONE',  ( 72.32470129585499308, 1.409272994606969975, -69.70523042975179351 ) ) ;
#4596=CARTESIAN_POINT ( 'NONE',  ( 64.91115770917910766, 1.389801772588449946, -61.03316673290180461 ) ) ;
#4602=ADVANCED_FACE ( 'NONE', ( #5659 ), #41286, .T. ) ;
#4640=CARTESIAN_POINT ( 'NONE',  ( 63.91099139885979241, 1.441354206319580111, -69.60041390115910076 ) ) ;
#4659=STYLED_ITEM ( 'NONE', ( #16128 ), #10006 ) ;
#4667=CARTESIAN_POINT ( 'NONE',  ( 64.95360084570980064, 1.395196698723390138, -61.05633982442969909 ) ) ;
#4694=CARTESIAN_POINT ( 'NONE',  ( 72.83393739769620367, 0.8838110553206759423, -68.50657137141709541 ) ) ;
#4725=CARTESIAN_POINT ( 'NONE',  ( 63.27605356278090198, 1.264489825601020190, -68.89055226466270199 ) ) ;
#4737=CARTESIAN_POINT ( 'NONE',  ( 71.40893329644839582, 0.8879664753683469414, -70.67740027405400838 ) ) ;
#4740=ORIENTED_EDGE ( 'NONE', *, *, #43940, .T. ) ;
#4743=CARTESIAN_POINT ( 'NONE',  ( 73.10713808934470137, 0.9971903505820729485, -68.99379187066199393 ) ) ;
#4746=CARTESIAN_POINT ( 'NONE',  ( 72.85271889401160195, 1.383136297697689976, -62.73294707603399445 ) ) ;
#4749=CARTESIAN_POINT ( 'NONE',  ( 71.42252419164299226, 1.263738073398980033, -60.81786852648419028 ) ) ;
#4750=FACE_OUTER_BOUND ( 'NONE', #30338, .T. ) ;
#4751=CARTESIAN_POINT ( 'NONE',  ( 71.96129531186480222, 1.170697810385400217, -61.07138367721960037 ) ) ;
#4754=CARTESIAN_POINT ( 'NONE',  ( 65.11408845474450402, 1.278021359705819870, -70.61864533961639268 ) ) ;
#4780=CARTESIAN_POINT ( 'NONE',  ( 64.93393739769619799, 1.883811055320669947, -69.84999999999999432 ) ) ;
#4795=CIRCLE ( 'NONE', #22365, 0.9999999999999964473 ) ;
#4797=CARTESIAN_POINT ( 'NONE',  ( 63.28287142701680068, 1.331842543267529821, -62.59469824041600816 ) ) ;
#4798=CARTESIAN_POINT ( 'NONE',  ( 71.83393739769618946, 10.88381105532070059, -62.44999999999999574 ) ) ;
#4805=CARTESIAN_POINT ( 'NONE',  ( 64.75883903758510485, 0.9989215084294049696, -60.69776330465320058 ) ) ;
#4818=ORIENTED_EDGE ( 'NONE', *, *, #3789, .T. ) ;
#4827=DIRECTION ( 'NONE',  ( 0.000000000000000000, 0.000000000000000000, -1.000000000000000000 ) ) ;
#4828=B_SPLINE_SURFACE_WITH_KNOTS ( 'NONE', 3, 3, ( 
 ( #44571, #20194, #8163, #45093, #4477, #9200, #16276, #40639, #5007, #31980 ),
 ( #25152, #1065, #36434, #28572, #17061, #8420, #48252, #41157, #21221, #40127 ),
 ( #28312, #12099, #33014, #16797, #20704, #36695, #5270, #4220, #8672, #44837 ),
 ( #795, #28832, #20447, #13145, #292, #47999, #24368, #47, #16024, #29095 ),
 ( #28055, #44311, #40381, #44057, #24106, #36184, #32229, #32745, #49037, #48772 ),
 ( #12876, #12346, #542, #8943, #16528, #32478, #48508, #24885, #40897, #4737 ),
 ( #12609, #20967, #36968, #42127, #50510, #18262, #9461, #1330, #26117, #33282 ),
 ( #37233, #50253, #49299, #17318, #13395, #19041, #18530, #38721, #15121, #14341 ),
 ( #38449, #22957, #46589, #30310, #46331, #26633, #2288, #46850, #29353, #14600 ),
 ( #10418, #45359, #11197, #6227, #26371, #22183, #7008, #31080, #42387, #6484 ),
 ( #38193, #22442, #27158, #2552, #3073, #10937, #34503, #30568, #26903, #10678 ),
 ( #42650, #6748, #22705, #43166, #51021, #2816, #34761, #50766, #38979, #30822 ),
 ( #42910, #35017, #47108, #7260, #15893, #47361, #8282, #20315, #24230, #31590 ),
 ( #166, #51541, #51790, #28180, #27927, #36056, #43929, #15638, #44182, #23976 ),
 ( #3327, #47869, #19562, #43420, #35286, #47611, #7520, #20063, #35551, #40255 ),
 ( #23727, #32358, #39743, #4089, #11712, #3589, #39229, #51284, #35806, #4347 ) ),
 .UNSPECIFIED., .F., .F., .F.,
 ( 4, 2, 2, 2, 2, 2, 2, 4 ),
 ( 4, 1, 1, 1, 1, 1, 1, 4 ),
 ( -1.891009999999999936E-14, 0.07216186899279498912, 0.1546325764131530056, 0.2061767685508769932, 0.2319488646197390147, 0.2731842183299179605, 0.3391607842662049954, 0.4123535371017729712 ),
 ( 0.000000000000000000, 0.1428571428571430157, 0.2857142857142860315, 0.4285714285714289917, 0.5714285714285709528, 0.7142857142857139685, 0.8571428571428569843, 1.000000000000000000 ),
 .UNSPECIFIED. ) ;
#4853=CARTESIAN_POINT ( 'NONE',  ( 72.20074884524329661, 1.275252243133929930, -69.97672534177469572 ) ) ;
#4856=CARTESIAN_POINT ( 'NONE',  ( 72.31796842074339793, 1.033013263524880099, -69.95125361163771061 ) ) ;
#4866=CARTESIAN_POINT ( 'NONE',  ( 64.12726891144080810, 1.458412159422780130, -61.50690654180700534 ) ) ;
#4895=CARTESIAN_POINT ( 'NONE',  ( 71.62484648860579739, 0.9098571636355720083, -60.77008670988870165 ) ) ;
#4908=CARTESIAN_POINT ( 'NONE',  ( 64.09336526242300636, 1.458407755040209919, -69.75916877191829713 ) ) ;
#4931=CARTESIAN_POINT ( 'NONE',  ( 65.19259745005730622, 1.384447124000270035, -60.97624892474630087 ) ) ;
#4945=DIRECTION ( 'NONE',  ( 0.000000000000000000, 1.000000000000000000, 0.000000000000000000 ) ) ;
#4949=VERTEX_POINT ( 'NONE', #31796 ) ;
#4963=VERTEX_POINT ( 'NONE', #7728 ) ;
#4984=FACE_OUTER_BOUND ( 'NONE', #24961, .T. ) ;
#4990=LINE ( 'NONE', #8146, #29886 ) ;
#4993=CARTESIAN_POINT ( 'NONE',  ( 63.16328864814500577, 1.096044978595170027, -68.93830798183888930 ) ) ;
#5007=CARTESIAN_POINT ( 'NONE',  ( 71.25019707560579718, 0.9212109678634080590, -70.77727272727280194 ) ) ;
#5013=CARTESIAN_POINT ( 'NONE',  ( 72.77520546617009245, 1.386446979194289941, -68.79214934801569825 ) ) ;
#5016=CARTESIAN_POINT ( 'NONE',  ( 73.19748134167231512, 1.099973129953850215, -62.51484271732719833 ) ) ;
#5018=CARTESIAN_POINT ( 'NONE',  ( 71.41482173131041122, 1.096036836948800053, -60.67470092284240479 ) ) ;
#5020=CARTESIAN_POINT ( 'NONE',  ( 72.07540109225739400, 1.000506532484820132, -61.12530190143370135 ) ) ;
#5022=CARTESIAN_POINT ( 'NONE',  ( 64.85894149894409111, 0.8879664753683379486, -70.67740027405400838 ) ) ;
#5041=B_SPLINE_SURFACE_WITH_KNOTS ( 'NONE', 3, 3, ( 
 ( #43057, #17079, #45110, #49054, #8692, #4754, #32244, #20209, #5286, #16542 ),
 ( #28325, #813, #33029, #44074, #17336, #13163, #36197, #29111, #9216, #25170 ),
 ( #8437, #21238, #33301, #307, #28586, #40396, #24119, #41177, #28849, #32761 ),
 ( #37247, #16288, #20722, #1345, #12112, #28068, #1080, #32496, #8176, #12362 ),
 ( #48521, #48266, #24643, #44853, #40139, #36710, #4238, #44325, #24381, #4492 ),
 ( #5022, #12628, #8957, #48786, #20459, #36449, #12894, #556, #44586, #24900 ),
 ( #16814, #40655, #40913, #20987, #36983, #50074, #46419, #25685, #6314, #22271 ),
 ( #21756, #17839, #30136, #30397, #25426, #33811, #10246, #45373, #26204, #41428 ),
 ( #49824, #37501, #13661, #46159, #42215, #13916, #38544, #45892, #1601, #18098 ),
 ( #38282, #29624, #29372, #50341, #2371, #37766, #6054, #41958, #42478, #18348 ),
 ( #14427, #49315, #34325, #1860, #14169, #22012, #33560, #29872, #49577, #9978 ),
 ( #18611, #41687, #10506, #25940, #38023, #6570, #2117, #26464, #5795, #45625 ),
 ( #34064, #22532, #2643, #13410, #9479, #5545, #21500, #17588, #9725, #11799 ),
 ( #23045, #15467, #39568, #15716, #19644, #31164, #27239, #2900, #42740, #27762 ),
 ( #43757, #50850, #23293, #3675, #14684, #39824, #35637, #6838, #51622, #31674 ),
 ( #42997, #30906, #7858, #3932, #22787, #51106, #11022, #46678, #47697, #51367 ) ),
 .UNSPECIFIED., .F., .F., .F.,
 ( 4, 2, 2, 2, 2, 2, 2, 4 ),
 ( 4, 1, 1, 1, 1, 1, 1, 4 ),
 ( 0.000000000000000000, 0.07216186899278899392, 0.1546325764131200042, 0.2061767685508260062, 0.2319488646196800063, 0.2731842183298449633, 0.3391607842661090166, 0.4123535371016520124 ),
 ( 0.000000000000000000, 0.1428571428571430157, 0.2857142857142860315, 0.4285714285714289917, 0.5714285714285709528, 0.7142857142857139685, 0.8571428571428569843, 1.000000000000000000 ),
 .UNSPECIFIED. ) ;
#5070=CARTESIAN_POINT ( 'NONE',  ( 63.19277908840750513, 0.9325382164350239922, -62.24624853760359855 ) ) ;
#5100=CARTESIAN_POINT ( 'NONE',  ( 63.76999183493178691, 1.442158793902849956, -61.94395472936509606 ) ) ;
#5105=ORIENTED_EDGE ( 'NONE', *, *, #50128, .T. ) ;
#5114=VECTOR ( 'NONE', #35544, 1000.000000000000000 ) ;
#5126=CARTESIAN_POINT ( 'NONE',  ( 72.83393739769620367, 1.883811055320669947, -62.44999999999999574 ) ) ;
#5127=CARTESIAN_POINT ( 'NONE',  ( 73.01560786460549934, 1.024253516290730026, -69.12311412914529285 ) ) ;
#5141=CARTESIAN_POINT ( 'NONE',  ( 64.43841554592269460, 1.426105412861020216, -61.24861962585290343 ) ) ;
#5146=DIRECTION ( 'NONE',  ( 0.000000000000000000, 1.000000000000000000, 0.000000000000000000 ) ) ;
#5149=AXIS2_PLACEMENT_3D ( 'NONE', #40918, #25429, #1349 ) ;
#5177=CARTESIAN_POINT ( 'NONE',  ( 65.13393739769620083, 1.383811055320669947, -65.65000000000000568 ) ) ;
#5184=CARTESIAN_POINT ( 'NONE',  ( 64.08753032830780683, 1.107039789628780024, -70.07374305313838647 ) ) ;
#5196=DIRECTION ( 'NONE',  ( 0.000000000000000000, -1.000000000000000000, 0.000000000000000000 ) ) ;
#5218=CARTESIAN_POINT ( 'NONE',  ( 63.43393739769620510, 1.383811055320669947, -68.50657137141709541 ) ) ;
#5229=CARTESIAN_POINT ( 'NONE',  ( 72.14060588395169304, 1.458412159422780130, -69.79309345819311261 ) ) ;
#5230=CARTESIAN_POINT ( 'NONE',  ( 63.44018392888030178, 1.383811055320669947, -62.77287342953649585 ) ) ;
#5246=CARTESIAN_POINT ( 'NONE',  ( 72.83393739769620367, 1.883811055320669947, -68.84999999999999432 ) ) ;
#5270=CARTESIAN_POINT ( 'NONE',  ( 71.26909468036909345, 1.099973129953850215, -70.71354394397609155 ) ) ;
#5271=DIRECTION ( 'NONE',  ( 0.000000000000000000, 0.000000000000000000, -1.000000000000000000 ) ) ;
#5277=CARTESIAN_POINT ( 'NONE',  ( 73.09245838956729813, 1.096153228089730147, -68.95757157983499042 ) ) ;
#5282=CARTESIAN_POINT ( 'NONE',  ( 71.33379467969419352, 1.389468113695450091, -61.03004030278179926 ) ) ;
#5284=CARTESIAN_POINT ( 'NONE',  ( 71.85037942476280648, 1.056975075119080065, -60.94761944900709949 ) ) ;
#5286=CARTESIAN_POINT ( 'NONE',  ( 65.25794138637670017, 1.383811055320669947, -70.38195992526379996 ) ) ;
#5287=ORIENTED_EDGE ( 'NONE', *, *, #49903, .F. ) ;
#5288=VERTEX_POINT ( 'NONE', #809 ) ;
#5292=ADVANCED_FACE ( 'NONE', ( #4750 ), #20717, .T. ) ;
#5309=AXIS2_PLACEMENT_3D ( 'NONE', #5246, #12853, #14995 ) ;
#5323=AXIS2_PLACEMENT_3D ( 'NONE', #45286, #36899, #17502 ) ;
#5330=CARTESIAN_POINT ( 'NONE',  ( 63.22343968446819673, 0.9036513197889520788, -62.20214363597960272 ) ) ;
#5340=CARTESIAN_POINT ( 'NONE',  ( 63.49874256803619943, 1.370386981549569727, -69.01316122778010254 ) ) ;
#5381=CARTESIAN_POINT ( 'NONE',  ( 72.72593655015040781, 1.394012070863599906, -68.94123343940819382 ) ) ;
#5394=CARTESIAN_POINT ( 'NONE',  ( 64.48466142462660855, 1.149538111077180069, -60.93632371623740340 ) ) ;
#5423=DIRECTION ( 'NONE',  ( 0.000000000000000000, 0.000000000000000000, -1.000000000000000000 ) ) ;
#5438=CARTESIAN_POINT ( 'NONE',  ( 63.94153426497989301, 1.200157450721869967, -69.90579656221390792 ) ) ;
#5449=EDGE_CURVE ( 'NONE', #41163, #49378, #23549, .T. ) ;
#5462=CARTESIAN_POINT ( 'NONE',  ( 65.01129443250870565, 1.391252479931859964, -61.03617692120100457 ) ) ;
#5468=CARTESIAN_POINT ( 'NONE',  ( 72.76779797359338886, 1.388189907116970101, -68.71367622713330547 ) ) ;
#5515=CARTESIAN_POINT ( 'NONE',  ( 64.92520290936280958, 0.8850831926798620186, -60.57999765399179637 ) ) ;
#5534=ORIENTED_EDGE ( 'NONE', *, *, #8742, .F. ) ;
#5536=CARTESIAN_POINT ( 'NONE',  ( 73.02809924467999281, 1.186515949276290227, -68.96459770949519452 ) ) ;
#5539=CARTESIAN_POINT ( 'NONE',  ( 73.06808687136680192, 1.187415670095769871, -62.40340069948359769 ) ) ;
#5541=CARTESIAN_POINT ( 'NONE',  ( 71.48076113803239195, 1.264121749638659864, -60.84994802006399794 ) ) ;
#5543=CARTESIAN_POINT ( 'NONE',  ( 71.53657551413809301, 1.402020837641559936, -61.10185970516889853 ) ) ;
#5545=CARTESIAN_POINT ( 'NONE',  ( 64.84535060374950888, 1.263738073398980033, -70.48213147351589214 ) ) ;
#5561=EDGE_CURVE ( 'NONE', #8299, #7479, #19126, .T. ) ;
#5588=CARTESIAN_POINT ( 'NONE',  ( 63.13746035244330557, 0.8910129994591549085, -62.32805707658469885 ) ) ;
#5597=CARTESIAN_POINT ( 'NONE',  ( 63.42025297602360467, 1.149536861557900247, -69.29926477292440268 ) ) ;
#5616=CARTESIAN_POINT ( 'NONE',  ( 63.61158869431360330, 1.412203896157240068, -62.26955982508579979 ) ) ;
#5629=CARTESIAN_POINT ( 'NONE',  ( 73.24758132965830271, 0.8838110553206740549, -68.78868353141480441 ) ) ;
#5645=CARTESIAN_POINT ( 'NONE',  ( 72.96483387528880371, 0.9208623934721590354, -69.20867653485849758 ) ) ;
#5648=CARTESIAN_POINT ( 'NONE',  ( 71.33393739770029640, 10.88381105532060111, -69.84999999999840270 ) ) ;
#5649=CARTESIAN_POINT ( 'NONE',  ( 65.16938214696820353, 1.384887413063050188, -70.31636399389039127 ) ) ;
#5651=DIRECTION ( 'NONE',  ( -1.000000000000000000, 0.000000000000000000, 0.000000000000000000 ) ) ;
#5657=CARTESIAN_POINT ( 'NONE',  ( 64.00995881370980101, 1.028300555801489935, -61.29114157291949994 ) ) ;
#5659=FACE_OUTER_BOUND ( 'NONE', #22129, .T. ) ;
#5677=ORIENTED_EDGE ( 'NONE', *, *, #2822, .F. ) ;
#5692=CARTESIAN_POINT ( 'NONE',  ( 63.92800470363879839, 1.456055302763120007, -69.58268673945899252 ) ) ;
#5718=EDGE_CURVE ( 'NONE', #8182, #39508, #34183, .T. ) ;
#5755=CARTESIAN_POINT ( 'NONE',  ( 65.02006347151939281, 1.101170701158060039, -60.57405794295090118 ) ) ;
#5778=CARTESIAN_POINT ( 'NONE',  ( 64.78392625511199299, 1.096932441169210071, -60.71856768636379797 ) ) ;
#5785=CARTESIAN_POINT ( 'NONE',  ( 73.11834175676820280, 0.9272522097098119254, -68.99005086130968323 ) ) ;
#5787=LINE ( 'NONE', #49815, #9464 ) ;
#5788=CARTESIAN_POINT ( 'NONE',  ( 72.85248830348810145, 1.369535599030039963, -62.52785204568030508 ) ) ;
#5790=CARTESIAN_POINT ( 'NONE',  ( 71.58938403497960223, 1.005545696829380109, -60.75297091621269630 ) ) ;
#5795=CARTESIAN_POINT ( 'NONE',  ( 65.00985940095789317, 1.385702546077159925, -70.29781821095090777 ) ) ;
#5818=CIRCLE ( 'NONE', #48458, 0.5000000000000018874 ) ;
#5838=CARTESIAN_POINT ( 'NONE',  ( 63.47556362806851382, 1.384708701328919878, -62.55544205298410532 ) ) ;
#5846=EDGE_CURVE ( 'NONE', #49949, #41228, #10049, .T. ) ;
#5848=CARTESIAN_POINT ( 'NONE',  ( 63.71146986217769381, 1.338416928215059976, -69.52371897276981372 ) ) ;
#5852=CARTESIAN_POINT ( 'NONE',  ( 71.25019707560579718, 0.9212109678634080590, -60.52272727272730179 ) ) ;
#5875=CARTESIAN_POINT ( 'NONE',  ( 73.26121012496899709, 0.8838110553206759423, -68.76625967790960203 ) ) ;
#5891=CARTESIAN_POINT ( 'NONE',  ( 73.16133767175010405, 0.8879664753683469414, -62.37500410124779648 ) ) ;
#5893=CARTESIAN_POINT ( 'NONE',  ( 72.69742484592399023, 1.402336724396409995, -68.91862208776170462 ) ) ;
#5901=CARTESIAN_POINT ( 'NONE',  ( 68.13393739769620083, 0.8838110553206759423, -65.65000000000000568 ) ) ;
#5907=CARTESIAN_POINT ( 'NONE',  ( 63.86181505067950326, 1.033004162168289941, -61.43684260791489748 ) ) ;
#5915=CARTESIAN_POINT ( 'NONE',  ( 71.33393739769790898, 11.38381099282070075, -62.44999999999869544 ) ) ;
#5946=CARTESIAN_POINT ( 'NONE',  ( 64.45072088349949979, 1.390546226751929959, -70.11984532146888682 ) ) ;
#5947=CYLINDRICAL_SURFACE ( 'NONE', #7153, 5.999999999999998224 ) ;
#5958=CARTESIAN_POINT ( 'NONE',  ( 63.18115153217100755, 0.8966068345641440285, -69.03681046574699565 ) ) ;
#5972=CARTESIAN_POINT ( 'NONE',  ( 72.33393739769618946, 10.88381105532070059, -68.84999999999999432 ) ) ;
#6000=LINE ( 'NONE', #37707, #33693 ) ;
#6001=AXIS2_PLACEMENT_3D ( 'NONE', #1738, #21892, #22148 ) ;
#6041=CARTESIAN_POINT ( 'NONE',  ( 64.95388650200960967, 1.388313565858570131, -61.02265534841509975 ) ) ;
#6046=CARTESIAN_POINT ( 'NONE',  ( 73.01377481872879116, 1.100585178972000033, -69.07860007646939948 ) ) ;
#6048=CARTESIAN_POINT ( 'NONE',  ( 73.20448466830819712, 0.9214125008369580261, -62.44212918470660156 ) ) ;
#6050=CARTESIAN_POINT ( 'NONE',  ( 71.54199927891758648, 1.099344084866040072, -60.75649936161010345 ) ) ;
#6054=CARTESIAN_POINT ( 'NONE',  ( 64.95585434546930514, 1.326578174762039986, -70.44621455782281316 ) ) ;
#6064=DIRECTION ( 'NONE',  ( 0.000000000000000000, -1.000000000000000000, 0.000000000000000000 ) ) ;
#6067=CARTESIAN_POINT ( 'NONE',  ( 64.93393739769619799, 11.38381105532070059, -69.34999999999999432 ) ) ;
#6100=CARTESIAN_POINT ( 'NONE',  ( 63.29194469617720387, 1.263903724274369811, -62.37965189720969761 ) ) ;
#6111=CARTESIAN_POINT ( 'NONE',  ( 63.38185292195529286, 1.308647200627810259, -68.98304916495260386 ) ) ;
#6117=CARTESIAN_POINT ( 'NONE',  ( 72.72470740462131289, 1.321111291668189747, -62.02365098255700104 ) ) ;
#6152=FACE_OUTER_BOUND ( 'NONE', #887, .T. ) ;
#6155=CARTESIAN_POINT ( 'NONE',  ( 72.73111481579618953, 1.374525224580429805, -69.09669985268870107 ) ) ;
#6166=FACE_OUTER_BOUND ( 'NONE', #34808, .T. ) ;
#6169=CARTESIAN_POINT ( 'NONE',  ( 63.83278432315639606, 1.031856533264720266, -61.46648470735859604 ) ) ;
#6195=ORIENTED_EDGE ( 'NONE', *, *, #5846, .T. ) ;
#6207=CARTESIAN_POINT ( 'NONE',  ( 64.41724364727048169, 1.057016615258209891, -70.35216550789259315 ) ) ;
#6217=CARTESIAN_POINT ( 'NONE',  ( 63.50007682179899149, 1.388189907116970101, -68.71367622713330547 ) ) ;
#6227=CARTESIAN_POINT ( 'NONE',  ( 71.31202044992319600, 1.326578174762039986, -70.44621455782281316 ) ) ;
#6235=CARTESIAN_POINT ( 'NONE',  ( 71.54045699608259667, 0.8986939045430389905, -70.58925035374331003 ) ) ;
#6305=CARTESIAN_POINT ( 'NONE',  ( 72.86479754607628934, 1.326666718054979821, -68.96486503246650557 ) ) ;
#6307=CARTESIAN_POINT ( 'NONE',  ( 72.80030139158668590, 1.384887413063060180, -62.68544474927200127 ) ) ;
#6314=CARTESIAN_POINT ( 'NONE',  ( 65.09799605061500927, 1.383357884654609959, -70.32891903079600127 ) ) ;
#6324=FACE_OUTER_BOUND ( 'NONE', #35678, .T. ) ;
#6351=CARTESIAN_POINT ( 'NONE',  ( 63.40197747243239945, 1.383811055320669947, -68.52599601131950635 ) ) ;
#6357=CARTESIAN_POINT ( 'NONE',  ( 63.25162284297759641, 1.007912009470880221, -62.17370354086050099 ) ) ;
#6365=CARTESIAN_POINT ( 'NONE',  ( 63.34671918778160205, 1.229987731989950150, -69.08683410666979796 ) ) ;
#6370=CARTESIAN_POINT ( 'NONE',  ( 72.98301648142211207, 1.028860820852099955, -62.13042434682570558 ) ) ;
#6373=VECTOR ( 'NONE', #12090, 1000.000000000000000 ) ;
#6409=VERTEX_POINT ( 'NONE', #22538 ) ;
#6430=CARTESIAN_POINT ( 'NONE',  ( 63.75074504544879517, 1.428542319231299818, -61.92421027702900460 ) ) ;
#6457=CIRCLE ( 'NONE', #32334, 0.5000000000000004441 ) ;
#6466=CARTESIAN_POINT ( 'NONE',  ( 64.45078520382470799, 1.153637615392060223, -70.33899815792979382 ) ) ;
#6473=CARTESIAN_POINT ( 'NONE',  ( 64.93393739769619799, 11.38381105532070059, -68.84999999999999432 ) ) ;
#6475=CARTESIAN_POINT ( 'NONE',  ( 63.15932386229340523, 0.8936201581567889685, -69.00461532610479765 ) ) ;
#6484=CARTESIAN_POINT ( 'NONE',  ( 71.47612964547808190, 0.8925687589132640376, -70.63296852923029689 ) ) ;
#6507=CARTESIAN_POINT ( 'NONE',  ( 64.43393739769710749, 11.38381105532080184, -69.34999999999971010 ) ) ;
#6530=CARTESIAN_POINT ( 'NONE',  ( 64.84562941585738827, 1.096044978595170027, -60.67935125044880351 ) ) ;
#6554=ORIENTED_EDGE ( 'NONE', *, *, #31874, .T. ) ;
#6560=CARTESIAN_POINT ( 'NONE',  ( 72.81285642849219641, 1.383357884654609959, -62.61405865291869333 ) ) ;
#6566=AXIS2_PLACEMENT_3D ( 'NONE', #35315, #8059, #23756 ) ;
#6570=CARTESIAN_POINT ( 'NONE',  ( 64.86358929490600644, 1.263903724274369811, -70.49199270151910923 ) ) ;
#6606=FACE_OUTER_BOUND ( 'NONE', #37621, .T. ) ;
#6625=CARTESIAN_POINT ( 'NONE',  ( 71.36046776202630326, 0.9940423591679348192, -60.60059430635039490 ) ) ;
#6627=CARTESIAN_POINT ( 'NONE',  ( 72.94959658490671472, 1.034647430441060001, -62.08420298997459952 ) ) ;
#6628=CIRCLE ( 'NONE', #21663, 5.999999999999998224 ) ;
#6630=EDGE_CURVE ( 'NONE', #4963, #2182, #36440, .T. ) ;
#6641=CARTESIAN_POINT ( 'NONE',  ( 63.47971227208819300, 1.385888765344509999, -68.65207957385619864 ) ) ;
#6654=EDGE_CURVE ( 'NONE', #7479, #9073, #41115, .T. ) ;
#6676=CARTESIAN_POINT ( 'NONE',  ( 63.16529205807979963, 1.278021359705829862, -62.63015105704829466 ) ) ;
#6677=LINE ( 'NONE', #10613, #39044 ) ;
#6678=AXIS2_PLACEMENT_3D ( 'NONE', #13966, #34112, #29920 ) ;
#6691=CARTESIAN_POINT ( 'NONE',  ( 63.72050982575409961, 1.191618978581419963, -61.62625993902970123 ) ) ;
#6701=ORIENTED_EDGE ( 'NONE', *, *, #1133, .F. ) ;
#6722=B_SPLINE_CURVE_WITH_KNOTS ( 'NONE', 3,
 ( #37566, #37055, #1151, #49387, #18170, #17148, #44923, #9024, #37314, #33884, #49895, #24968, #13483, #5100, #25499, #41502, #5616, #10057, #1675, #26017 ),
 .UNSPECIFIED., .F., .F.,
 ( 4, 2, 2, 2, 2, 2, 2, 2, 2, 4 ),
 ( 0.000000000000000000, 0.08842663233073849716, 0.2261948956704462055, 0.3749999999999999445, 0.4999999999999988898, 0.5624999999999988898, 0.6624999999999995337, 0.7983826544642954604, 0.9363829142756890933, 1.000000000000000000 ),
 .UNSPECIFIED. ) ;
#6725=CARTESIAN_POINT ( 'NONE',  ( 64.48795401538340855, 1.045503847279079856, -70.40650121518619642 ) ) ;
#6739=CARTESIAN_POINT ( 'NONE',  ( 65.27736602627911111, 1.383811055320669947, -70.34999999999999432 ) ) ;
#6748=CARTESIAN_POINT ( 'NONE',  ( 71.25801539443460797, 1.385702546077159925, -70.29781821095090777 ) ) ;
#6757=CARTESIAN_POINT ( 'NONE',  ( 71.62484648860579739, 0.9098571636355720083, -70.52991329011129551 ) ) ;
#6771=CARTESIAN_POINT ( 'NONE',  ( 71.62064552848029564, 0.9479899806831150189, -60.76708149872590070 ) ) ;
#6798=CARTESIAN_POINT ( 'NONE',  ( 64.84324960441189489, 0.8888742037077609348, -60.63285689971630177 ) ) ;
#6828=CARTESIAN_POINT ( 'NONE',  ( 72.94510729672219895, 1.263823323415690147, -62.32316323322979912 ) ) ;
#6838=CARTESIAN_POINT ( 'NONE',  ( 64.89503925317049493, 1.371509258145880095, -70.32114135108699315 ) ) ;
#6862=EDGE_CURVE ( 'NONE', #8182, #9073, #2017, .T. ) ;
#6893=CARTESIAN_POINT ( 'NONE',  ( 71.34390086684349797, 1.188582381068100213, -60.69479001402090290 ) ) ;
#6895=CARTESIAN_POINT ( 'NONE',  ( 72.88602187343720118, 1.308647200627810259, -62.31695083504749988 ) ) ;
#6908=ORIENTED_EDGE ( 'NONE', *, *, #47966, .T. ) ;
#6950=ADVANCED_FACE ( 'NONE', ( #50696 ), #39166, .F. ) ;
#6952=CARTESIAN_POINT ( 'NONE',  ( 63.84815580435130045, 1.437400661353670062, -61.78179097966380340 ) ) ;
#6956=CARTESIAN_POINT ( 'NONE',  ( 73.13235683752471061, 1.096291039689160085, -68.89363957891330870 ) ) ;
#6959=ORIENTED_EDGE ( 'NONE', *, *, #2063, .T. ) ;
#6982=CARTESIAN_POINT ( 'NONE',  ( 64.91115770917960504, 1.389801772588459938, -70.26683326709820676 ) ) ;
#6991=CARTESIAN_POINT ( 'NONE',  ( 71.90108049458170569, 1.446932438105679841, -69.97684691838689730 ) ) ;
#7007=ORIENTED_EDGE ( 'NONE', *, *, #22674, .T. ) ;
#7008=CARTESIAN_POINT ( 'NONE',  ( 71.44150897753121399, 1.096153228089730147, -70.60852099187108877 ) ) ;
#7032=DIRECTION ( 'NONE',  ( 0.000000000000000000, -1.000000000000000000, 0.000000000000000000 ) ) ;
#7037=FACE_OUTER_BOUND ( 'NONE', #31298, .T. ) ;
#7055=CARTESIAN_POINT ( 'NONE',  ( 65.03937945068028625, 1.384708701328909886, -60.99162623037230446 ) ) ;
#7085=CARTESIAN_POINT ( 'NONE',  ( 72.74645547301390991, 1.390806392144110060, -68.86952544730040415 ) ) ;
#7087=CARTESIAN_POINT ( 'NONE',  ( 72.88423911510749065, 1.325841671674429900, -62.37472934403619718 ) ) ;
#7136=CARTESIAN_POINT ( 'NONE',  ( 63.23627918741579634, 0.9395704634982890990, -62.18392983749130565 ) ) ;
#7149=CARTESIAN_POINT ( 'NONE',  ( 71.39250861737149023, 1.096110717717199812, -60.66079369553730061 ) ) ;
#7151=CARTESIAN_POINT ( 'NONE',  ( 72.38882998111121481, 1.407740700961940039, -61.66563034611200322 ) ) ;
#7153=AXIS2_PLACEMENT_3D ( 'NONE', #1750, #17736, #11175 ) ;
#7181=B_SPLINE_SURFACE_WITH_KNOTS ( 'NONE', 3, 3, ( 
 ( #13466, #29927, #22067, #6111, #25479, #41226, #10299, #2173, #33865 ),
 ( #29421, #2422, #38076, #14480, #6365, #25221, #49876, #29673, #49625 ),
 ( #30451, #41483, #5340, #45944, #21293, #1395, #18152, #18406, #10034 ),
 ( #26000, #34382, #45426, #34118, #9530, #5597, #46214, #50129, #21552 ),
 ( #37297, #38333, #22327, #13971, #41742, #17384, #14225, #33349, #49366 ),
 ( #30197, #37548, #1653, #1913, #17645, #50394, #33611, #13719, #45682 ),
 ( #9784, #25735, #37820, #5848, #21813, #25575, #33447, #33703, #49467 ),
 ( #5692, #4640, #49209, #13558, #41581, #29520, #36605, #45524, #710 ),
 ( #17735, #21392, #29765, #21643, #24534, #33189, #45004, #13053, #37143 ),
 ( #4908, #20616, #45264, #45784, #16701, #5438, #49720, #9376, #9106 ),
 ( #13808, #8847, #9620, #44743, #24798, #37650, #1498, #20882, #29007 ),
 ( #41323, #25055, #40808, #40552, #1749, #32655, #48685, #12786, #36877 ),
 ( #28744, #32923, #976, #16977, #48952, #41072, #5184, #21137, #1240 ),
 ( #17228, #25320, #13301, #37396, #29262, #17483, #42102, #41843, #46307 ),
 ( #14837, #2268, #5946, #33954, #50738, #30799, #31059, #46567, #50997 ),
 ( #46049, #18761, #9873, #10136, #14577, #6466, #6207, #30543, #34481 ),
 ( #2008, #34734, #18507, #25828, #21904, #38173, #6725, #15098, #10916 ),
 ( #34211, #10655, #14319, #26613, #30291, #22423, #22161, #37915, #10396 ),
 ( #46828, #18242, #17990, #49972, #26878, #42889, #14064, #42627, #30024 ),
 ( #26097, #6982, #50232, #26351, #22681, #38427, #42363, #38700, #50487 ) ),
 .UNSPECIFIED., .F., .F., .F.,
 ( 4, 2, 2, 2, 2, 2, 2, 2, 2, 4 ),
 ( 4, 1, 1, 1, 1, 1, 4 ),
 ( -1.826162956740689847, -1.664693056096139934, -1.413098168491170092, -1.141351847962929877, -0.9130814783703469217, -0.7989462935740540006, -0.6163299978999839945, -0.3676482854780290244, -0.1181677997689200010, 0.000000000000000000 ),
 ( 0.000000000000000000, 0.1666666666666670182, 0.3333333333333329818, 0.5000000000000000000, 0.6666666666666670737, 0.8333333333333330373, 1.000000000000000000 ),
 .UNSPECIFIED. ) ;
#7191=CARTESIAN_POINT ( 'NONE',  ( 63.01386660552499563, 0.9960089569207349891, -62.53811752243721145 ) ) ;
#7195=CARTESIAN_POINT ( 'NONE',  ( 63.43778145654710698, 0.9561296872662310431, -61.91446069548659636 ) ) ;
#7202=CARTESIAN_POINT ( 'NONE',  ( 63.27515794601240628, 0.9525601718079100833, -62.12948614655890367 ) ) ;
#7205=CYLINDRICAL_SURFACE ( 'NONE', #39296, 0.4999999999999994449 ) ;
#7206=CARTESIAN_POINT ( 'NONE',  ( 73.04943094402750603, 1.269319268680890067, -68.77895457036579785 ) ) ;
#7219=EDGE_CURVE ( 'NONE', #43577, #11677, #35089, .T. ) ;
#7227=( GEOMETRIC_REPRESENTATION_CONTEXT ( 3 ) GLOBAL_UNCERTAINTY_ASSIGNED_CONTEXT ( ( #4394 ) ) GLOBAL_UNIT_ASSIGNED_CONTEXT ( ( #23715, #32088, #47856 ) ) REPRESENTATION_CONTEXT ( 'NONE', 'WORKASPACE' ) );
#7246=CARTESIAN_POINT ( 'NONE',  ( 72.05097492716728880, 1.266076987106930174, -70.10514767873740993 ) ) ;
#7260=CARTESIAN_POINT ( 'NONE',  ( 71.37118938927949330, 1.325715844996850024, -70.41854262496009653 ) ) ;
#7278=ORIENTED_EDGE ( 'NONE', *, *, #33166, .F. ) ;
#7290=CARTESIAN_POINT ( 'NONE',  ( 63.93393739769614825, 11.38381105532090309, -62.44999999999986784 ) ) ;
#7306=CARTESIAN_POINT ( 'NONE',  ( 64.79014552703418417, 0.9971903505820729485, -60.67679930835159752 ) ) ;
#7315=EDGE_CURVE ( 'NONE', #10362, #29849, #21684, .T. ) ;
#7319=CARTESIAN_POINT ( 'NONE',  ( 68.13393739769620083, 0.8838110553206759423, -65.65000000000000568 ) ) ;
#7338=CARTESIAN_POINT ( 'NONE',  ( 72.91105647262868672, 1.325839985408290067, -62.43087585298830078 ) ) ;
#7402=CARTESIAN_POINT ( 'NONE',  ( 71.28940315555229290, 0.9947083095259759977, -60.55634004142090276 ) ) ;
#7404=CARTESIAN_POINT ( 'NONE',  ( 72.32632772932539922, 1.200157260841289819, -61.39419087681179832 ) ) ;
#7432=AXIS2_PLACEMENT_3D ( 'NONE', #32758, #36707, #12890 ) ;
#7448=CARTESIAN_POINT ( 'NONE',  ( 63.00666467042349694, 0.9212109678634080590, -62.53374032209040223 ) ) ;
#7452=CARTESIAN_POINT ( 'NONE',  ( 63.30304092011339634, 0.9208623934744530892, -62.09132346512820533 ) ) ;
#7464=CARTESIAN_POINT ( 'NONE',  ( 73.14800808192789816, 0.9948723650351710690, -68.93161800279381168 ) ) ;
#7472=EDGE_LOOP ( 'NONE', ( #13797, #2302, #36712, #33579 ) ) ;
#7479=VERTEX_POINT ( 'NONE', #20646 ) ;
#7485=CARTESIAN_POINT ( 'NONE',  ( 72.80030139158668590, 1.384887413063060180, -62.68544474927200127 ) ) ;
#7502=CARTESIAN_POINT ( 'NONE',  ( 71.78321337075939823, 1.149538111076449987, -70.36367628376740413 ) ) ;
#7520=CARTESIAN_POINT ( 'NONE',  ( 71.56253747416570832, 1.100585178972000033, -70.52983742103249654 ) ) ;
#7532=ORIENTED_EDGE ( 'NONE', *, *, #24931, .F. ) ;
#7536=CIRCLE ( 'NONE', #40180, 0.5000000000000004441 ) ;
#7550=CARTESIAN_POINT ( 'NONE',  ( 63.13746035244330557, 0.8910129994591539093, -68.97194292341539779 ) ) ;
#7565=CARTESIAN_POINT ( 'NONE',  ( 65.11747358718548639, 1.386342629514219826, -61.00047607903670155 ) ) ;
#7578=CARTESIAN_POINT ( 'NONE',  ( 73.01385068780759013, 0.9098571636355720083, -69.14090909090960224 ) ) ;
#7601=CARTESIAN_POINT ( 'NONE',  ( 72.79231116732400153, 1.384708701328909886, -62.55544205298410532 ) ) ;
#7642=CARTESIAN_POINT ( 'NONE',  ( 63.11986671346460298, 0.9948723650351710690, -68.93161800279381168 ) ) ;
#7665=CARTESIAN_POINT ( 'NONE',  ( 71.29497000743199919, 0.8840451408750739093, -60.55014093144429665 ) ) ;
#7667=CARTESIAN_POINT ( 'NONE',  ( 72.27703085588929355, 1.458412159422780130, -61.64333151374460584 ) ) ;
#7708=APPLICATION_CONTEXT ( 'automotive_design' ) ;
#7714=CARTESIAN_POINT ( 'NONE',  ( 63.45006824032990522, 1.383161449028140089, -62.62844710992279573 ) ) ;
#7718=CARTESIAN_POINT ( 'NONE',  ( 63.38217364139809007, 0.9405967369938049716, -61.98545004926840107 ) ) ;
#7728=CARTESIAN_POINT ( 'NONE',  ( 71.33393739769650210, 1.396834109478129804, -70.23662692463440749 ) ) ;
#7731=CARTESIAN_POINT ( 'NONE',  ( 72.81285642849219641, 1.383357884654609959, -68.68594134708139620 ) ) ;
#7741=ORIENTED_EDGE ( 'NONE', *, *, #47852, .T. ) ;
#7755=CIRCLE ( 'NONE', #20292, 0.4999999999999982236 ) ;
#7764=CARTESIAN_POINT ( 'NONE',  ( 71.92220195954379847, 1.332297898505690137, -70.13430431592830416 ) ) ;
#7813=CARTESIAN_POINT ( 'NONE',  ( 71.33393739769628894, 10.88381105532070059, -61.94999999999999574 ) ) ;
#7829=DIRECTION ( 'NONE',  ( 0.5818181818182710519, 0.000000000000000000, -0.8133188816852104930 ) ) ;
#7853=CARTESIAN_POINT ( 'NONE',  ( 72.92486918121919359, 1.326324093417220240, -62.46048956832549948 ) ) ;
#7858=CARTESIAN_POINT ( 'NONE',  ( 64.65764093855688088, 1.007912009470870229, -70.53231455471869538 ) ) ;
#7885=ADVANCED_FACE ( 'NONE', ( #16344 ), #14516, .T. ) ;
#7893=CARTESIAN_POINT ( 'NONE',  ( 63.41515590138089919, 1.383136297697689976, -68.56705292396610218 ) ) ;
#7907=ORIENTED_EDGE ( 'NONE', *, *, #17615, .T. ) ;
#7914=CARTESIAN_POINT ( 'NONE',  ( 71.19138260135351004, 1.383767307422969939, -60.97855929785719553 ) ) ;
#7916=CARTESIAN_POINT ( 'NONE',  ( 72.19159089122339878, 1.443555314919450216, -61.52390474483700444 ) ) ;
#7945=CARTESIAN_POINT ( 'NONE',  ( 63.80708344237820739, 1.446931645112450093, -69.41713212316639670 ) ) ;
#7959=CARTESIAN_POINT ( 'NONE',  ( 63.19978792402569923, 1.187415670095769871, -62.40340069948359769 ) ) ;
#7963=CARTESIAN_POINT ( 'NONE',  ( 63.94990637464879768, 1.033013263524900083, -61.34874638836249972 ) ) ;
#7972=CARTESIAN_POINT ( 'NONE',  ( 63.29963954055089914, 0.9577391936096369962, -62.09594281269529858 ) ) ;
#8004=VERTEX_POINT ( 'NONE', #36252 ) ;
#8008=UNCERTAINTY_MEASURE_WITH_UNIT (LENGTH_MEASURE( 1.000000000000000082E-05 ), #10591, 'distance_accuracy_value', 'NONE');
#8009=CARTESIAN_POINT ( 'NONE',  ( 72.65443274204099566, 1.179532368575559875, -69.54928105623400825 ) ) ;
#8025=ORIENTED_EDGE ( 'NONE', *, *, #30989, .T. ) ;
#8058=EDGE_LOOP ( 'NONE', ( #2509, #6908, #36852, #35547 ) ) ;
#8059=DIRECTION ( 'NONE',  ( 0.000000000000000000, 0.000000000000000000, -1.000000000000000000 ) ) ;
#8061=CARTESIAN_POINT ( 'NONE',  ( 64.68608103367601814, 0.9036513197889380899, -70.56049771322830111 ) ) ;
#8085=DIRECTION ( 'NONE',  ( -0.8133188816852104930, 0.000000000000000000, -0.5818181818182710519 ) ) ;
#8141=B_SPLINE_CURVE_WITH_KNOTS ( 'NONE', 3,
 ( #48577, #20507, #36757, #33077, #32810, #44122, #28895, #25216, #44897, #28632, #9004, #1391, #28373, #1129, #12408, #44380, #44633, #24947, #40958, #48836 ),
 .UNSPECIFIED., .F., .F.,
 ( 4, 2, 2, 2, 2, 2, 2, 2, 2, 4 ),
 ( 0.000000000000000000, 0.08842663233499932496, 0.2261948956690018608, 0.3750000000000019984, 0.5000000000000005551, 0.5625000000000008882, 0.6625000000000003109, 0.7983826544665608704, 0.9363829142900766955, 1.000000000000000000 ),
 .UNSPECIFIED. ) ;
#8146=CARTESIAN_POINT ( 'NONE',  ( 71.33393739769628894, 10.88381105532070059, -69.84999999999999432 ) ) ;
#8149=CARTESIAN_POINT ( 'NONE',  ( 63.06393505168800573, 0.8850831926798630178, -68.85873448833339694 ) ) ;
#8163=CARTESIAN_POINT ( 'NONE',  ( 71.04878173523039209, 1.375383258925270136, -70.44587820682191648 ) ) ;
#8171=CARTESIAN_POINT ( 'NONE',  ( 71.44620697304119972, 0.9254905997697669973, -60.64710470602509673 ) ) ;
#8173=CARTESIAN_POINT ( 'NONE',  ( 72.09652352821250076, 1.406831506490820116, -61.37777621199789735 ) ) ;
#8176=CARTESIAN_POINT ( 'NONE',  ( 65.17314292416639887, 1.382830464309369844, -70.35440931850220636 ) ) ;
#8182=VERTEX_POINT ( 'NONE', #13469 ) ;
#8183=ADVANCED_FACE ( 'NONE', ( #29424 ), #16733, .T. ) ;
#8217=CARTESIAN_POINT ( 'NONE',  ( 63.45501836690030473, 1.383357884654609959, -62.61405865291869333 ) ) ;
#8243=VERTEX_POINT ( 'NONE', #50589 ) ;
#8248=CARTESIAN_POINT ( 'NONE',  ( 72.73458218292580568, 1.393731187554809958, -62.48946499964799983 ) ) ;
#8263=CARTESIAN_POINT ( 'NONE',  ( 72.19051388041059170, 1.409766894666529824, -69.84163571632670653 ) ) ;
#8282=CARTESIAN_POINT ( 'NONE',  ( 71.50269221454749413, 1.097545367735389910, -70.56928864606310015 ) ) ;
#8299=VERTEX_POINT ( 'NONE', #34846 ) ;
#8347=AXIS2_PLACEMENT_3D ( 'NONE', #30231, #18700, #46247 ) ;
#8375=CARTESIAN_POINT ( 'NONE',  ( 71.63754647491310834, 1.424120032877639996, -70.11997829442159968 ) ) ;
#8378=ORIENTED_EDGE ( 'NONE', *, *, #32687, .T. ) ;
#8392=CIRCLE ( 'NONE', #14231, 0.4999999999999865663 ) ;
#8402=ADVANCED_FACE ( 'NONE', ( #19543 ), #48981, .T. ) ;
#8404=DIRECTION ( 'NONE',  ( -0.7071067811865475727, 0.000000000000000000, -0.7071067811865475727 ) ) ;
#8407=CARTESIAN_POINT ( 'NONE',  ( 63.06902243323368396, 0.9940695285616559795, -68.85188839627709001 ) ) ;
#8420=CARTESIAN_POINT ( 'NONE',  ( 71.21626143364200345, 1.196343736543249880, -70.67573229508370503 ) ) ;
#8431=CARTESIAN_POINT ( 'NONE',  ( 71.28621524259639841, 1.327322800621349996, -60.84198109300940160 ) ) ;
#8433=CARTESIAN_POINT ( 'NONE',  ( 71.67377888102110717, 1.031491003830389941, -60.81565309434889599 ) ) ;
#8437=CARTESIAN_POINT ( 'NONE',  ( 64.97290478796050195, 0.8840451408750739093, -70.74985906855570761 ) ) ;
#8439=ORIENTED_EDGE ( 'NONE', *, *, #38931, .F. ) ;
#8440=CARTESIAN_POINT ( 'NONE',  ( 71.83406239765299972, 11.38381103969570063, -62.44999999999849649 ) ) ;
#8471=ADVANCED_FACE ( 'NONE', ( #18457 ), #42576, .F. ) ;
#8477=CARTESIAN_POINT ( 'NONE',  ( 63.06339012708429692, 0.9214125008369580261, -62.44212918470660156 ) ) ;
#8496=EDGE_LOOP ( 'NONE', ( #11929, #32550, #1454, #18876, #31481, #12426 ) ) ;
#8517=DIRECTION ( 'NONE',  ( 0.000000000000000000, 0.000000000000000000, -1.000000000000000000 ) ) ;
#8532=CARTESIAN_POINT ( 'NONE',  ( 72.25629666767210324, 1.056850087111250058, -70.01040857010899288 ) ) ;
#8534=B_SPLINE_CURVE_WITH_KNOTS ( 'NONE', 3,
 ( #33809, #13912, #45889, #50071, #14166, #25938, #10243, #22010, #36816, #37865, #17685, #34428, #10608, #1962, #21722, #29841 ),
 .UNSPECIFIED., .F., .F.,
 ( 4, 2, 2, 2, 2, 2, 2, 4 ),
 ( -8.599659000000000768E-15, 0.07216186899280199740, 0.1546325764131579739, 0.2061767685508799908, 0.2319488646197410409, 0.2731842183299189597, 0.3391607842662029970, 0.4123535371017689743 ),
 .UNSPECIFIED. ) ;
#8561=ORIENTED_EDGE ( 'NONE', *, *, #6654, .F. ) ;
#8609=CARTESIAN_POINT ( 'NONE',  ( 64.97340239734420209, 1.393731187554809958, -61.04935521477050031 ) ) ;
#8659=CARTESIAN_POINT ( 'NONE',  ( 63.34531745652139989, 1.374300485541529948, -68.58542282960749503 ) ) ;
#8661=CARTESIAN_POINT ( 'NONE',  ( 72.60719124696490212, 0.9098571636355720083, -68.84999999999999432 ) ) ;
#8672=CARTESIAN_POINT ( 'NONE',  ( 71.29455428839979447, 0.9209334348186318797, -70.75011546227260339 ) ) ;
#8680=CARTESIAN_POINT ( 'NONE',  ( 73.01149271009099095, 1.265664290790580182, -68.85308916926389600 ) ) ;
#8683=CARTESIAN_POINT ( 'NONE',  ( 73.10258273731270151, 1.278021359705829862, -62.63015105704819518 ) ) ;
#8686=CARTESIAN_POINT ( 'NONE',  ( 71.54045699608269615, 0.8986939045430379913, -60.71074964625670134 ) ) ;
#8689=CARTESIAN_POINT ( 'NONE',  ( 71.95061440476429482, 1.334524132314490075, -61.18591595078659395 ) ) ;
#8692=CARTESIAN_POINT ( 'NONE',  ( 65.07262241358380095, 1.198183261254780030, -70.68687062374729635 ) ) ;
#8699=DIRECTION ( 'NONE',  ( 0.000000000000000000, -1.000000000000000000, 0.000000000000000000 ) ) ;
#8712=ORIENTED_EDGE ( 'NONE', *, *, #26234, .T. ) ;
#8720=CARTESIAN_POINT ( 'NONE',  ( 64.93393739769619799, 1.396834109478129804, -70.23662692463440749 ) ) ;
#8729=ORIENTED_EDGE ( 'NONE', *, *, #15618, .T. ) ;
#8733=CARTESIAN_POINT ( 'NONE',  ( 63.41515590138089919, 1.383136297697689976, -62.73294707603399445 ) ) ;
#8742=EDGE_CURVE ( 'NONE', #37946, #41163, #48901, .T. ) ;
#8743=CARTESIAN_POINT ( 'NONE',  ( 64.93408011569830762, 1.389468113695450091, -61.03004030278179926 ) ) ;
#8758=ORIENTED_EDGE ( 'NONE', *, *, #42309, .F. ) ;
#8786=AXIS2_PLACEMENT_3D ( 'NONE', #46976, #51148, #15246 ) ;
#8789=CARTESIAN_POINT ( 'NONE',  ( 72.52593196779452001, 1.270920007605160107, -69.64171779669759133 ) ) ;
#8802=ADVANCED_FACE ( 'NONE', ( #28884 ), #49862, .T. ) ;
#8803=CARTESIAN_POINT ( 'NONE',  ( 64.18351159802539030, 1.441354674475120001, -61.42706364365079708 ) ) ;
#8847=CARTESIAN_POINT ( 'NONE',  ( 64.11159536369549983, 1.443019942996689897, -69.80885301619480288 ) ) ;
#8879=CARTESIAN_POINT ( 'NONE',  ( 63.93393739769619089, 10.88381105532070059, -68.84999999999999432 ) ) ;
#8912=AXIS2_PLACEMENT_3D ( 'NONE', #20073, #36066, #14868 ) ;
#8926=CARTESIAN_POINT ( 'NONE',  ( 63.78749078828948882, 1.530257664727401767, -62.44999999999999574 ) ) ;
#8929=CARTESIAN_POINT ( 'NONE',  ( 63.15271035305199376, 0.9966178393190270324, -68.98171082814549493 ) ) ;
#8943=CARTESIAN_POINT ( 'NONE',  ( 71.25020460053529803, 1.328674444234379859, -70.47425850519080370 ) ) ;
#8948=CARTESIAN_POINT ( 'NONE',  ( 72.96606887121211571, 1.263738073398970041, -68.93858679394679712 ) ) ;
#8953=CARTESIAN_POINT ( 'NONE',  ( 71.29339335573889969, 1.327097482837290121, -60.84525133028229504 ) ) ;
#8955=CARTESIAN_POINT ( 'NONE',  ( 71.75685251123249486, 1.434949534324269971, -61.23975123050709612 ) ) ;
#8957=CARTESIAN_POINT ( 'NONE',  ( 64.86758340617990370, 0.9945465939392450494, -70.67393287070269992 ) ) ;
#8998=CARTESIAN_POINT ( 'NONE',  ( 63.43898171031399613, 1.369976237678180109, -62.46883854029779570 ) ) ;
#9003=ADVANCED_FACE ( 'NONE', ( #6606 ), #26244, .T. ) ;
#9004=CARTESIAN_POINT ( 'NONE',  ( 72.13898961932780196, 1.457833794292699992, -61.50804513633939763 ) ) ;
#9008=ADVANCED_FACE ( 'NONE', ( #47227 ), #42310, .T. ) ;
#9024=CARTESIAN_POINT ( 'NONE',  ( 64.20123866503199395, 1.456055805561079941, -61.44407688768469455 ) ) ;
#9026=ORIENTED_EDGE ( 'NONE', *, *, #50867, .F. ) ;
#9034=CARTESIAN_POINT ( 'NONE',  ( 72.76396860142250489, 1.388715606738730068, -62.57493595107060713 ) ) ;
#9049=CARTESIAN_POINT ( 'NONE',  ( 72.99206043124139853, 1.132579237369250036, -69.08822821206570097 ) ) ;
#9051=CARTESIAN_POINT ( 'NONE',  ( 71.90718900442459471, 0.9644290104346029402, -70.31590730770628284 ) ) ;
#9062=CARTESIAN_POINT ( 'NONE',  ( 64.31051442921079797, 1.400155911913310014, -61.27037346668680584 ) ) ;
#9073=VERTEX_POINT ( 'NONE', #6739 ) ;
#9076=ORIENTED_EDGE ( 'NONE', *, *, #6630, .T. ) ;
#9106=CARTESIAN_POINT ( 'NONE',  ( 63.92076813643380007, 1.033004454759739899, -69.92211063522330505 ) ) ;
#9134=CARTESIAN_POINT ( 'NONE',  ( 72.78816252330430814, 1.385888765344509999, -68.65207957385619864 ) ) ;
#9145=AXIS2_PLACEMENT_3D ( 'NONE', #36890, #5196, #25332 ) ;
#9185=CARTESIAN_POINT ( 'NONE',  ( 72.86589732295999511, 1.383811055320669947, -68.52599601131950635 ) ) ;
#9200=CARTESIAN_POINT ( 'NONE',  ( 71.19525238180870019, 1.198183261254780030, -70.68687062374729635 ) ) ;
#9206=CARTESIAN_POINT ( 'NONE',  ( 72.99348972288790094, 1.187296498006439993, -69.02170307486190381 ) ) ;
#9209=CARTESIAN_POINT ( 'NONE',  ( 72.92255733887110125, 1.374300485541529948, -62.71457717039259450 ) ) ;
#9213=CARTESIAN_POINT ( 'NONE',  ( 71.81682835125050701, 1.153605328057990098, -60.96078815522670169 ) ) ;
#9216=CARTESIAN_POINT ( 'NONE',  ( 65.23737843152780158, 1.383411777981069957, -70.37541122638330648 ) ) ;
#9229=VERTEX_POINT ( 'NONE', #11761 ) ;
#9263=CARTESIAN_POINT ( 'NONE',  ( 63.35681832276381442, 1.325839985408290067, -62.43087585298830078 ) ) ;
#9264=DIRECTION ( 'NONE',  ( 1.000000000000000000, 0.000000000000000000, 0.000000000000000000 ) ) ;
#9287=VERTEX_POINT ( 'NONE', #35788 ) ;
#9305=CARTESIAN_POINT ( 'NONE',  ( 72.75396425272869294, 1.390208944942419755, -62.54542373973200142 ) ) ;
#9333=CARTESIAN_POINT ( 'NONE',  ( 64.03462240194079413, 1.348268854479560019, -61.41792271134369940 ) ) ;
#9376=CARTESIAN_POINT ( 'NONE',  ( 63.92116633856140595, 1.061268877959919976, -69.92250879741870051 ) ) ;
#9410=CIRCLE ( 'NONE', #26964, 5.999999999999998224 ) ;
#9418=CARTESIAN_POINT ( 'NONE',  ( 72.69742484592399023, 1.402336724396409995, -68.91862208776170462 ) ) ;
#9432=ORIENTED_EDGE ( 'NONE', *, *, #39582, .T. ) ;
#9440=CARTESIAN_POINT ( 'NONE',  ( 65.19259745005730622, 1.384447124000270035, -60.97624892474630087 ) ) ;
#9447=CARTESIAN_POINT ( 'NONE',  ( 64.81979753630260177, 0.8904513541338869853, -60.64834380034769623 ) ) ;
#9461=CARTESIAN_POINT ( 'NONE',  ( 71.39250861737149023, 1.096110717717199812, -70.63920630446268945 ) ) ;
#9464=VECTOR ( 'NONE', #45884, 1000.000000000000000 ) ;
#9468=CARTESIAN_POINT ( 'NONE',  ( 72.80537809983910336, 1.383767307422960169, -68.70744520365728647 ) ) ;
#9473=CARTESIAN_POINT ( 'NONE',  ( 71.50564047255809896, 1.187296498006439993, -60.79044767480839795 ) ) ;
#9476=CARTESIAN_POINT ( 'NONE',  ( 71.86457203492498991, 0.9897451961560271849, -60.94993607748450160 ) ) ;
#9479=CARTESIAN_POINT ( 'NONE',  ( 64.80090148641970416, 1.186614556332910020, -70.53308468150621025 ) ) ;
#9502=AXIS2_PLACEMENT_3D ( 'NONE', #48320, #28378, #44386 ) ;
#9514=CARTESIAN_POINT ( 'NONE',  ( 73.26121012496899709, 0.8838110553206759423, -62.53374032209040223 ) ) ;
#9521=CARTESIAN_POINT ( 'NONE',  ( 63.45453858566830974, 1.370853092582090094, -62.43091793016829882 ) ) ;
#9530=CARTESIAN_POINT ( 'NONE',  ( 63.45118475302019334, 1.239064938996009779, -69.25399354804109464 ) ) ;
#9568=CARTESIAN_POINT ( 'NONE',  ( 73.08672326322148649, 0.8966068345641480253, -62.26318953425310099 ) ) ;
#9570=CARTESIAN_POINT ( 'NONE',  ( 72.85189580008329813, 1.309820314133779862, -69.05029809067748658 ) ) ;
#9583=CARTESIAN_POINT ( 'NONE',  ( 64.03801787523769917, 1.197080272271600077, -61.30148670604589967 ) ) ;
#9618=CARTESIAN_POINT ( 'NONE',  ( 72.33393739769618946, 1.883811055320669947, -62.44999999999999574 ) ) ;
#9620=CARTESIAN_POINT ( 'NONE',  ( 64.07869229662848909, 1.409273244282670090, -69.84075035169790624 ) ) ;
#9646=CARTESIAN_POINT ( 'NONE',  ( 72.77398937677050128, 1.387412027389909985, -68.69511434646409498 ) ) ;
#9652=EDGE_CURVE ( 'NONE', #38817, #37903, #48102, .T. ) ;
#9668=EDGE_LOOP ( 'NONE', ( #46686, #7741, #26856, #32274 ) ) ;
#9669=DIRECTION ( 'NONE',  ( 0.000000000000000000, 1.000000000000000000, 0.000000000000000000 ) ) ;
#9686=MECHANICAL_DESIGN_GEOMETRIC_PRESENTATION_REPRESENTATION('',(#4659),#7227);
#9687=CARTESIAN_POINT ( 'NONE',  ( 65.00498282733049393, 1.269319268680890067, -60.73450645366879996 ) ) ;
#9710=CARTESIAN_POINT ( 'NONE',  ( 64.85866674173239232, 1.325841671674429900, -60.89969828258869455 ) ) ;
#9716=CARTESIAN_POINT ( 'NONE',  ( 73.11516444234040080, 0.9966178393190270324, -68.98171082814549493 ) ) ;
#9719=CARTESIAN_POINT ( 'NONE',  ( 73.13170780125059878, 0.9259537755896120048, -62.33000265676009377 ) ) ;
#9721=CARTESIAN_POINT ( 'NONE',  ( 71.60339545440879760, 0.9065823421260970072, -60.75474143511929981 ) ) ;
#9725=CARTESIAN_POINT ( 'NONE',  ( 64.99178804968069301, 1.386446979194299933, -70.29126806847389730 ) ) ;
#9738=DIRECTION ( 'NONE',  ( -1.000000000000000000, 0.000000000000000000, 0.000000000000000000 ) ) ;
#9753=ADVANCED_FACE ( 'NONE', ( #6152 ), #22108, .T. ) ;
#9766=DIRECTION ( 'NONE',  ( 0.000000000000000000, -1.000000000000000000, 0.000000000000000000 ) ) ;
#9774=CARTESIAN_POINT ( 'NONE',  ( 63.27605356278090198, 1.264489825601020190, -62.40944773533740175 ) ) ;
#9784=CARTESIAN_POINT ( 'NONE',  ( 63.80708344237820739, 1.446931645112450093, -69.41713212316639670 ) ) ;
#9818=EDGE_CURVE ( 'NONE', #11637, #10547, #49840, .T. ) ;
#9828=CARTESIAN_POINT ( 'NONE',  ( 72.68207769252681771, 1.402020837641670070, -69.05263811644309158 ) ) ;
#9831=CARTESIAN_POINT ( 'NONE',  ( 65.23632417210519918, 1.383928098097870096, -70.33743540642140601 ) ) ;
#9839=CARTESIAN_POINT ( 'NONE',  ( 64.41203867946529726, 1.158194067776729952, -60.98980919032499770 ) ) ;
#9840=ORIENTED_EDGE ( 'NONE', *, *, #50128, .F. ) ;
#9860=FACE_OUTER_BOUND ( 'NONE', #21060, .T. ) ;
#9873=CARTESIAN_POINT ( 'NONE',  ( 64.60878109323620322, 1.379695757017360025, -70.20843506130859168 ) ) ;
#9884=CARTESIAN_POINT ( 'NONE',  ( 63.49151163952229382, 1.387131204727280132, -68.68796153961081075 ) ) ;
#9921=CARTESIAN_POINT ( 'NONE',  ( 72.83393739769620367, 1.383811055320669947, -62.79342862858290886 ) ) ;
#9941=CARTESIAN_POINT ( 'NONE',  ( 65.11408845474450402, 1.278021359705819870, -60.68135466038360448 ) ) ;
#9944=DIRECTION ( 'NONE',  ( 1.000000000000000000, 0.000000000000000000, 0.000000000000000000 ) ) ;
#9952=ORIENTED_EDGE ( 'NONE', *, *, #13311, .F. ) ;
#9960=AXIS2_PLACEMENT_3D ( 'NONE', #21863, #38914, #18975 ) ;
#9965=CARTESIAN_POINT ( 'NONE',  ( 64.95360084570980064, 1.395196698723390138, -61.05633982442969909 ) ) ;
#9970=CARTESIAN_POINT ( 'NONE',  ( 72.96845534527879806, 1.188860127980290171, -69.06196878611640955 ) ) ;
#9972=CARTESIAN_POINT ( 'NONE',  ( 73.11081010690780602, 1.190292248953970011, -62.47835652209879953 ) ) ;
#9978=CARTESIAN_POINT ( 'NONE',  ( 65.05887334876689465, 1.388715606738730068, -70.28003120372629553 ) ) ;
#9986=DIRECTION ( 'NONE',  ( 0.000000000000000000, 0.000000000000000000, 1.000000000000000000 ) ) ;
#10006=MANIFOLD_SOLID_BREP ( 'Stock-MAS-691-1', #1694 ) ;
#10024=CARTESIAN_POINT ( 'NONE',  ( 63.16073670604789925, 0.9971903505820729485, -62.30620812933800323 ) ) ;
#10025=DIRECTION ( 'NONE',  ( 1.000000000000000000, 0.000000000000000000, 0.000000000000000000 ) ) ;
#10034=CARTESIAN_POINT ( 'NONE',  ( 63.32231416895070453, 0.9254875393589979682, -69.23491771966379815 ) ) ;
#10049=CIRCLE ( 'NONE', #29995, 5.500000000000005329 ) ;
#10057=CARTESIAN_POINT ( 'NONE',  ( 63.57044994947320760, 1.402336724397559964, -62.38137791222469986 ) ) ;
#10075=AXIS2_PLACEMENT_3D ( 'NONE', #5915, #16939, #32883 ) ;
#10084=CARTESIAN_POINT ( 'NONE',  ( 72.94808712738880274, 1.229084191802120030, -69.04069905742069579 ) ) ;
#10100=CARTESIAN_POINT ( 'NONE',  ( 63.71470905091258885, 1.396295651964360118, -61.88579195298250113 ) ) ;
#10125=CYLINDRICAL_SURFACE ( 'NONE', #6001, 1.000000000000000888 ) ;
#10136=CARTESIAN_POINT ( 'NONE',  ( 64.54859588824778882, 1.318423743231420087, -70.26560465517479770 ) ) ;
#10148=AXIS2_PLACEMENT_3D ( 'NONE', #45047, #32186, #28789 ) ;
#10149=CARTESIAN_POINT ( 'NONE',  ( 63.40532295848070987, 1.369664981662509939, -68.74641178933899255 ) ) ;
#10169=ORIENTED_EDGE ( 'NONE', *, *, #42114, .T. ) ;
#10206=CARTESIAN_POINT ( 'NONE',  ( 65.07863563811220331, 1.331842543267529821, -60.79893402932049895 ) ) ;
#10233=CARTESIAN_POINT ( 'NONE',  ( 64.76518258084500701, 1.097545367735389910, -60.73071135393688991 ) ) ;
#10239=CARTESIAN_POINT ( 'NONE',  ( 73.10458614724748827, 1.096044978595170027, -62.36169201816110075 ) ) ;
#10243=CARTESIAN_POINT ( 'NONE',  ( 71.42462519098059204, 0.8888742037077599356, -60.63285689971630177 ) ) ;
#10246=CARTESIAN_POINT ( 'NONE',  ( 64.98165955279610273, 1.327322800621349996, -70.45801890699070213 ) ) ;
#10257=B_SPLINE_SURFACE_WITH_KNOTS ( 'NONE', 3, 3, ( 
 ( #49784, #21974, #41916, #26167, #9941, #37986, #2081, #34028, #45591, #25647 ),
 ( #21203, #41137, #49277, #1820, #33522, #50038, #5755, #22234, #18310, #45335 ),
 ( #30095, #13876, #37209, #21464, #1310, #13369, #29335, #38242, #21712, #46122 ),
 ( #9440, #50305, #17801, #10206, #42177, #25389, #29836, #41391, #14390, #37463 ),
 ( #1561, #17549, #49534, #29586, #9687, #11504, #31127, #27204, #47153, #39273 ),
 ( #22749, #35598, #39534, #27461, #23515, #34551, #3378, #43464, #51069, #19350 ),
 ( #7565, #35332, #19607, #3635, #18575, #15170, #30615, #15683, #10724, #6798 ),
 ( #14904, #38769, #14647, #15431, #31382, #51584, #51331, #31637, #10468, #30869 ),
 ( #18827, #26424, #47409, #42441, #35065, #26678, #6530, #46639, #22492, #38500 ),
 ( #50813, #2602, #46896, #50555, #42700, #2862, #34810, #10987, #11242, #26951 ),
 ( #42956, #7055, #23005, #39026, #3121, #43215, #19088, #7306, #23258, #41940 ),
 ( #357, #41672, #42202, #12412, #1845, #30123, #5778, #4805, #21740, #46142 ),
 ( #33797, #4537, #37748, #606, #20772, #36761, #10233, #872, #17823, #40446 ),
 ( #20510, #6041, #16592, #9710, #34049, #14155, #18081, #16866, #50059, #49806 ),
 ( #9965, #8743, #36503, #25925, #26192, #48317, #28899, #38007, #24691, #13899 ),
 ( #12943, #29857, #40707, #32544, #36248, #20256, #16339, #32295, #32813, #28376 ) ),
 .UNSPECIFIED., .F., .F., .F.,
 ( 4, 2, 2, 2, 2, 2, 2, 4 ),
 ( 4, 1, 1, 1, 1, 1, 1, 4 ),
 ( -4.528785000000000087E-15, 0.07216186899280399580, 0.1546325764131560032, 0.2061767685508759940, 0.2319488646197360171, 0.2731842183299119653, 0.3391607842661930050, 0.4123535371017559847 ),
 ( 0.000000000000000000, 0.1428571428571430157, 0.2857142857142860315, 0.4285714285714289917, 0.5714285714285709528, 0.7142857142857139685, 0.8571428571428569843, 1.000000000000000000 ),
 .UNSPECIFIED. ) ;
#10288=DIRECTION ( 'NONE',  ( 0.000000000000000000, 0.000000000000000000, 1.000000000000000000 ) ) ;
#10299=CARTESIAN_POINT ( 'NONE',  ( 63.25226693078700180, 1.024253516290730026, -69.12311412914529285 ) ) ;
#10306=CARTESIAN_POINT ( 'NONE',  ( 72.89288316602700490, 1.231980527807239989, -62.16651341217360027 ) ) ;
#10311=ORIENTED_EDGE ( 'NONE', *, *, #35907, .T. ) ;
#10331=CARTESIAN_POINT ( 'NONE',  ( 71.83406239697100659, 11.38381102407110035, -68.85000000076199456 ) ) ;
#10336=CIRCLE ( 'NONE', #46374, 0.4999999999999983902 ) ;
#10352=CARTESIAN_POINT ( 'NONE',  ( 65.07026117056300052, 1.388189907116970101, -70.28386057589730740 ) ) ;
#10361=CARTESIAN_POINT ( 'NONE',  ( 63.82110572780499780, 1.345243094457279964, -61.64184835600830326 ) ) ;
#10362=VERTEX_POINT ( 'NONE', #42320 ) ;
#10389=FACE_OUTER_BOUND ( 'NONE', #50725, .T. ) ;
#10396=CARTESIAN_POINT ( 'NONE',  ( 64.57410506046470289, 0.9210617359723509701, -70.48005104816739674 ) ) ;
#10411=CARTESIAN_POINT ( 'NONE',  ( 63.29194469617720387, 1.263903724274369811, -68.92034810279041324 ) ) ;
#10413=DIRECTION ( 'NONE',  ( -1.000000000000000000, 0.000000000000000000, 0.000000000000000000 ) ) ;
#10418=CARTESIAN_POINT ( 'NONE',  ( 71.19761362482960010, 1.388189907116970101, -70.28386057589720792 ) ) ;
#10468=CARTESIAN_POINT ( 'NONE',  ( 64.82166782235130142, 0.9254905997697669973, -60.64710470602509673 ) ) ;
#10498=CARTESIAN_POINT ( 'NONE',  ( 73.01385068780759013, 0.9098571636355680115, -69.14090909090950277 ) ) ;
#10500=CARTESIAN_POINT ( 'NONE',  ( 73.13683269167120216, 0.9254905997697669973, -62.33773042465509917 ) ) ;
#10506=CARTESIAN_POINT ( 'NONE',  ( 64.75883903758510485, 0.9989215084294049696, -70.60223669534690316 ) ) ;
#10516=DIRECTION ( 'NONE',  ( 2.867428237999167073E-28, -3.637457002807960330E-11, -1.000000000000000000 ) ) ;
#10547=VERTEX_POINT ( 'NONE', #38236 ) ;
#10551=CARTESIAN_POINT ( 'NONE',  ( 63.25409997666370288, 1.100585178971990041, -62.22139992353060478 ) ) ;
#10563=CARTESIAN_POINT ( 'NONE',  ( 71.07527734533519492, 1.384447124000270035, -60.97624892474630087 ) ) ;
#10565=CARTESIAN_POINT ( 'NONE',  ( 72.83816022157699877, 1.310552739454540205, -62.22324284883860201 ) ) ;
#10591=( LENGTH_UNIT ( ) NAMED_UNIT ( * ) SI_UNIT ( .MILLI., .METRE. ) );
#10608=CARTESIAN_POINT ( 'NONE',  ( 71.54045699608269615, 0.8986939045430379913, -60.71074964625670134 ) ) ;
#10611=CIRCLE ( 'NONE', #48234, 6.000000000000005329 ) ;
#10613=CARTESIAN_POINT ( 'NONE',  ( 72.33393739769618946, 1.883811055320669947, -68.84999999999999432 ) ) ;
#10624=CARTESIAN_POINT ( 'NONE',  ( 63.75661388851530376, 1.112168069084249922, -61.55316875389540598 ) ) ;
#10655=CARTESIAN_POINT ( 'NONE',  ( 64.84151977724279448, 1.394090247237909974, -70.24155908324229358 ) ) ;
#10664=CARTESIAN_POINT ( 'NONE',  ( 71.86857605226019530, 1.394112346783849876, -70.08832560374550269 ) ) ;
#10678=CARTESIAN_POINT ( 'NONE',  ( 71.48855272380100701, 0.8936201581567889685, -70.62461353540280129 ) ) ;
#10697=CARTESIAN_POINT ( 'NONE',  ( 71.60705152684150221, 1.024253516290730026, -60.76832953309080665 ) ) ;
#10724=CARTESIAN_POINT ( 'NONE',  ( 64.84489409100200419, 0.9242073871622918935, -60.63177898966700496 ) ) ;
#10755=CARTESIAN_POINT ( 'NONE',  ( 73.17063711417530669, 1.097895768572089814, -62.46942512468480402 ) ) ;
#10820=CARTESIAN_POINT ( 'NONE',  ( 71.11795458202399800, 1.382840740411490188, -60.95335679887120506 ) ) ;
#10835=CARTESIAN_POINT ( 'NONE',  ( 63.50390619396989678, 1.388715606738730068, -68.72506404892941134 ) ) ;
#10850=CARTESIAN_POINT ( 'NONE',  ( 63.11679429741250402, 0.8888742037077599356, -62.35931220671560027 ) ) ;
#10876=AXIS2_PLACEMENT_3D ( 'NONE', #45227, #16658, #37610 ) ;
#10883=CARTESIAN_POINT ( 'NONE',  ( 63.75644714388239720, 1.054781932184780002, -61.54608750241579429 ) ) ;
#10887=CARTESIAN_POINT ( 'NONE',  ( 73.08275130671789555, 1.274277262446050107, -68.71132524057000523 ) ) ;
#10902=CIRCLE ( 'NONE', #37631, 0.5000000000000000000 ) ;
#10916=CARTESIAN_POINT ( 'NONE',  ( 64.46842165375500144, 0.9408120350972830614, -70.40100145642890084 ) ) ;
#10922=CARTESIAN_POINT ( 'NONE',  ( 71.63754647491310834, 1.424120032877639996, -70.11997829442159968 ) ) ;
#10927=CARTESIAN_POINT ( 'NONE',  ( 63.28685848367280897, 1.187931651339009909, -69.04190732916428885 ) ) ;
#10937=CARTESIAN_POINT ( 'NONE',  ( 71.41841232404479456, 1.186701509386330011, -70.56202332290359891 ) ) ;
#10962=DIRECTION ( 'NONE',  ( 1.000000000000000000, 0.000000000000000000, 0.000000000000000000 ) ) ;
#10987=CARTESIAN_POINT ( 'NONE',  ( 64.80222656955069738, 0.9966178393190270324, -60.66877295535580572 ) ) ;
#11011=CARTESIAN_POINT ( 'NONE',  ( 73.03159560797669769, 0.9395704634982890990, -69.11607016250870572 ) ) ;
#11013=CARTESIAN_POINT ( 'NONE',  ( 73.01377481872879116, 1.100585178972000033, -62.22139992353060478 ) ) ;
#11015=DIRECTION ( 'NONE',  ( 0.000000000000000000, 1.000000000000000000, 0.000000000000000000 ) ) ;
#11017=DIRECTION ( 'NONE',  ( 0.000000000000000000, -1.000000000000000000, 0.000000000000000000 ) ) ;
#11018=AXIS2_PLACEMENT_3D ( 'NONE', #44639, #41484, #41743 ) ;
#11022=CARTESIAN_POINT ( 'NONE',  ( 64.81907236522980043, 1.326666718054990035, -70.38086014838010840 ) ) ;
#11068=CARTESIAN_POINT ( 'NONE',  ( 63.40307724931621181, 1.326666718054969829, -62.33513496753349870 ) ) ;
#11081=CARTESIAN_POINT ( 'NONE',  ( 71.31451227301140250, 1.097895768572089814, -60.61330028352099930 ) ) ;
#11083=CARTESIAN_POINT ( 'NONE',  ( 72.39815743494149558, 1.277726347179370059, -61.51551921202479889 ) ) ;
#11096=CARTESIAN_POINT ( 'NONE',  ( 63.52011431889719972, 1.391252479931859964, -62.52735703481241103 ) ) ;
#11102=DIRECTION ( 'NONE',  ( 0.000000000000000000, 1.000000000000000000, 0.000000000000000000 ) ) ;
#11138=CARTESIAN_POINT ( 'NONE',  ( 63.64445560419389381, 1.419970371293449940, -62.18985507218640407 ) ) ;
#11142=CARTESIAN_POINT ( 'NONE',  ( 73.15615143370008866, 1.097085799869280009, -68.85468201266050414 ) ) ;
#11175=DIRECTION ( 'NONE',  ( -1.000000000000000000, 0.000000000000000000, 0.000000000000000000 ) ) ;
#11181=CARTESIAN_POINT ( 'NONE',  ( 71.65351305086610978, 1.028860820851649871, -70.49907908372900067 ) ) ;
#11187=CARTESIAN_POINT ( 'NONE',  ( 63.39331655121669939, 1.326134026835569912, -68.94513744192749982 ) ) ;
#11197=CARTESIAN_POINT ( 'NONE',  ( 71.25608535201600091, 1.369535599030039963, -70.36855090579189209 ) ) ;
#11211=FACE_OUTER_BOUND ( 'NONE', #3995, .T. ) ;
#11215=EDGE_LOOP ( 'NONE', ( #11578, #633, #46858, #35173 ) ) ;
#11219=AXIS2_PLACEMENT_3D ( 'NONE', #29965, #26554, #37856 ) ;
#11223=CARTESIAN_POINT ( 'NONE',  ( 72.60719124696490212, 0.9098571636355720083, -62.44999999999999574 ) ) ;
#11226=DIRECTION ( 'NONE',  ( 0.000000000000000000, 1.000000000000000000, 0.000000000000000000 ) ) ;
#11230=EDGE_CURVE ( 'NONE', #13020, #51085, #8534, .T. ) ;
#11237=CARTESIAN_POINT ( 'NONE',  ( 71.17189893730710537, 1.387131204727280132, -70.29242575817399086 ) ) ;
#11242=CARTESIAN_POINT ( 'NONE',  ( 64.79388653638659434, 0.9272522097098119254, -60.66559564092809609 ) ) ;
#11249=CARTESIAN_POINT ( 'NONE',  ( 72.50969334808389988, 1.026088617261680103, -69.75574693290749906 ) ) ;
#11253=DIRECTION ( 'NONE',  ( 0.000000000000000000, 1.000000000000000000, 0.000000000000000000 ) ) ;
#11273=CARTESIAN_POINT ( 'NONE',  ( 72.76128204928120624, 1.388313565858570131, -62.46994910431339321 ) ) ;
#11325=CARTESIAN_POINT ( 'NONE',  ( 63.25144821230251324, 0.9425424353906030062, -62.16269173205530763 ) ) ;
#11338=CARTESIAN_POINT ( 'NONE',  ( 71.21254218222989607, 1.330484379554840002, -60.80906431331560213 ) ) ;
#11340=CARTESIAN_POINT ( 'NONE',  ( 72.48245069165039922, 1.197080272271600077, -61.55408047754139744 ) ) ;
#11365=CARTESIAN_POINT ( 'NONE',  ( 63.23867883281550206, 0.9065823421260940096, -62.18054194328749418 ) ) ;
#11387=CARTESIAN_POINT ( 'NONE',  ( 63.09706677394889596, 1.198183261254780030, -62.58868501588759869 ) ) ;
#11399=CARTESIAN_POINT ( 'NONE',  ( 63.41597899531610238, 1.309820314134120034, -62.24970190930920211 ) ) ;
#11400=ORIENTED_EDGE ( 'NONE', *, *, #50754, .T. ) ;
#11403=CARTESIAN_POINT ( 'NONE',  ( 73.15108049798000422, 0.8888742037077609348, -68.94068779328439689 ) ) ;
#11422=VERTEX_POINT ( 'NONE', #33460 ) ;
#11436=EDGE_CURVE ( 'NONE', #9073, #8299, #2447, .T. ) ;
#11443=CARTESIAN_POINT ( 'NONE',  ( 71.66763488949699479, 0.9543424661145570864, -70.49936564611709855 ) ) ;
#11448=CARTESIAN_POINT ( 'NONE',  ( 63.33388541776019309, 1.264121749638649872, -68.99682374033621102 ) ) ;
#11486=EDGE_CURVE ( 'NONE', #16929, #31343, #5818, .T. ) ;
#11488=CARTESIAN_POINT ( 'NONE',  ( 63.93393739769609141, 10.88381105532070059, -62.44999999999999574 ) ) ;
#11504=CARTESIAN_POINT ( 'NONE',  ( 64.96229391979498757, 1.190292248953970011, -60.67312729078840050 ) ) ;
#11532=EDGE_CURVE ( 'NONE', #37903, #48585, #4124, .T. ) ;
#11535=CARTESIAN_POINT ( 'NONE',  ( 73.00002125581650603, 1.102139304147779830, -62.20100733290610151 ) ) ;
#11559=ORIENTED_EDGE ( 'NONE', *, *, #2519, .T. ) ;
#11560=EDGE_LOOP ( 'NONE', ( #37848, #20269, #7007, #39313 ) ) ;
#11574=CARTESIAN_POINT ( 'NONE',  ( 63.48441347673288959, 1.386342629514219826, -68.66646381051069170 ) ) ;
#11578=ORIENTED_EDGE ( 'NONE', *, *, #20615, .F. ) ;
#11597=CARTESIAN_POINT ( 'NONE',  ( 71.30558087559749936, 1.190292248953970011, -60.67312729078840050 ) ) ;
#11599=CARTESIAN_POINT ( 'NONE',  ( 72.43598295795109721, 1.061277144319840104, -61.46676083746540087 ) ) ;
#11601=FACE_OUTER_BOUND ( 'NONE', #1879, .T. ) ;
#11637=VERTEX_POINT ( 'NONE', #37874 ) ;
#11641=CARTESIAN_POINT ( 'NONE',  ( 63.08005232011719698, 0.8859637708054489691, -62.41593972647859800 ) ) ;
#11654=EDGE_LOOP ( 'NONE', ( #6195, #34187, #38976, #6959, #19717 ) ) ;
#11657=CARTESIAN_POINT ( 'NONE',  ( 72.89924231985609993, 1.371651820402770117, -68.64970267437179530 ) ) ;
#11677=VERTEX_POINT ( 'NONE', #39939 ) ;
#11682=CARTESIAN_POINT ( 'NONE',  ( 68.13393739769620083, -42.11618894467930119, -65.65000000000000568 ) ) ;
#11696=CARTESIAN_POINT ( 'NONE',  ( 71.83183169758690667, 0.9828917932938358026, -70.37585607920048858 ) ) ;
#11705=CARTESIAN_POINT ( 'NONE',  ( 64.02817266311009803, 1.026090475080779996, -70.02573918086800120 ) ) ;
#11712=CARTESIAN_POINT ( 'NONE',  ( 71.50060750274239751, 1.264689361399219836, -70.43884909106640180 ) ) ;
#11741=EDGE_CURVE ( 'NONE', #42080, #10547, #15047, .T. ) ;
#11743=DIRECTION ( 'NONE',  ( 0.000000000000000000, 0.000000000000000000, -1.000000000000000000 ) ) ;
#11748=CARTESIAN_POINT ( 'NONE',  ( 64.81199447428100768, 0.8910129994591419189, -70.64647704525310701 ) ) ;
#11761=CARTESIAN_POINT ( 'NONE',  ( 63.54731047306190561, 1.396834109478129804, -62.44999999999999574 ) ) ;
#11768=AXIS2_PLACEMENT_3D ( 'NONE', #34461, #38410, #26335 ) ;
#11777=VERTEX_POINT ( 'NONE', #2169 ) ;
#11794=CARTESIAN_POINT ( 'NONE',  ( 72.99182123261159916, 1.264489825601020190, -62.40944773533740175 ) ) ;
#11799=CARTESIAN_POINT ( 'NONE',  ( 65.01129443250870565, 1.391252479931859964, -70.26382307879910627 ) ) ;
#11811=FACE_OUTER_BOUND ( 'NONE', #18107, .T. ) ;
#11812=CARTESIAN_POINT ( 'NONE',  ( 70.99050876911339003, 0.8838110553206759423, -70.34999999999999432 ) ) ;
#11836=CARTESIAN_POINT ( 'NONE',  ( 63.44650199127489998, 1.383928098097870096, -68.54761322559109260 ) ) ;
#11860=CARTESIAN_POINT ( 'NONE',  ( 71.27608674571190761, 1.386446979194299933, -61.00873193152619933 ) ) ;
#11862=CARTESIAN_POINT ( 'NONE',  ( 72.61842109033369752, 1.039769764133420038, -61.66260107181680183 ) ) ;
#11883=CARTESIAN_POINT ( 'NONE',  ( 63.02029346573409185, 0.8838110553206740549, -62.51131646858519275 ) ) ;
#11886=CARTESIAN_POINT ( 'NONE',  ( 62.13393739769620083, 0.8838110553206759423, -65.65000000000000568 ) ) ;
#11893=CARTESIAN_POINT ( 'NONE',  ( 64.67348939754930370, 1.419996320997050088, -70.13930819973541020 ) ) ;
#11905=CARTESIAN_POINT ( 'NONE',  ( 63.13475262569159696, 0.9955677559369568996, -62.34557165980569948 ) ) ;
#11919=CARTESIAN_POINT ( 'NONE',  ( 63.37834727611930674, 0.9755120847815890173, -61.99042069074619832 ) ) ;
#11929=ORIENTED_EDGE ( 'NONE', *, *, #41272, .F. ) ;
#11934=DIRECTION ( 'NONE',  ( 0.000000000000000000, -1.000000000000000000, 0.000000000000000000 ) ) ;
#11947=CIRCLE ( 'NONE', #41231, 0.5000000000000000000 ) ;
#11955=CARTESIAN_POINT ( 'NONE',  ( 72.48038400710301232, 1.530257664727401545, -68.84999999999999432 ) ) ;
#11956=CARTESIAN_POINT ( 'NONE',  ( 72.06663613036050720, 1.456055805561079941, -69.85592311231539497 ) ) ;
#12048=CARTESIAN_POINT ( 'NONE',  ( 71.83393739769618946, 10.88381105532070059, -62.44999999999999574 ) ) ;
#12062=DIRECTION ( 'NONE',  ( 1.000000000000000000, 0.000000000000000000, 0.000000000000000000 ) ) ;
#12087=CARTESIAN_POINT ( 'NONE',  ( 63.17872741171709805, 1.188582381068100213, -68.85996346914730282 ) ) ;
#12090=DIRECTION ( 'NONE',  ( 0.000000000000000000, 0.000000000000000000, -1.000000000000000000 ) ) ;
#12099=CARTESIAN_POINT ( 'NONE',  ( 71.05099032166229733, 1.383136297697689976, -70.36878149631539259 ) ) ;
#12107=CARTESIAN_POINT ( 'NONE',  ( 71.21710443884710173, 1.384378348444510243, -60.98758765055369935 ) ) ;
#12109=CARTESIAN_POINT ( 'NONE',  ( 72.68564311439560299, 1.087300712305049988, -61.74844476645729685 ) ) ;
#12110=ADVANCED_FACE ( 'NONE', ( #48509 ), #36435, .T. ) ;
#12112=CARTESIAN_POINT ( 'NONE',  ( 64.98600614086839755, 1.191644800533210091, -70.64005307315139248 ) ) ;
#12113=ORIENTED_EDGE ( 'NONE', *, *, #22211, .T. ) ;
#12139=LINE ( 'NONE', #4780, #24792 ) ;
#12141=CARTESIAN_POINT ( 'NONE',  ( 64.12887023277500020, 1.457834087086459895, -69.79194131696009151 ) ) ;
#12155=CARTESIAN_POINT ( 'NONE',  ( 63.36863247553639411, 1.371651820402770117, -62.65029732562830844 ) ) ;
#12175=EDGE_LOOP ( 'NONE', ( #43925, #46023 ) ) ;
#12205=CARTESIAN_POINT ( 'NONE',  ( 72.41971899104120780, 1.437400661353670062, -69.51820902033620087 ) ) ;
#12211=CARTESIAN_POINT ( 'NONE',  ( 63.77506981661740326, 1.028299550205570068, -69.77396888106839867 ) ) ;
#12250=CARTESIAN_POINT ( 'NONE',  ( 64.84324960441189489, 0.8888742037077579372, -70.66714310028379487 ) ) ;
#12251=DIRECTION ( 'NONE',  ( -1.000000000000000000, 0.000000000000000000, 0.000000000000000000 ) ) ;
#12308=ORIENTED_EDGE ( 'NONE', *, *, #48865, .F. ) ;
#12309=CARTESIAN_POINT ( 'NONE',  ( 71.38118348160060123, 1.400446703426730055, -70.22110957219430816 ) ) ;
#12311=ORIENTED_EDGE ( 'NONE', *, *, #43714, .T. ) ;
#12327=CARTESIAN_POINT ( 'NONE',  ( 71.07527734533519492, 1.384447124000270035, -60.97624892474630087 ) ) ;
#12329=DIRECTION ( 'NONE',  ( 0.000000000000000000, 0.7071067811865492381, 0.7071067811865457964 ) ) ;
#12334=CARTESIAN_POINT ( 'NONE',  ( 63.00666467042349694, 0.9212109678634080590, -68.76625967790960203 ) ) ;
#12346=CARTESIAN_POINT ( 'NONE',  ( 71.15549028777350316, 1.383161449028130097, -70.33386915736630840 ) ) ;
#12349=EDGE_CURVE ( 'NONE', #33931, #34264, #15063, .T. ) ;
#12355=CARTESIAN_POINT ( 'NONE',  ( 71.29701819511369365, 1.369719003397489976, -60.94773069968270107 ) ) ;
#12356=ADVANCED_FACE ( 'NONE', ( #43114 ), #7205, .T. ) ;
#12358=CARTESIAN_POINT ( 'NONE',  ( 71.47028093172080787, 1.369286338573760142, -61.00325184746190388 ) ) ;
#12362=CARTESIAN_POINT ( 'NONE',  ( 65.19259745005730622, 1.384447124000270035, -70.32375107525380997 ) ) ;
#12403=CARTESIAN_POINT ( 'NONE',  ( 63.13104210372130609, 0.9254905997697669973, -62.33773042465509917 ) ) ;
#12408=CARTESIAN_POINT ( 'NONE',  ( 71.75685251123249486, 1.434949534324269971, -61.23975123050709612 ) ) ;
#12412=CARTESIAN_POINT ( 'NONE',  ( 64.91481325068460251, 1.325839985408290067, -60.87288092506760506 ) ) ;
#12426=ORIENTED_EDGE ( 'NONE', *, *, #47696, .F. ) ;
#12435=ORIENTED_EDGE ( 'NONE', *, *, #14312, .F. ) ;
#12456=CARTESIAN_POINT ( 'NONE',  ( 72.66407988305761023, 1.091560265417719888, -69.57662740730940243 ) ) ;
#12484=VERTEX_POINT ( 'NONE', #27621 ) ;
#12542=CARTESIAN_POINT ( 'NONE',  ( 65.25681082723269810, 1.383811055320669947, -60.95624653118409242 ) ) ;
#12546=AXIS2_PLACEMENT_3D ( 'NONE', #4221, #5271, #543 ) ;
#12562=DIRECTION ( 'NONE',  ( -0.8059588108975358489, 0.1342272854598799692, 0.5765530599820818392 ) ) ;
#12576=DIRECTION ( 'NONE',  ( 0.000000000000000000, 1.000000000000000000, 0.000000000000000000 ) ) ;
#12578=PRODUCT_CONTEXT ( 'NONE', #7708, 'mechanical' ) ;
#12597=CARTESIAN_POINT ( 'NONE',  ( 63.24512423172760833, 1.266538207494809942, -68.83138049123679991 ) ) ;
#12609=CARTESIAN_POINT ( 'NONE',  ( 71.15040120820690106, 1.386342629514219826, -70.29952392096339508 ) ) ;
#12616=CARTESIAN_POINT ( 'NONE',  ( 73.20448466830819712, 0.9214125008369580261, -68.85787081529349507 ) ) ;
#12622=CARTESIAN_POINT ( 'NONE',  ( 71.35306154470789863, 1.325839985408290067, -60.87288092506760506 ) ) ;
#12624=CARTESIAN_POINT ( 'NONE',  ( 71.77894708589589357, 1.045341414532560131, -60.89274515693429635 ) ) ;
#12628=CARTESIAN_POINT ( 'NONE',  ( 64.86043556304430524, 0.9234936569010840923, -70.67837287176459427 ) ) ;
#12673=CARTESIAN_POINT ( 'NONE',  ( 63.10820510261260097, 1.196343736543249880, -62.56767596405429543 ) ) ;
#12709=DIRECTION ( 'NONE',  ( -0.5765530599821041546, 0.1342272854595170650, 0.8059588108975803689 ) ) ;
#12727=CARTESIAN_POINT ( 'NONE',  ( 72.35673087767170841, 1.454949836291170140, -69.56035747320190410 ) ) ;
#12741=CARTESIAN_POINT ( 'NONE',  ( 64.20123866503199395, 1.456055805561079941, -61.44407688768469455 ) ) ;
#12751=ORIENTED_EDGE ( 'NONE', *, *, #46268, .F. ) ;
#12776=CARTESIAN_POINT ( 'NONE',  ( 64.77932207159149414, 0.8936201581567910779, -70.62461353540290077 ) ) ;
#12786=CARTESIAN_POINT ( 'NONE',  ( 64.03000686827549259, 1.054783673856589887, -70.02747328088919687 ) ) ;
#12832=CARTESIAN_POINT ( 'NONE',  ( 72.49788296046230585, 1.442158793902679870, -69.35604527063249236 ) ) ;
#12834=ADVANCED_FACE ( 'NONE', ( #26267 ), #38117, .T. ) ;
#12838=DIRECTION ( 'NONE',  ( 1.000000000000000000, 0.000000000000000000, 0.000000000000000000 ) ) ;
#12853=DIRECTION ( 'NONE',  ( 0.000000000000000000, 0.000000000000000000, -1.000000000000000000 ) ) ;
#12857=CARTESIAN_POINT ( 'NONE',  ( 71.17905174416029013, 1.387412027389909985, -61.00994802092580471 ) ) ;
#12859=CYLINDRICAL_SURFACE ( 'NONE', #44484, 0.4999999999999994449 ) ;
#12865=CARTESIAN_POINT ( 'NONE',  ( 63.16073670604789925, 0.9971903505820729485, -68.99379187066199393 ) ) ;
#12876=CARTESIAN_POINT ( 'NONE',  ( 71.13601697155240799, 1.385888765344509999, -70.30422512560809878 ) ) ;
#12884=CARTESIAN_POINT ( 'NONE',  ( 73.01702207920239118, 1.186614556332910020, -68.98303591127670131 ) ) ;
#12887=CARTESIAN_POINT ( 'NONE',  ( 73.24770736846269870, 0.9209567800143640959, -62.51152384389749272 ) ) ;
#12889=CARTESIAN_POINT ( 'NONE',  ( 71.38053669821270830, 1.187415670095769871, -60.71585052632950408 ) ) ;
#12890=DIRECTION ( 'NONE',  ( -0.7071067811865457964, 0.7071067811865492381, 0.000000000000000000 ) ) ;
#12892=CARTESIAN_POINT ( 'NONE',  ( 71.69261393255278847, 0.9208623934718309645, -60.81910352240609541 ) ) ;
#12894=CARTESIAN_POINT ( 'NONE',  ( 65.01767019485730259, 1.328674444234379859, -70.47425850519080370 ) ) ;
#12920=EDGE_CURVE ( 'NONE', #28142, #31343, #19232, .T. ) ;
#12927=DIRECTION ( 'NONE',  ( 0.000000000000000000, 0.000000000000000000, -1.000000000000000000 ) ) ;
#12934=CARTESIAN_POINT ( 'NONE',  ( 63.51391054266390768, 1.390208944942419755, -62.54542373973200142 ) ) ;
#12943=CARTESIAN_POINT ( 'NONE',  ( 64.93393739769589956, 1.396834109478120034, -61.06337307536559678 ) ) ;
#12948=ORIENTED_EDGE ( 'NONE', *, *, #11486, .T. ) ;
#12969=ORIENTED_EDGE ( 'NONE', *, *, #29963, .T. ) ;
#12994=CARTESIAN_POINT ( 'NONE',  ( 72.24311954201340313, 1.458407608744489936, -69.69055806410209186 ) ) ;
#12997=CARTESIAN_POINT ( 'NONE',  ( 72.05113849075890187, 0.9952277120684990264, -70.19587804460290670 ) ) ;
#13006=CARTESIAN_POINT ( 'NONE',  ( 64.36679430080839381, 1.446932438105809737, -61.32315308161489753 ) ) ;
#13007=EDGE_LOOP ( 'NONE', ( #29236, #13474, #18783, #16897, #32028 ) ) ;
#13020=VERTEX_POINT ( 'NONE', #28202 ) ;
#13053=CARTESIAN_POINT ( 'NONE',  ( 63.83188146504109284, 1.061276598305570085, -69.83322846870700573 ) ) ;
#13131=CARTESIAN_POINT ( 'NONE',  ( 73.10258273731270151, 1.278021359705819870, -68.66984894295178776 ) ) ;
#13145=CARTESIAN_POINT ( 'NONE',  ( 71.18923915728029783, 1.331842543267529821, -70.50106597067950531 ) ) ;
#13148=ORIENTED_EDGE ( 'NONE', *, *, #45775, .F. ) ;
#13151=CARTESIAN_POINT ( 'NONE',  ( 72.79634974714259954, 1.384378348444520013, -68.73316704115080711 ) ) ;
#13154=CARTESIAN_POINT ( 'NONE',  ( 73.22759735627531086, 0.9947083095259759977, -62.49453424214399888 ) ) ;
#13158=CARTESIAN_POINT ( 'NONE',  ( 71.77241571698009182, 1.241979851175089911, -60.99005311882309854 ) ) ;
#13159=AXIS2_PLACEMENT_3D ( 'NONE', #18578, #9944, #30619 ) ;
#13163=CARTESIAN_POINT ( 'NONE',  ( 65.09331375576360301, 1.276058558775509999, -70.60879112794539481 ) ) ;
#13179=B_SPLINE_CURVE_WITH_KNOTS ( 'NONE', 3,
 ( #47777, #11883, #27073, #27841, #43841, #38632, #10850, #19212, #22872, #34674, #27328, #50933, #50674, #14772, #11365, #30741 ),
 .UNSPECIFIED., .F., .F.,
 ( 4, 2, 2, 2, 2, 2, 2, 4 ),
 ( -8.523275000000000432E-16, 0.07216186899280999101, 0.1546325764131659952, 0.2061767685508879844, 0.2319488646197490067, 0.2731842183299269533, 0.3391607842662109906, 0.4123535371017769680 ),
 .UNSPECIFIED. ) ;
#13202=CARTESIAN_POINT ( 'NONE',  ( 63.41989057163110743, 1.369544300367010026, -62.51645495968789845 ) ) ;
#13221=ORIENTED_EDGE ( 'NONE', *, *, #7219, .T. ) ;
#13229=CARTESIAN_POINT ( 'NONE',  ( 72.48038400710301232, 1.530257664727401545, -65.65000000000000568 ) ) ;
#13230=ORIENTED_EDGE ( 'NONE', *, *, #27836, .F. ) ;
#13236=EDGE_LOOP ( 'NONE', ( #48602, #16676, #26795, #25747 ) ) ;
#13237=CARTESIAN_POINT ( 'NONE',  ( 72.74776047649520194, 1.391252479931859964, -62.52735703481241103 ) ) ;
#13251=CARTESIAN_POINT ( 'NONE',  ( 73.01385068780759013, 0.9098571636355720083, -62.15909090909049439 ) ) ;
#13263=CARTESIAN_POINT ( 'NONE',  ( 64.15658392863279857, 1.099201050715910011, -61.16377310064390116 ) ) ;
#13267=CIRCLE ( 'NONE', #671, 6.000000000000005329 ) ;
#13301=CARTESIAN_POINT ( 'NONE',  ( 64.36988470191930389, 1.396287116999079814, -70.06934168479099867 ) ) ;
#13311=EDGE_CURVE ( 'NONE', #36774, #14211, #3748, .T. ) ;
#13319=DIRECTION ( 'NONE',  ( 0.000000000000000000, 1.000000000000000000, 0.000000000000000000 ) ) ;
#13357=ADVANCED_FACE ( 'NONE', ( #41188 ), #42625, .F. ) ;
#13367=ORIENTED_EDGE ( 'NONE', *, *, #22674, .F. ) ;
#13369=CARTESIAN_POINT ( 'NONE',  ( 65.03067915409710054, 1.194703186106690129, -60.63553603340079690 ) ) ;
#13380=CARTESIAN_POINT ( 'NONE',  ( 64.64302830678670375, 0.9098571636355720083, -60.77008670988870165 ) ) ;
#13395=CARTESIAN_POINT ( 'NONE',  ( 71.33702656696020483, 1.265664290790580182, -70.52755531239479581 ) ) ;
#13400=CARTESIAN_POINT ( 'NONE',  ( 73.10855093309899644, 0.8936201581567889685, -69.00461532610479765 ) ) ;
#13407=CARTESIAN_POINT ( 'NONE',  ( 71.89814544471239799, 1.396295651964280182, -61.23077165321539184 ) ) ;
#13410=CARTESIAN_POINT ( 'NONE',  ( 64.76518258084509228, 1.097545367735389910, -70.56928864606319962 ) ) ;
#13453=AXIS2_PLACEMENT_3D ( 'NONE', #37246, #25425, #28585 ) ;
#13456=CARTESIAN_POINT ( 'NONE',  ( 63.22228946811710415, 1.003508719580009867, -62.21555175845400498 ) ) ;
#13457=DIRECTION ( 'NONE',  ( 0.000000000000000000, 0.000000000000000000, -1.000000000000000000 ) ) ;
#13460=DIRECTION ( 'NONE',  ( 6.938893903907222067E-15, 0.000000000000000000, -1.000000000000000000 ) ) ;
#13466=CARTESIAN_POINT ( 'NONE',  ( 63.54731047306190561, 1.396834109478129804, -68.84999999999999432 ) ) ;
#13469=CARTESIAN_POINT ( 'NONE',  ( 64.93393739769619799, 1.396834109478129804, -70.23662692463440749 ) ) ;
#13474=ORIENTED_EDGE ( 'NONE', *, *, #49288, .T. ) ;
#13483=CARTESIAN_POINT ( 'NONE',  ( 63.86577392472210590, 1.451792515613489876, -61.80022504404329453 ) ) ;
#13492=PRODUCT_DEFINITION_FORMATION_WITH_SPECIFIED_SOURCE ( 'ANY', '', #16002, .NOT_KNOWN. ) ;
#13511=CARTESIAN_POINT ( 'NONE',  ( 72.56482987857130240, 1.421976796945970012, -69.29343522641019604 ) ) ;
#13522=CARTESIAN_POINT ( 'NONE',  ( 64.64547391238390617, 1.377110276564549984, -61.07324425200700091 ) ) ;
#13551=CARTESIAN_POINT ( 'NONE',  ( 68.13393739769620083, 0.8838110553206759423, -65.65000000000000568 ) ) ;
#13558=CARTESIAN_POINT ( 'NONE',  ( 63.83871783002559397, 1.346166815163519992, -69.67924993017680890 ) ) ;
#13577=CARTESIAN_POINT ( 'NONE',  ( 65.23632417210509971, 1.383928098097870096, -60.96256459357869772 ) ) ;
#13583=CARTESIAN_POINT ( 'NONE',  ( 72.77636315587029969, 1.387131204727280132, -68.68796153961081075 ) ) ;
#13629=CARTESIAN_POINT ( 'NONE',  ( 64.22355794744891000, 1.454950765200730078, -69.87277598216670071 ) ) ;
#13634=CARTESIAN_POINT ( 'NONE',  ( 64.68608103367580497, 0.9036513197889539661, -60.73950228677190211 ) ) ;
#13652=CARTESIAN_POINT ( 'NONE',  ( 73.11690592692660573, 0.8925687589132640376, -68.99219224778180148 ) ) ;
#13655=CARTESIAN_POINT ( 'NONE',  ( 72.95819590288698464, 1.328674444234379859, -62.53373279716100086 ) ) ;
#13657=CARTESIAN_POINT ( 'NONE',  ( 71.29447239804829906, 1.393731187554809958, -61.04935521477050031 ) ) ;
#13661=CARTESIAN_POINT ( 'NONE',  ( 64.82191989009379540, 0.9958340104639651358, -70.64420736479868879 ) ) ;
#13709=CARTESIAN_POINT ( 'NONE',  ( 63.40532295848070987, 1.369664981662529923, -62.55358821066108987 ) ) ;
#13719=CARTESIAN_POINT ( 'NONE',  ( 63.58464056502309347, 1.025917269765419970, -69.56324595238550046 ) ) ;
#13721=ORIENTED_EDGE ( 'NONE', *, *, #39582, .F. ) ;
#13737=CARTESIAN_POINT ( 'NONE',  ( 63.93393739769619089, 1.883811055320669947, -68.84999999999999432 ) ) ;
#13758=CARTESIAN_POINT ( 'NONE',  ( 73.20393974370449541, 0.8850831926798620186, -62.44126551166660022 ) ) ;
#13760=CARTESIAN_POINT ( 'NONE',  ( 72.83631794868971099, 1.056975075118959939, -69.36644202706580131 ) ) ;
#13773=CIRCLE ( 'NONE', #43079, 0.5000000000000000000 ) ;
#13775=CARTESIAN_POINT ( 'NONE',  ( 64.55375726973680628, 0.9618757110842720559, -60.83484875704370154 ) ) ;
#13796=DIRECTION ( 'NONE',  ( 0.000000000000000000, 0.000000000000000000, -1.000000000000000000 ) ) ;
#13797=ORIENTED_EDGE ( 'NONE', *, *, #32015, .T. ) ;
#13808=CARTESIAN_POINT ( 'NONE',  ( 64.12887023277500020, 1.457834087086459895, -69.79194131696009151 ) ) ;
#13817=CARTESIAN_POINT ( 'NONE',  ( 63.47556362806851382, 1.384708701328909886, -68.74455794701600553 ) ) ;
#13841=EDGE_LOOP ( 'NONE', ( #9952, #51096, #35026, #14203 ) ) ;
#13876=CARTESIAN_POINT ( 'NONE',  ( 65.21688447373020381, 1.383136297697689976, -60.93121850368469694 ) ) ;
#13899=CARTESIAN_POINT ( 'NONE',  ( 64.66447934098378880, 0.9065823421260970072, -60.75474143511929981 ) ) ;
#13905=CARTESIAN_POINT ( 'NONE',  ( 73.10923647485390120, 1.096036836948800053, -68.93088433361418765 ) ) ;
#13908=CARTESIAN_POINT ( 'NONE',  ( 72.83058059882510804, 1.382840740411490188, -62.66598281567230089 ) ) ;
#13912=CARTESIAN_POINT ( 'NONE',  ( 71.27262092911099955, 0.8838110553206740549, -60.53635606803790381 ) ) ;
#13916=CARTESIAN_POINT ( 'NONE',  ( 64.92362553771700107, 1.265401080857980087, -70.52378931128959039 ) ) ;
#13926=ORIENTED_EDGE ( 'NONE', *, *, #50630, .T. ) ;
#13931=DIRECTION ( 'NONE',  ( 0.000000000000000000, 1.000000000000000000, 0.000000000000000000 ) ) ;
#13936=ORIENTED_EDGE ( 'NONE', *, *, #9652, .T. ) ;
#13954=ADVANCED_FACE ( 'NONE', ( #41122 ), #17024, .T. ) ;
#13961=CARTESIAN_POINT ( 'NONE',  ( 63.49151163952229382, 1.387131204727290124, -62.61203846038919352 ) ) ;
#13966=CARTESIAN_POINT ( 'NONE',  ( 71.33393739769628894, 1.883811055320669947, -70.34999999999999432 ) ) ;
#13971=CARTESIAN_POINT ( 'NONE',  ( 63.54316066981328959, 1.321110558595150142, -69.27633817897910262 ) ) ;
#13976=CARTESIAN_POINT ( 'NONE',  ( 72.86184465953650147, 1.051325075269279985, -61.96652996135610181 ) ) ;
#14004=B_SPLINE_SURFACE_WITH_KNOTS ( 'NONE', 3, 3, ( 
 ( #51739, #15835, #44579, #25161, #8683, #24893, #17329, #49308, #33292, #20713 ),
 ( #49048, #29361, #9209, #24635, #36977, #41168, #45367, #3540, #12887, #19510 ),
 ( #20977, #4746, #48780, #1074, #36704, #40906, #5016, #13154, #29104, #38537 ),
 ( #41421, #2364, #42471, #49816, #37756, #50587, #10755, #29616, #6048, #17832 ),
 ( #6307, #13908, #42209, #45885, #22265, #9972, #38015, #21748, #21494, #25934 ),
 ( #46412, #33805, #37494, #13655, #45619, #41948, #34583, #49569, #30647, #38273 ),
 ( #30130, #6560, #29865, #22525, #18342, #2633, #14162, #41680, #18605, #14677 ),
 ( #46670, #50332, #22006, #14420, #2110, #5539, #30388, #1594, #10500, #17582 ),
 ( #18089, #34057, #1854, #50067, #46151, #33552, #10239, #34319, #9719, #25678 ),
 ( #26456, #26198, #5788, #39817, #19887, #23803, #43251, #3927, #3669, #35878 ),
 ( #15199, #7601, #31667, #7853, #11794, #35363, #43751, #31158, #43499, #47186 ),
 ( #39309, #35099, #23545, #7338, #33548, #15971, #46929, #31925, #39563, #51362 ),
 ( #23037, #47947, #26714, #14935, #23286, #3152, #27754, #19639, #51100, #27492 ),
 ( #35631, #11273, #3412, #7087, #6828, #27233, #42733, #47690, #19120, #22780 ),
 ( #50844, #19380, #38800, #34844, #2894, #18859, #11013, #51617, #15710, #30900 ),
 ( #26984, #42991, #15462, #39059, #31412, #47440, #11535, #20654, #33226, #24056 ) ),
 .UNSPECIFIED., .F., .F., .F.,
 ( 4, 2, 2, 2, 2, 2, 2, 4 ),
 ( 4, 1, 1, 1, 1, 1, 1, 4 ),
 ( 6.613222000000000237E-15, 0.07216186899281500089, 0.1546325764131659952, 0.2061767685508859860, 0.2319488646197460091, 0.2731842183299219573, 0.3391607842662039962, 0.4123535371017659767 ),
 ( 0.000000000000000000, 0.1428571428571430157, 0.2857142857142860315, 0.4285714285714289917, 0.5714285714285709528, 0.7142857142857139685, 0.8571428571428569843, 1.000000000000000000 ),
 .UNSPECIFIED. ) ;
#14013=CARTESIAN_POINT ( 'NONE',  ( 72.82314924247010879, 1.153605328057900170, -69.33289095355348763 ) ) ;
#14019=CARTESIAN_POINT ( 'NONE',  ( 65.01129443250870565, 1.391252479931859964, -70.26382307879910627 ) ) ;
#14028=CARTESIAN_POINT ( 'NONE',  ( 63.89396393056810552, 1.440335647928530083, -61.72174419063350115 ) ) ;
#14052=CARTESIAN_POINT ( 'NONE',  ( 71.83393739769618946, 11.38381105532070059, -68.84999999999999432 ) ) ;
#14064=CARTESIAN_POINT ( 'NONE',  ( 64.62682451405710538, 1.027624964385369877, -70.50782134747939267 ) ) ;
#14075=CARTESIAN_POINT ( 'NONE',  ( 63.32591849070559675, 1.327322800621349996, -68.80227784490020326 ) ) ;
#14114=CYLINDRICAL_SURFACE ( 'NONE', #25310, 0.4999999999999364397 ) ;
#14121=VERTEX_POINT ( 'NONE', #9921 ) ;
#14138=CARTESIAN_POINT ( 'NONE',  ( 65.01767771978660448, 0.8838110553206759423, -60.52272727272730179 ) ) ;
#14141=CARTESIAN_POINT ( 'NONE',  ( 64.93393739769619799, 11.38381105532070059, -61.94999999999999574 ) ) ;
#14143=ORIENTED_EDGE ( 'NONE', *, *, #47982, .F. ) ;
#14155=CARTESIAN_POINT ( 'NONE',  ( 64.76223432283440218, 1.187296498006439993, -60.79044767480839795 ) ) ;
#14162=CARTESIAN_POINT ( 'NONE',  ( 73.12314370215899828, 1.096110717717209804, -62.39142878032480155 ) ) ;
#14164=CARTESIAN_POINT ( 'NONE',  ( 71.44880243016270072, 1.326666718054979821, -60.91913985162000245 ) ) ;
#14166=CARTESIAN_POINT ( 'NONE',  ( 71.36799767121769378, 0.8859637708054480809, -60.59611492242089525 ) ) ;
#14169=CARTESIAN_POINT ( 'NONE',  ( 64.84946247134770658, 1.186701509386330011, -70.56202332290359891 ) ) ;
#14203=ORIENTED_EDGE ( 'NONE', *, *, #43013, .T. ) ;
#14211=VERTEX_POINT ( 'NONE', #47138 ) ;
#14215=CARTESIAN_POINT ( 'NONE',  ( 63.28685848367280897, 1.187931651339009909, -62.25809267083580778 ) ) ;
#14216=DIRECTION ( 'NONE',  ( 0.000000000000000000, -1.000000000000000000, 0.000000000000000000 ) ) ;
#14225=CARTESIAN_POINT ( 'NONE',  ( 63.46161254120319484, 1.063296977482639960, -69.40459734810629300 ) ) ;
#14230=CARTESIAN_POINT ( 'NONE',  ( 72.80915813965889072, 1.367045641526529964, -62.38166218803879559 ) ) ;
#14231=AXIS2_PLACEMENT_3D ( 'NONE', #3851, #43935, #16147 ) ;
#14244=CARTESIAN_POINT ( 'NONE',  ( 63.49388541862201407, 1.387412027389909985, -68.69511434646409498 ) ) ;
#14250=EDGE_CURVE ( 'NONE', #1196, #23424, #27704, .T. ) ;
#14270=CARTESIAN_POINT ( 'NONE',  ( 68.13393739769620083, 11.38381105532070059, -65.65000000000000568 ) ) ;
#14272=DIRECTION ( 'NONE',  ( 0.000000000000000000, 0.000000000000000000, -1.000000000000000000 ) ) ;
#14273=CARTESIAN_POINT ( 'NONE',  ( 72.72056432233058842, 1.396834109478129804, -68.84999999999999432 ) ) ;
#14277=CARTESIAN_POINT ( 'NONE',  ( 72.33393739770313857, 10.88381105532029380, -69.85000000000677289 ) ) ;
#14286=CARTESIAN_POINT ( 'NONE',  ( 63.47399051652649860, 1.241979851175949889, -62.01152168070590420 ) ) ;
#14312=EDGE_CURVE ( 'NONE', #29849, #37903, #19335, .T. ) ;
#14319=CARTESIAN_POINT ( 'NONE',  ( 64.79641848607099064, 1.369332017692449943, -70.29624551492651108 ) ) ;
#14332=CARTESIAN_POINT ( 'NONE',  ( 63.23977555071250123, 1.186515949276290227, -68.96459770949519452 ) ) ;
#14341=CARTESIAN_POINT ( 'NONE',  ( 71.44807725908989937, 0.8904513541338849869, -70.65165619965239330 ) ) ;
#14373=CIRCLE ( 'NONE', #11018, 0.5000000000000000000 ) ;
#14390=CARTESIAN_POINT ( 'NONE',  ( 64.92606658240281092, 0.9214125008369580261, -60.57945272938810177 ) ) ;
#14420=CARTESIAN_POINT ( 'NONE',  ( 72.94195630468689728, 1.327322800621349996, -62.49772215509980100 ) ) ;
#14427=CARTESIAN_POINT ( 'NONE',  ( 64.77932207159149414, 0.8936201581567889685, -70.62461353540280129 ) ) ;
#14445=EDGE_CURVE ( 'NONE', #41111, #28142, #18407, .T. ) ;
#14470=CARTESIAN_POINT ( 'NONE',  ( 71.33393739769670105, 0.9098571636355720083, -61.17674615073129729 ) ) ;
#14480=CARTESIAN_POINT ( 'NONE',  ( 63.40501886558961075, 1.309113972621119837, -69.02948859405739768 ) ) ;
#14483=CARTESIAN_POINT ( 'NONE',  ( 71.17456103962899761, 1.276058558775509999, -60.69120887205459525 ) ) ;
#14486=CARTESIAN_POINT ( 'NONE',  ( 72.85590616764901029, 0.9486745332815790244, -61.94714277540219882 ) ) ;
#14513=CARTESIAN_POINT ( 'NONE',  ( 73.20393974370439594, 0.8850831926798620186, -68.85873448833349642 ) ) ;
#14516=TOROIDAL_SURFACE ( 'NONE', #21311, 5.500000000000000000, 0.5000000000000000000 ) ;
#14534=DIRECTION ( 'NONE',  ( -0.8059588108975778153, 0.1342272854594989684, -0.5765530599821118152 ) ) ;
#14544=CARTESIAN_POINT ( 'NONE',  ( 63.55130486076479457, 0.9860880133283479454, -61.77606584740419748 ) ) ;
#14577=CARTESIAN_POINT ( 'NONE',  ( 64.49518718159480102, 1.242005038313980014, -70.30973843397600831 ) ) ;
#14585=CARTESIAN_POINT ( 'NONE',  ( 71.52463645511689094, 1.229084191802120030, -70.46414972969260759 ) ) ;
#14589=CARTESIAN_POINT ( 'NONE',  ( 63.19468704395299596, 0.8986939045430379913, -69.05651959838648679 ) ) ;
#14600=CARTESIAN_POINT ( 'NONE',  ( 71.45588032111159293, 0.8910129994591549085, -70.64647704525299332 ) ) ;
#14645=AXIS2_PLACEMENT_3D ( 'NONE', #19659, #12576, #36402 ) ;
#14647=CARTESIAN_POINT ( 'NONE',  ( 65.03752560835731344, 1.369664981662519931, -60.92138556078450051 ) ) ;
#14677=CARTESIAN_POINT ( 'NONE',  ( 73.15108049798000422, 0.8888742037077609348, -62.35931220671560027 ) ) ;
#14684=CARTESIAN_POINT ( 'NONE',  ( 64.74203006853210240, 1.187931651339009909, -70.49707891402360360 ) ) ;
#14707=EDGE_CURVE ( 'NONE', #16787, #5288, #7536, .T. ) ;
#14731=CARTESIAN_POINT ( 'NONE',  ( 63.51397770047800861, 1.389468113695440099, -62.45014271800210537 ) ) ;
#14744=CARTESIAN_POINT ( 'NONE',  ( 71.33861941035669929, 1.097085799869280009, -60.62778596399619602 ) ) ;
#14759=CARTESIAN_POINT ( 'NONE',  ( 63.54027722212589424, 1.395196698723390138, -68.83033655198650536 ) ) ;
#14769=DIRECTION ( 'NONE',  ( 0.000000000000000000, 0.000000000000000000, 1.000000000000000000 ) ) ;
#14772=CARTESIAN_POINT ( 'NONE',  ( 63.22343968446819673, 0.9036513197889520788, -62.20214363597949614 ) ) ;
#14804=CARTESIAN_POINT ( 'NONE',  ( 63.83389103303669998, 1.116860450401449878, -61.47226487784700311 ) ) ;
#14807=DIRECTION ( 'NONE',  ( 0.000000000000000000, 0.000000000000000000, -1.000000000000000000 ) ) ;
#14808=CARTESIAN_POINT ( 'NONE',  ( 73.18852689059310990, 0.9219904752505979628, -68.88295677568349618 ) ) ;
#14825=DIRECTION ( 'NONE',  ( 0.000000000000000000, 1.000000000000000000, 0.000000000000000000 ) ) ;
#14826=CARTESIAN_POINT ( 'NONE',  ( 65.01767771978660448, 0.8838110553206759423, -60.52272727272730179 ) ) ;
#14837=CARTESIAN_POINT ( 'NONE',  ( 64.51140068127359939, 1.434916633744939940, -70.06045877469239258 ) ) ;
#14845=CARTESIAN_POINT ( 'NONE',  ( 72.05113849075890187, 0.9952277120684979161, -70.19587804460300617 ) ) ;
#14865=CARTESIAN_POINT ( 'NONE',  ( 71.34267188602959209, 0.8850831926798620186, -70.72000234600820079 ) ) ;
#14868=DIRECTION ( 'NONE',  ( -1.000000000000000000, 0.000000000000000000, 0.000000000000000000 ) ) ;
#14879=FACE_OUTER_BOUND ( 'NONE', #41585, .T. ) ;
#14904=CARTESIAN_POINT ( 'NONE',  ( 65.09597585808539577, 1.387131204727280132, -61.00757424182599920 ) ) ;
#14933=CARTESIAN_POINT ( 'NONE',  ( 72.92278648876269642, 1.264689361399219836, -69.01667010504620237 ) ) ;
#14935=CARTESIAN_POINT ( 'NONE',  ( 72.90248002265630589, 1.325715844996850024, -62.41274800841679848 ) ) ;
#14986=CARTESIAN_POINT ( 'NONE',  ( 63.52141932237860544, 1.390806392144100068, -62.43047455269960011 ) ) ;
#14995=DIRECTION ( 'NONE',  ( 0.000000000000000000, -1.000000000000000000, 0.000000000000000000 ) ) ;
#14998=CARTESIAN_POINT ( 'NONE',  ( 71.30079129029560647, 1.267233196669030004, -60.75373513970999539 ) ) ;
#15000=CARTESIAN_POINT ( 'NONE',  ( 73.01385068780759013, 0.9098571636355720083, -62.15909090909049439 ) ) ;
#15047=CIRCLE ( 'NONE', #23367, 0.5000000000000004441 ) ;
#15060=CARTESIAN_POINT ( 'NONE',  ( 63.87013147868781004, 1.277124412296160028, -61.51639082798710234 ) ) ;
#15063=LINE ( 'NONE', #27111, #32555 ) ;
#15064=CARTESIAN_POINT ( 'NONE',  ( 73.24770736846269870, 0.9209567800143640959, -68.78847615610258970 ) ) ;
#15080=ORIENTED_EDGE ( 'NONE', *, *, #31664, .F. ) ;
#15098=CARTESIAN_POINT ( 'NONE',  ( 64.47339077398659413, 0.9757097601092069583, -70.40482852006680048 ) ) ;
#15101=ORIENTED_EDGE ( 'NONE', *, *, #46325, .F. ) ;
#15105=CARTESIAN_POINT ( 'NONE',  ( 71.92023852231459102, 1.432916438945839976, -69.99522902979279593 ) ) ;
#15111=CARTESIAN_POINT ( 'NONE',  ( 63.40307724931621181, 1.326666718054969829, -68.96486503246650557 ) ) ;
#15121=CARTESIAN_POINT ( 'NONE',  ( 71.44620697304119972, 0.9254905997697669973, -70.65289529397499280 ) ) ;
#15163=CARTESIAN_POINT ( 'NONE',  ( 71.25658036288379549, 1.391252479931859964, -70.26382307879899258 ) ) ;
#15170=CARTESIAN_POINT ( 'NONE',  ( 64.90928650851489579, 1.188042061556800144, -60.70318061837799917 ) ) ;
#15192=ORIENTED_EDGE ( 'NONE', *, *, #32015, .F. ) ;
#15199=CARTESIAN_POINT ( 'NONE',  ( 72.76396860142250489, 1.388715606738730068, -62.57493595107060713 ) ) ;
#15205=AXIS2_PLACEMENT_3D ( 'NONE', #32997, #776, #523 ) ;
#15206=AXIS2_PLACEMENT_3D ( 'NONE', #21124, #20597, #24781 ) ;
#15246=DIRECTION ( 'NONE',  ( 1.000000000000000000, 0.000000000000000000, 0.000000000000000000 ) ) ;
#15265=CARTESIAN_POINT ( 'NONE',  ( 71.14534185144368905, 1.334812829108570131, -60.78020385162600547 ) ) ;
#15266=ADVANCED_FACE ( 'NONE', ( #11601 ), #5041, .T. ) ;
#15268=CARTESIAN_POINT ( 'NONE',  ( 72.47916642748789684, 1.432916438945919912, -61.86369887538009493 ) ) ;
#15315=DIRECTION ( 'NONE',  ( -1.000000000000000000, 0.000000000000000000, 0.000000000000000000 ) ) ;
#15325=CARTESIAN_POINT ( 'NONE',  ( 63.27571426518280617, 1.027568165752089868, -62.14345989183700425 ) ) ;
#15329=CARTESIAN_POINT ( 'NONE',  ( 73.08914738367541020, 1.188582381068100213, -68.85996346914730282 ) ) ;
#15337=AXIS2_PLACEMENT_3D ( 'NONE', #1442, #14272, #26303 ) ;
#15350=CARTESIAN_POINT ( 'NONE',  ( 72.82769086651219936, 1.383811055320669947, -62.77287342953649585 ) ) ;
#15366=CARTESIAN_POINT ( 'NONE',  ( 71.46698656264879901, 1.308647200627810259, -70.40208447574099182 ) ) ;
#15375=CARTESIAN_POINT ( 'NONE',  ( 64.93393739769619799, 1.883811055320669947, -69.84999999999999432 ) ) ;
#15400=DIRECTION ( 'NONE',  ( 0.000000000000000000, 0.000000000000000000, -1.000000000000000000 ) ) ;
#15412=CARTESIAN_POINT ( 'NONE',  ( 63.25402410758490390, 0.9098571636355720083, -69.14090909090960224 ) ) ;
#15413=DIRECTION ( 'NONE',  ( 0.000000000000000000, 1.000000000000000000, 0.000000000000000000 ) ) ;
#15431=CARTESIAN_POINT ( 'NONE',  ( 64.98165955279600325, 1.327322800621349996, -60.84198109300940160 ) ) ;
#15438=CARTESIAN_POINT ( 'NONE',  ( 71.67217357260551580, 0.9170823515327869435, -70.49605724842390941 ) ) ;
#15449=CARTESIAN_POINT ( 'NONE',  ( 71.33393739769628894, 10.88381105532070059, -61.94999999999999574 ) ) ;
#15462=CARTESIAN_POINT ( 'NONE',  ( 72.79675206836721202, 1.372372808637209785, -62.39142423721519748 ) ) ;
#15467=CARTESIAN_POINT ( 'NONE',  ( 64.68925548900169531, 0.9369374701296260266, -70.56272516144500173 ) ) ;
#15503=CARTESIAN_POINT ( 'NONE',  ( 63.18512348867459849, 1.274277262446069869, -68.71132524057000523 ) ) ;
#15523=CARTESIAN_POINT ( 'NONE',  ( 71.15378634064809660, 1.278021359705819870, -60.68135466038360448 ) ) ;
#15525=CARTESIAN_POINT ( 'NONE',  ( 72.57226300143969411, 1.394112346784049938, -61.91536134543299852 ) ) ;
#15544=CARTESIAN_POINT ( 'NONE',  ( 71.33393739769628894, 10.88381105532070059, -62.44999999999999574 ) ) ;
#15545=SHAPE_REPRESENTATION_RELATIONSHIP ( 'NONE' , 'NONE' ,  #50919, #2932 ) ;
#15575=CARTESIAN_POINT ( 'NONE',  ( 63.55130486076469509, 0.9860880133283429494, -61.77606584740410511 ) ) ;
#15589=CARTESIAN_POINT ( 'NONE',  ( 72.81780655506248934, 1.383161449028130097, -68.67155289007729380 ) ) ;
#15601=EDGE_CURVE ( 'NONE', #44049, #41820, #40221, .T. ) ;
#15608=CARTESIAN_POINT ( 'NONE',  ( 72.78346131865960444, 1.386342629514219826, -62.63353618948930546 ) ) ;
#15618=EDGE_CURVE ( 'NONE', #48970, #32793, #43246, .T. ) ;
#15624=CARTESIAN_POINT ( 'NONE',  ( 71.61742398551369604, 1.231980527806860071, -70.40894576833619567 ) ) ;
#15629=CARTESIAN_POINT ( 'NONE',  ( 63.46279604660929863, 1.371509258145880095, -68.88889814452589633 ) ) ;
#15632=CARTESIAN_POINT ( 'NONE',  ( 64.19260248505071331, 1.000485720979659821, -70.17481423849019961 ) ) ;
#15638=CARTESIAN_POINT ( 'NONE',  ( 71.56838563924230812, 1.003508719580009867, -70.56164792957919474 ) ) ;
#15646=ORIENTED_EDGE ( 'NONE', *, *, #9818, .T. ) ;
#15649=ORIENTED_EDGE ( 'NONE', *, *, #22435, .T. ) ;
#15667=CARTESIAN_POINT ( 'NONE',  ( 63.11679429741240455, 0.8888742037077590474, -68.94068779328429741 ) ) ;
#15683=CARTESIAN_POINT ( 'NONE',  ( 64.85231939490250852, 0.9948723650351710690, -60.63592931576840073 ) ) ;
#15710=CARTESIAN_POINT ( 'NONE',  ( 73.03159560797669769, 0.9395704634982890990, -62.18392983749130565 ) ) ;
#15716=CARTESIAN_POINT ( 'NONE',  ( 64.72587551647490045, 1.099344084866029858, -70.54350063839000029 ) ) ;
#15723=ADVANCED_FACE ( 'NONE', ( #29206 ), #50764, .F. ) ;
#15752=CARTESIAN_POINT ( 'NONE',  ( 63.16529205807979963, 1.278021359705819870, -68.66984894295178776 ) ) ;
#15768=DIRECTION ( 'NONE',  ( -0.8545454545454611583, 0.000000000000000000, 0.5193766129849238800 ) ) ;
#15771=DIRECTION ( 'NONE',  ( 1.000000000000000000, 0.000000000000000000, 0.000000000000000000 ) ) ;
#15773=CARTESIAN_POINT ( 'NONE',  ( 71.44807725908989937, 0.8904513541338849869, -60.64834380034769623 ) ) ;
#15775=CARTESIAN_POINT ( 'NONE',  ( 72.67592461730299647, 1.176186365485209828, -61.77681041909720250 ) ) ;
#15784=DIRECTION ( 'NONE',  ( -1.000000000000000000, 0.000000000000000000, 0.000000000000000000 ) ) ;
#15791=DIRECTION ( 'NONE',  ( -1.000000000000000000, 0.000000000000000000, 0.000000000000000000 ) ) ;
#15816=CARTESIAN_POINT ( 'NONE',  ( 63.39699138880700247, 1.369885150286800135, -62.57510434557890733 ) ) ;
#15833=CARTESIAN_POINT ( 'NONE',  ( 73.23405285996879854, 0.9209334348186318797, -68.81061689070359932 ) ) ;
#15835=CARTESIAN_POINT ( 'NONE',  ( 72.86589732295999511, 1.383811055320669947, -62.77400398868049081 ) ) ;
#15863=ADVANCED_FACE ( 'NONE', ( #50693 ), #30577, .T. ) ;
#15879=CARTESIAN_POINT ( 'NONE',  ( 72.55770162222249553, 1.107037132887370046, -69.69638372295169404 ) ) ;
#15887=LINE ( 'NONE', #15375, #5114 ) ;
#15893=CARTESIAN_POINT ( 'NONE',  ( 71.42252419164299226, 1.263738073398970041, -70.48213147351589214 ) ) ;
#15922=CARTESIAN_POINT ( 'NONE',  ( 68.13393739769620083, -42.11618894467930119, -65.65000000000000568 ) ) ;
#15936=ORIENTED_EDGE ( 'NONE', *, *, #35104, .T. ) ;
#15949=EDGE_CURVE ( 'NONE', #11777, #38817, #19172, .T. ) ;
#15958=ORIENTED_EDGE ( 'NONE', *, *, #23615, .F. ) ;
#15971=CARTESIAN_POINT ( 'NONE',  ( 73.02809924467999281, 1.186515949276290227, -62.33540229050490211 ) ) ;
#15992=AXIS2_PLACEMENT_3D ( 'NONE', #28002, #11015, #27494 ) ;
#16002=PRODUCT ( 'Wheel Axle Bolt', 'Wheel Axle Bolt', '', ( #12578 ) ) ;
#16009=CARTESIAN_POINT ( 'NONE',  ( 63.40852617131290003, 1.383411777981069957, -68.54655896616850441 ) ) ;
#16024=CARTESIAN_POINT ( 'NONE',  ( 71.34180821298970443, 0.9214125008369580261, -70.72054727061200197 ) ) ;
#16026=ORIENTED_EDGE ( 'NONE', *, *, #20615, .T. ) ;
#16027=DIRECTION ( 'NONE',  ( -0.5193766129849320956, 0.000000000000000000, -0.8545454545454562734 ) ) ;
#16032=CARTESIAN_POINT ( 'NONE',  ( 71.23851365796429036, 1.390208944942409985, -61.02997314496759884 ) ) ;
#16034=CARTESIAN_POINT ( 'NONE',  ( 72.79412820737060485, 1.158194067776799896, -61.92810128176829920 ) ) ;
#16061=CARTESIAN_POINT ( 'NONE',  ( 64.51140068127359939, 1.434916633744939940, -70.06045877469239258 ) ) ;
#16075=CARTESIAN_POINT ( 'NONE',  ( 63.11172336169240538, 1.097085799869280009, -62.44531798733959960 ) ) ;
#16125=CARTESIAN_POINT ( 'NONE',  ( 72.54736496963849390, 1.191618978581419963, -69.67374006097030303 ) ) ;
#16128=PRESENTATION_STYLE_ASSIGNMENT (( #35539 ) ) ;
#16147=DIRECTION ( 'NONE',  ( -1.000000000000000000, 0.000000000000000000, 0.000000000000000000 ) ) ;
#16184=ORIENTED_EDGE ( 'NONE', *, *, #12920, .F. ) ;
#16199=LINE ( 'NONE', #48172, #21467 ) ;
#16215=AXIS2_PLACEMENT_3D ( 'NONE', #4694, #1028, #48730 ) ;
#16223=DIRECTION ( 'NONE',  ( 0.000000000000000000, 0.000000000000000000, 1.000000000000000000 ) ) ;
#16263=CARTESIAN_POINT ( 'NONE',  ( 63.03382193542370260, 0.9209334348186318797, -68.81061689070359932 ) ) ;
#16276=CARTESIAN_POINT ( 'NONE',  ( 71.22645170866519493, 1.102581332775290024, -70.73820378408520071 ) ) ;
#16284=CARTESIAN_POINT ( 'NONE',  ( 71.46564822584178955, 0.9966178393190270324, -60.66877295535580572 ) ) ;
#16286=CARTESIAN_POINT ( 'NONE',  ( 71.79848734841181113, 0.9405967369903619479, -60.89823624368939647 ) ) ;
#16288=CARTESIAN_POINT ( 'NONE',  ( 64.92606658240281092, 0.9214125008369580261, -70.72054727061200197 ) ) ;
#16292=CARTESIAN_POINT ( 'NONE',  ( 72.33393739769915953, 11.38368607098440499, -61.44999999999753015 ) ) ;
#16332=CARTESIAN_POINT ( 'NONE',  ( 63.11571638736320011, 0.9242073871622918935, -62.36095669330580193 ) ) ;
#16334=CARTESIAN_POINT ( 'NONE',  ( 72.33393739769618946, 1.383811055320669947, -68.84999999999999432 ) ) ;
#16339=CARTESIAN_POINT ( 'NONE',  ( 64.68494473060239613, 1.102139304147779830, -60.78391614187979997 ) ) ;
#16344=FACE_OUTER_BOUND ( 'NONE', #7472, .T. ) ;
#16352=ORIENTED_EDGE ( 'NONE', *, *, #50149, .T. ) ;
#16384=PRODUCT_DEFINITION_CONTEXT ( 'detailed design', #16716, 'design' ) ;
#16386=CARTESIAN_POINT ( 'NONE',  ( 72.59802144691040837, 1.334524132314419909, -69.46667700706710491 ) ) ;
#16399=CARTESIAN_POINT ( 'NONE',  ( 64.66082326855099893, 1.024253516290730026, -60.76832953309080665 ) ) ;
#16423=TOROIDAL_SURFACE ( 'NONE', #44784, 5.500000000000000000, 0.5000000000000000000 ) ;
#16479=DIRECTION ( 'NONE',  ( 8.604228440844980354E-13, 0.9739538916850960515, -0.2267461507312888980 ) ) ;
#16510=DIRECTION ( 'NONE',  ( -1.000000000000000000, 0.000000000000000000, 0.000000000000000000 ) ) ;
#16513=DIRECTION ( 'NONE',  ( -1.000000000000000000, 0.000000000000000000, 0.000000000000000000 ) ) ;
#16515=CARTESIAN_POINT ( 'NONE',  ( 63.39147977162330960, 1.370118064600899910, -68.71049874078630637 ) ) ;
#16528=CARTESIAN_POINT ( 'NONE',  ( 71.30079129029560647, 1.267233196669030004, -70.54626486029009413 ) ) ;
#16532=CARTESIAN_POINT ( 'NONE',  ( 63.43393739769620510, 0.8838110553206759423, -62.79342862858290886 ) ) ;
#16537=CARTESIAN_POINT ( 'NONE',  ( 71.42224537953511287, 1.096044978595160035, -60.67935125044880351 ) ) ;
#16539=CARTESIAN_POINT ( 'NONE',  ( 71.69810449264960539, 1.236214136008269904, -60.94130379687539545 ) ) ;
#16542=CARTESIAN_POINT ( 'NONE',  ( 65.27736602627911111, 1.383811055320669947, -70.34999999999999432 ) ) ;
#16569=CARTESIAN_POINT ( 'NONE',  ( 63.66395377270059441, 1.424118951467219896, -69.15359763556290318 ) ) ;
#16583=CARTESIAN_POINT ( 'NONE',  ( 63.03407832914061260, 0.8840451408750739093, -62.48896739026430680 ) ) ;
#16592=CARTESIAN_POINT ( 'NONE',  ( 64.91485532786460055, 1.370853092582090094, -60.97060118797210038 ) ) ;
#16639=CARTESIAN_POINT ( 'NONE',  ( 72.15779067374299416, 1.443559558797639975, -69.80991579785110446 ) ) ;
#16656=CARTESIAN_POINT ( 'NONE',  ( 63.99945660972100825, 1.277726347179370059, -61.38577996275480331 ) ) ;
#16657=ORIENTED_EDGE ( 'NONE', *, *, #32687, .F. ) ;
#16658=DIRECTION ( 'NONE',  ( 0.000000000000000000, 1.000000000000000000, 0.000000000000000000 ) ) ;
#16676=ORIENTED_EDGE ( 'NONE', *, *, #22944, .T. ) ;
#16683=EDGE_CURVE ( 'NONE', #35448, #31343, #39430, .T. ) ;
#16690=CARTESIAN_POINT ( 'NONE',  ( 64.89987712417480736, 0.8859637708054459715, -70.70388507757908769 ) ) ;
#16701=CARTESIAN_POINT ( 'NONE',  ( 63.96720938203739593, 1.277721779380850187, -69.88196296493690340 ) ) ;
#16716=APPLICATION_CONTEXT ( 'automotive_design' ) ;
#16729=AXIS2_PLACEMENT_3D ( 'NONE', #34782, #51306, #15400 ) ;
#16733=B_SPLINE_SURFACE_WITH_KNOTS ( 'NONE', 3, 3, ( 
 ( #37824, #5852, #45430, #17649, #3731, #15523, #50397, #35428, #38864, #51172 ),
 ( #2953, #26782, #43053, #39373, #39119, #14483, #35165, #31475, #19184, #34907 ),
 ( #7665, #34643, #7402, #18669, #50648, #50906, #15265, #31221, #3213, #47248 ),
 ( #47499, #26520, #2696, #11081, #30714, #22589, #30454, #38606, #46477, #10563 ),
 ( #46736, #42537, #6625, #14744, #11597, #30966, #11338, #27556, #10820, #27302 ),
 ( #23608, #42797, #39628, #19703, #6893, #14998, #22843, #18923, #43564, #43310 ),
 ( #23350, #46996, #27049, #7149, #3474, #23101, #19445, #51427, #40135, #48782 ),
 ( #15773, #8171, #44848, #5018, #12889, #36706, #8431, #28845, #7914, #16808 ),
 ( #32238, #28582, #4231, #16537, #20455, #43815, #8953, #40908, #36445, #551 ),
 ( #44067, #40392, #16284, #24895, #35695, #302, #32489, #32757, #12107, #44582 ),
 ( #19948, #39886, #24377, #24115, #28320, #23863, #20716, #51679, #807, #20205 ),
 ( #3985, #36192, #35938, #58, #48517, #48261, #12622, #12355, #24638, #16032 ),
 ( #8686, #40651, #31988, #31727, #47753, #4749, #44321, #4486, #11860, #27815 ),
 ( #48008, #28064, #20980, #6050, #9473, #21750, #45621, #25421, #49310, #13657 ),
 ( #9721, #36979, #5790, #2112, #41682, #5541, #37760, #30132, #5282, #29867 ),
 ( #41170, #21496, #1856, #17834, #25680, #33807, #14164, #18091, #49050, #25164 ) ),
 .UNSPECIFIED., .F., .F., .F.,
 ( 4, 2, 2, 2, 2, 2, 2, 4 ),
 ( 4, 1, 1, 1, 1, 1, 1, 4 ),
 ( -8.599659000000000768E-15, 0.07216186899280199740, 0.1546325764131580016, 0.2061767685508799908, 0.2319488646197410131, 0.2731842183299189597, 0.3391607842662029970, 0.4123535371017689743 ),
 ( 0.000000000000000000, 0.1428571428571430157, 0.2857142857142860315, 0.4285714285714289917, 0.5714285714285709528, 0.7142857142857139685, 0.8571428571428569843, 1.000000000000000000 ),
 .UNSPECIFIED. ) ;
#16734=LINE ( 'NONE', #8879, #44865 ) ;
#16740=DIRECTION ( 'NONE',  ( 0.000000000000000000, 0.000000000000000000, -1.000000000000000000 ) ) ;
#16762=VERTEX_POINT ( 'NONE', #42913 ) ;
#16783=CARTESIAN_POINT ( 'NONE',  ( 63.17541640582520301, 1.096153228089730147, -68.95757157983499042 ) ) ;
#16787=VERTEX_POINT ( 'NONE', #30570 ) ;
#16797=CARTESIAN_POINT ( 'NONE',  ( 71.14534185144368905, 1.334812829108570131, -70.51979614837409827 ) ) ;
#16803=CARTESIAN_POINT ( 'NONE',  ( 72.93015195551900831, 1.326578174762039986, -68.82808305222700085 ) ) ;
#16808=CARTESIAN_POINT ( 'NONE',  ( 71.17189893730710537, 1.387131204727290124, -61.00757424182599920 ) ) ;
#16810=CARTESIAN_POINT ( 'NONE',  ( 71.42517083710241366, 1.394012070863459796, -61.05800084754509527 ) ) ;
#16814=CARTESIAN_POINT ( 'NONE',  ( 64.84324960441189489, 0.8888742037077569380, -70.66714310028379487 ) ) ;
#16841=CARTESIAN_POINT ( 'NONE',  ( 63.57990658082609770, 1.404649297339839897, -68.94572984764299406 ) ) ;
#16844=ORIENTED_EDGE ( 'NONE', *, *, #50658, .T. ) ;
#16856=CARTESIAN_POINT ( 'NONE',  ( 63.37726551317079782, 1.370937308141420230, -62.62705977251020784 ) ) ;
#16866=CARTESIAN_POINT ( 'NONE',  ( 64.69948915615019303, 1.003508719580009867, -60.73835207042080242 ) ) ;
#16897=ORIENTED_EDGE ( 'NONE', *, *, #42232, .T. ) ;
#16898=ORIENTED_EDGE ( 'NONE', *, *, #4012, .F. ) ;
#16915=CARTESIAN_POINT ( 'NONE',  ( 72.38974652088450057, 1.200157260841289819, -69.84239033162910459 ) ) ;
#16925=CARTESIAN_POINT ( 'NONE',  ( 68.13393739769620083, -42.61618894467930119, -71.15000000000000568 ) ) ;
#16929=VERTEX_POINT ( 'NONE', #35810 ) ;
#16931=CARTESIAN_POINT ( 'NONE',  ( 63.97587150976810477, 1.409763019284750118, -61.55987120268989798 ) ) ;
#16939=DIRECTION ( 'NONE',  ( 8.877345525967771201E-15, 1.000000000000000000, 1.071590398323126076E-14 ) ) ;
#16941=EDGE_LOOP ( 'NONE', ( #39866, #5677 ) ) ;
#16975=CARTESIAN_POINT ( 'NONE',  ( 71.69261393255278847, 0.9208623934718319637, -60.81910352240609541 ) ) ;
#16977=CARTESIAN_POINT ( 'NONE',  ( 64.18261223640590174, 1.342504466669670160, -70.01010272223928155 ) ) ;
#17019=CARTESIAN_POINT ( 'NONE',  ( 71.90108049458170569, 1.446932438105679841, -69.97684691838689730 ) ) ;
#17024=CYLINDRICAL_SURFACE ( 'NONE', #35079, 0.4999999999999994449 ) ;
#17061=CARTESIAN_POINT ( 'NONE',  ( 71.17456103962899761, 1.276058558775519991, -70.60879112794539481 ) ) ;
#17068=CARTESIAN_POINT ( 'NONE',  ( 72.76396860142250489, 1.388715606738730068, -68.72506404892941134 ) ) ;
#17072=B_SPLINE_CURVE_WITH_KNOTS ( 'NONE', 3,
 ( #30610, #46632, #22744, #38762, #3115, #2857, #18821, #11237, #30863, #50808, #22999, #51063, #15163, #20106, #20356, #27456 ),
 .UNSPECIFIED., .F., .F.,
 ( 4, 2, 2, 2, 2, 2, 2, 4 ),
 ( -1.891009999999999936E-14, 0.07216186899279498912, 0.1546325764131530334, 0.2061767685508769932, 0.2319488646197389869, 0.2731842183299179605, 0.3391607842662049954, 0.4123535371017730267 ),
 .UNSPECIFIED. ) ;
#17077=CARTESIAN_POINT ( 'NONE',  ( 72.00214641803239601, 1.437400661353670062, -61.36421840665509819 ) ) ;
#17079=CARTESIAN_POINT ( 'NONE',  ( 65.01767771978660448, 0.9212109678634080590, -70.77727272727270247 ) ) ;
#17084=ORIENTED_EDGE ( 'NONE', *, *, #14445, .T. ) ;
#17104=AXIS2_PLACEMENT_3D ( 'NONE', #36187, #44315, #31983 ) ;
#17108=ORIENTED_EDGE ( 'NONE', *, *, #29155, .F. ) ;
#17119=CARTESIAN_POINT ( 'NONE',  ( 63.26014808640670140, 1.265401080857970095, -62.43968814002079881 ) ) ;
#17148=CARTESIAN_POINT ( 'NONE',  ( 64.45847733817470271, 1.439519383694989996, -61.26834731818230040 ) ) ;
#17176=CARTESIAN_POINT ( 'NONE',  ( 72.73876892620509693, 1.391735898526219817, -68.90669866800179477 ) ) ;
#17187=CARTESIAN_POINT ( 'NONE',  ( 64.68898706140620902, 1.405464757956139898, -61.12024232051220451 ) ) ;
#17188=EDGE_LOOP ( 'NONE', ( #20520, #9432, #30402, #36664, #42122, #24520 ) ) ;
#17204=CARTESIAN_POINT ( 'NONE',  ( 63.43393739769620510, 1.383811055320669947, -68.50657137141709541 ) ) ;
#17226=CARTESIAN_POINT ( 'NONE',  ( 72.67981544229699864, 0.9952277120690129486, -61.73279890693489591 ) ) ;
#17228=CARTESIAN_POINT ( 'NONE',  ( 64.42805214825888527, 1.442148388150169991, -70.01405398929449575 ) ) ;
#17257=DIRECTION ( 'NONE',  ( 0.000000000000000000, 1.000000000000000000, 0.000000000000000000 ) ) ;
#17261=ORIENTED_EDGE ( 'NONE', *, *, #40229, .T. ) ;
#17263=EDGE_CURVE ( 'NONE', #35448, #51296, #31926, .T. ) ;
#17270=ORIENTED_EDGE ( 'NONE', *, *, #49976, .T. ) ;
#17272=AXIS2_PLACEMENT_3D ( 'NONE', #3079, #27163, #19824 ) ;
#17276=CARTESIAN_POINT ( 'NONE',  ( 72.70940061843029412, 1.399433130755119992, -68.88399041770809106 ) ) ;
#17302=VECTOR ( 'NONE', #39361, 1000.000000000000000 ) ;
#17318=CARTESIAN_POINT ( 'NONE',  ( 71.28621524259639841, 1.327322800621349996, -70.45801890699070213 ) ) ;
#17326=CARTESIAN_POINT ( 'NONE',  ( 73.07317914023670369, 1.000225705806889964, -69.04426126474540126 ) ) ;
#17329=CARTESIAN_POINT ( 'NONE',  ( 73.22214118178139586, 1.102581332775290024, -62.55748568903110396 ) ) ;
#17333=CARTESIAN_POINT ( 'NONE',  ( 71.92139930889749166, 1.254613999359859955, -61.09530678593939967 ) ) ;
#17335=VERTEX_POINT ( 'NONE', #50199 ) ;
#17336=CARTESIAN_POINT ( 'NONE',  ( 65.05161336175061138, 1.196343736543249880, -70.67573229508370503 ) ) ;
#17373=CARTESIAN_POINT ( 'NONE',  ( 63.49388541862201407, 1.387412027389909985, -62.60488565353588797 ) ) ;
#17384=CARTESIAN_POINT ( 'NONE',  ( 63.47373889294079419, 1.158192848841449907, -69.37188851713681004 ) ) ;
#17429=CARTESIAN_POINT ( 'NONE',  ( 72.62341919120400746, 1.419970371292329947, -69.11014492780159912 ) ) ;
#17442=CARTESIAN_POINT ( 'NONE',  ( 64.14331810339599826, 1.010053820890950194, -61.16840880232479805 ) ) ;
#17457=ORIENTED_EDGE ( 'NONE', *, *, #45482, .F. ) ;
#17471=FACE_OUTER_BOUND ( 'NONE', #11560, .T. ) ;
#17483=CARTESIAN_POINT ( 'NONE',  ( 64.23479494327480666, 1.179519272898400084, -70.17061531731100388 ) ) ;
#17502=DIRECTION ( 'NONE',  ( 0.5193766129849299862, 0.000000000000000000, 0.8545454545454573836 ) ) ;
#17503=CARTESIAN_POINT ( 'NONE',  ( 65.05887334876679517, 1.388715606738730068, -61.01996879627380110 ) ) ;
#17549=CARTESIAN_POINT ( 'NONE',  ( 65.14992021336850314, 1.382840740411490188, -60.95335679887120506 ) ) ;
#17550=VECTOR ( 'NONE', #10413, 1000.000000000000000 ) ;
#17559=CARTESIAN_POINT ( 'NONE',  ( 73.25400818986750551, 0.9960089569207349891, -68.76188247756290650 ) ) ;
#17579=CARTESIAN_POINT ( 'NONE',  ( 72.83620669801349834, 1.369719003397489976, -68.81308079741751271 ) ) ;
#17582=CARTESIAN_POINT ( 'NONE',  ( 73.13559359734860266, 0.8904513541338849869, -62.33586013860640662 ) ) ;
#17588=CARTESIAN_POINT ( 'NONE',  ( 64.95277593799409033, 1.369976237678190101, -70.34495568738229565 ) ) ;
#17615=EDGE_CURVE ( 'NONE', #41914, #27414, #18710, .T. ) ;
#17634=CARTESIAN_POINT ( 'NONE',  ( 63.15779899367210248, 0.9281439705311369526, -62.29764659744859756 ) ) ;
#17645=CARTESIAN_POINT ( 'NONE',  ( 63.61467066632980760, 1.258805424669340089, -69.48497663681300196 ) ) ;
#17649=CARTESIAN_POINT ( 'NONE',  ( 71.22645170866519493, 1.102581332775290024, -60.56179621591489592 ) ) ;
#17667=DIRECTION ( 'NONE',  ( 0.000000000000000000, 1.000000000000000000, 0.000000000000000000 ) ) ;
#17680=ORIENTED_EDGE ( 'NONE', *, *, #45775, .T. ) ;
#17684=CARTESIAN_POINT ( 'NONE',  ( 72.80915813965889072, 1.367045641526529964, -68.91833781196129394 ) ) ;
#17685=CARTESIAN_POINT ( 'NONE',  ( 71.48855272380100701, 0.8936201581567920771, -60.67538646459720297 ) ) ;
#17697=CARTESIAN_POINT ( 'NONE',  ( 64.26020817765768811, 1.338417587229490113, -61.22754019711940288 ) ) ;
#17735=CARTESIAN_POINT ( 'NONE',  ( 63.99083253892909084, 1.458411868502019981, -69.65665569611660146 ) ) ;
#17736=DIRECTION ( 'NONE',  ( 0.000000000000000000, 1.000000000000000000, 0.000000000000000000 ) ) ;
#17745=CARTESIAN_POINT ( 'NONE',  ( 63.20250508406000023, 1.096932441169210071, -69.00001114258428458 ) ) ;
#17761=CARTESIAN_POINT ( 'NONE',  ( 72.80768847295010460, 1.384447124000270035, -68.59133994763901399 ) ) ;
#17780=ORIENTED_EDGE ( 'NONE', *, *, #33050, .F. ) ;
#17801=CARTESIAN_POINT ( 'NONE',  ( 65.13423472332449649, 1.371651820402789879, -60.88469507784019896 ) ) ;
#17806=CARTESIAN_POINT ( 'NONE',  ( 64.93393739756689342, 1.883811055192859962, -68.84999999978390406 ) ) ;
#17811=DIRECTION ( 'NONE',  ( 0.5765530599821100388, 0.1342272854595110421, 0.8059588108975772602 ) ) ;
#17823=CARTESIAN_POINT ( 'NONE',  ( 64.73018593529980080, 0.9325382164350239922, -60.70884169071130287 ) ) ;
#17827=VERTEX_POINT ( 'NONE', #8926 ) ;
#17829=CARTESIAN_POINT ( 'NONE',  ( 72.76779797359338886, 1.388189907116970101, -68.71367622713330547 ) ) ;
#17832=CARTESIAN_POINT ( 'NONE',  ( 73.20393974370449541, 0.8850831926798630178, -62.44126551166660022 ) ) ;
#17834=CARTESIAN_POINT ( 'NONE',  ( 71.58293006479010501, 1.102139304147779830, -60.78391614187979997 ) ) ;
#17839=CARTESIAN_POINT ( 'NONE',  ( 64.82166782235140090, 0.9254905997697669973, -70.65289529397499280 ) ) ;
#17850=ORIENTED_EDGE ( 'NONE', *, *, #26912, .T. ) ;
#17883=CARTESIAN_POINT ( 'NONE',  ( 63.15271035305199376, 0.9966178393190270324, -62.31828917185450223 ) ) ;
#17897=CARTESIAN_POINT ( 'NONE',  ( 72.86285390192669809, 1.309114013480920047, -62.27050734077629812 ) ) ;
#17898=ADVANCED_FACE ( 'NONE', ( #21470 ), #25090, .T. ) ;
#17935=CARTESIAN_POINT ( 'NONE',  ( 73.18782247527531126, 0.8859637708054480809, -62.41593972647859800 ) ) ;
#17937=CARTESIAN_POINT ( 'NONE',  ( 72.87560783889900051, 1.145379646617900038, -69.26025556182580090 ) ) ;
#17939=CARTESIAN_POINT ( 'NONE',  ( 71.83393739770048114, 11.38381105532050164, -69.35000000000411546 ) ) ;
#17942=CARTESIAN_POINT ( 'NONE',  ( 65.02936113742829605, 1.390208944942409985, -70.27002685503249779 ) ) ;
#17950=CIRCLE ( 'NONE', #17104, 1.000000000000001332 ) ;
#17952=CARTESIAN_POINT ( 'NONE',  ( 63.61344205335330315, 1.179532368575769707, -61.75071894376389992 ) ) ;
#17988=CARTESIAN_POINT ( 'NONE',  ( 72.85590616764901029, 0.9486745332815759157, -61.94714277540219882 ) ) ;
#17990=CARTESIAN_POINT ( 'NONE',  ( 64.83129507992209994, 1.367974574076199934, -70.31116820499129005 ) ) ;
#18001=CARTESIAN_POINT ( 'NONE',  ( 63.32918872797849019, 1.327097482837290121, -68.80945595804269033 ) ) ;
#18034=CARTESIAN_POINT ( 'NONE',  ( 63.93393739769709327, 11.38381105532164028, -69.84999999999999432 ) ) ;
#18081=CARTESIAN_POINT ( 'NONE',  ( 64.72587551647490045, 1.099344084866040072, -60.75649936161010345 ) ) ;
#18089=CARTESIAN_POINT ( 'NONE',  ( 72.77398937677050128, 1.387412027389909985, -62.60488565353588797 ) ) ;
#18091=CARTESIAN_POINT ( 'NONE',  ( 71.39251316048110141, 1.372372808637209785, -60.98718532932910819 ) ) ;
#18098=CARTESIAN_POINT ( 'NONE',  ( 65.08882305123219680, 1.387412027389909985, -70.29005197907430613 ) ) ;
#18107=EDGE_LOOP ( 'NONE', ( #19621, #3230, #34619, #7532, #27177, #47636 ) ) ;
#18112=DIRECTION ( 'NONE',  ( 0.000000000000000000, 0.000000000000000000, 1.000000000000000000 ) ) ;
#18152=CARTESIAN_POINT ( 'NONE',  ( 63.31827236005010917, 1.034646415858929913, -69.21578891831741487 ) ) ;
#18157=CARTESIAN_POINT ( 'NONE',  ( 73.01560786460549934, 1.024253516290730026, -62.17688587085479668 ) ) ;
#18162=ORIENTED_EDGE ( 'NONE', *, *, #15618, .F. ) ;
#18170=CARTESIAN_POINT ( 'NONE',  ( 64.63032832047218790, 1.424120032878319897, -61.18002170558170150 ) ) ;
#18189=EDGE_CURVE ( 'NONE', #42080, #13020, #9410, .T. ) ;
#18196=CARTESIAN_POINT ( 'NONE',  ( 72.94809253479790812, 1.136600705753959994, -69.15465073100889981 ) ) ;
#18208=ORIENTED_EDGE ( 'NONE', *, *, #17263, .F. ) ;
#18211=CARTESIAN_POINT ( 'NONE',  ( 63.55532107491779215, 1.170697810385689985, -61.82264208582909504 ) ) ;
#18222=ORIENTED_EDGE ( 'NONE', *, *, #19788, .F. ) ;
#18237=CARTESIAN_POINT ( 'NONE',  ( 64.43393739769619799, 10.88381105532070059, -64.04999999999999716 ) ) ;
#18242=CARTESIAN_POINT ( 'NONE',  ( 64.87665750633441064, 1.391769041008540153, -70.25462587105869261 ) ) ;
#18254=CARTESIAN_POINT ( 'NONE',  ( 63.34300561417320807, 1.326324093417220240, -68.83951043167449768 ) ) ;
#18262=CARTESIAN_POINT ( 'NONE',  ( 71.35858828687760536, 1.188042061556800144, -70.59681938162209747 ) ) ;
#18265=CARTESIAN_POINT ( 'NONE',  ( 73.26121012496899709, 0.8838110553206759423, -68.76625967790960203 ) ) ;
#18270=CARTESIAN_POINT ( 'NONE',  ( 71.40893329644839582, 0.8879664753683499390, -70.67740027405390890 ) ) ;
#18310=CARTESIAN_POINT ( 'NONE',  ( 64.99546124159368787, 0.9209567800143640959, -60.53623002923360730 ) ) ;
#18323=ORIENTED_EDGE ( 'NONE', *, *, #48316, .F. ) ;
#18342=CARTESIAN_POINT ( 'NONE',  ( 73.02275056366489991, 1.266538207494809942, -62.46861950876320435 ) ) ;
#18348=CARTESIAN_POINT ( 'NONE',  ( 65.07026117056300052, 1.388189907116970101, -70.28386057589730740 ) ) ;
#18402=CIRCLE ( 'NONE', #44329, 0.4999999999999982236 ) ;
#18406=CARTESIAN_POINT ( 'NONE',  ( 63.31878016527869590, 0.9618743906590719872, -69.23017199065189686 ) ) ;
#18407=CIRCLE ( 'NONE', #51037, 0.4999999999999935052 ) ;
#18411=CARTESIAN_POINT ( 'NONE',  ( 72.73408845884699758, 1.392490173688170074, -62.38007352545039907 ) ) ;
#18412=CIRCLE ( 'NONE', #10075, 0.5002499999041537526 ) ;
#18430=ORIENTED_EDGE ( 'NONE', *, *, #42489, .T. ) ;
#18436=CARTESIAN_POINT ( 'NONE',  ( 73.11690592692650625, 0.8925687589132609290, -68.99219224778180148 ) ) ;
#18457=FACE_OUTER_BOUND ( 'NONE', #8496, .T. ) ;
#18472=CARTESIAN_POINT ( 'NONE',  ( 63.77381348670360950, 1.342503070345590022, -61.69870111945830615 ) ) ;
#18507=CARTESIAN_POINT ( 'NONE',  ( 64.68616649449130307, 1.374598250659150089, -70.24664079970339969 ) ) ;
#18515=CARTESIAN_POINT ( 'NONE',  ( 71.61827519252990726, 1.134960180547589959, -70.47795848906230276 ) ) ;
#18522=CARTESIAN_POINT ( 'NONE',  ( 63.19978792402569923, 1.187415670095769871, -68.89659930051639947 ) ) ;
#18530=CARTESIAN_POINT ( 'NONE',  ( 71.41482173131041122, 1.096036836948800053, -70.62529907715760658 ) ) ;
#18545=EDGE_LOOP ( 'NONE', ( #40930, #44181, #31379, #48136 ) ) ;
#18548=CARTESIAN_POINT ( 'NONE',  ( 71.65889518049858964, 0.9150552061894319245, -60.79444388203420147 ) ) ;
#18575=CARTESIAN_POINT ( 'NONE',  ( 64.95255690645950608, 1.266538207494809942, -60.76118683403129950 ) ) ;
#18578=CARTESIAN_POINT ( 'NONE',  ( 71.33393739769628894, 10.88381105532070059, -69.34999999999999432 ) ) ;
#18605=CARTESIAN_POINT ( 'NONE',  ( 73.15215840802929392, 0.9242073871622918935, -62.36095669330580193 ) ) ;
#18611=CARTESIAN_POINT ( 'NONE',  ( 64.74712693194939561, 0.8966068345641440285, -70.60278586552529134 ) ) ;
#18615=DIRECTION ( 'NONE',  ( -1.000000000000000000, 0.000000000000000000, 0.000000000000000000 ) ) ;
#18633=CIRCLE ( 'NONE', #32001, 0.5000000000000004441 ) ;
#18669=CARTESIAN_POINT ( 'NONE',  ( 71.26909468036909345, 1.099973129953850215, -60.58645605602389850 ) ) ;
#18672=CARTESIAN_POINT ( 'NONE',  ( 72.66369507718221143, 1.405464757956500055, -62.20504966370589983 ) ) ;
#18684=CARTESIAN_POINT ( 'NONE',  ( 63.50007682179899149, 1.388189907116970101, -68.71367622713330547 ) ) ;
#18693=CARTESIAN_POINT ( 'NONE',  ( 71.83393739769618946, 10.88381105532070059, -67.25000000000000000 ) ) ;
#18694=DIRECTION ( 'NONE',  ( 1.000000000000000000, 0.000000000000000000, 0.000000000000000000 ) ) ;
#18699=ADVANCED_FACE ( 'NONE', ( #3099 ), #41965, .T. ) ;
#18700=DIRECTION ( 'NONE',  ( -1.000000000000000000, 0.000000000000000000, 0.000000000000000000 ) ) ;
#18710=B_SPLINE_CURVE_WITH_KNOTS ( 'NONE', 3,
 ( #13251, #29716, #1441, #1958, #9568, #29200, #45210, #49669, #33393, #42051, #5891, #17935, #13758, #41526, #33651, #21336 ),
 .UNSPECIFIED., .F., .F.,
 ( 4, 2, 2, 2, 2, 2, 2, 4 ),
 ( 6.605827000000000045E-15, 0.07319275283556900269, 0.1391693187718509861, 0.1804046724820269898, 0.2061767685508869852, 0.2577209606886070037, 0.3401916681089580119, 0.4123535371017659767 ),
 .UNSPECIFIED. ) ;
#18720=CIRCLE ( 'NONE', #16215, 0.5000000000000045519 ) ;
#18726=CARTESIAN_POINT ( 'NONE',  ( 63.71017317316999851, 1.107037132887370046, -61.60361627704830312 ) ) ;
#18730=CARTESIAN_POINT ( 'NONE',  ( 73.24087495431770378, 0.9952464559119579279, -68.78371246661670568 ) ) ;
#18761=CARTESIAN_POINT ( 'NONE',  ( 64.65174547131330485, 1.408734182879959995, -70.16322028441409486 ) ) ;
#18770=CARTESIAN_POINT ( 'NONE',  ( 71.57888773397908722, 1.405464757955549926, -70.17975767949100430 ) ) ;
#18783=ORIENTED_EDGE ( 'NONE', *, *, #22457, .T. ) ;
#18810=EDGE_LOOP ( 'NONE', ( #24644, #37099, #18865, #50137 ) ) ;
#18818=DIRECTION ( 'NONE',  ( 1.000000000000000000, 0.000000000000000000, 0.000000000000000000 ) ) ;
#18821=CARTESIAN_POINT ( 'NONE',  ( 71.15040120820690106, 1.386342629514219826, -70.29952392096339508 ) ) ;
#18827=CARTESIAN_POINT ( 'NONE',  ( 65.08882305123219680, 1.387412027389909985, -61.00994802092580471 ) ) ;
#18830=DIRECTION ( 'NONE',  ( 0.8059588108975762610, 0.1342272854594990239, 0.5765530599821140356 ) ) ;
#18859=CARTESIAN_POINT ( 'NONE',  ( 72.98101631171969927, 1.187931651339009909, -62.25809267083580778 ) ) ;
#18865=ORIENTED_EDGE ( 'NONE', *, *, #39305, .T. ) ;
#18871=FACE_OUTER_BOUND ( 'NONE', #29741, .T. ) ;
#18876=ORIENTED_EDGE ( 'NONE', *, *, #16683, .F. ) ;
#18884=COLOUR_RGB ( '', 0.66274510, 0.83137255, 0.94901961) ;
#18885=CARTESIAN_POINT ( 'NONE',  ( 68.13393739769620083, 0.8838110553206759423, -65.65000000000000568 ) ) ;
#18898=AXIS2_PLACEMENT_3D ( 'NONE', #24811, #36889, #36615 ) ;
#18922=LINE ( 'NONE', #37822, #21550 ) ;
#18923=CARTESIAN_POINT ( 'NONE',  ( 71.19443613848248731, 1.370118064600899910, -60.90754237392700077 ) ) ;
#18925=CARTESIAN_POINT ( 'NONE',  ( 73.01685589897030582, 0.9479899806831150189, -62.16329186921600325 ) ) ;
#18932=ORIENTED_EDGE ( 'NONE', *, *, #41775, .F. ) ;
#18941=DIRECTION ( 'NONE',  ( 0.000000000000000000, -1.000000000000000000, 0.000000000000000000 ) ) ;
#18975=DIRECTION ( 'NONE',  ( 0.000000000000000000, 0.000000000000000000, -1.000000000000000000 ) ) ;
#18983=CARTESIAN_POINT ( 'NONE',  ( 63.51813308628860710, 1.318402576461300102, -62.06494149197789767 ) ) ;
#18987=CARTESIAN_POINT ( 'NONE',  ( 72.95819590288708412, 1.328674444234379859, -68.76626720283900340 ) ) ;
#19009=ORIENTED_EDGE ( 'NONE', *, *, #22944, .F. ) ;
#19013=AXIS2_PLACEMENT_3D ( 'NONE', #32797, #36230, #32024 ) ;
#19025=CARTESIAN_POINT ( 'NONE',  ( 71.69973440771281048, 1.034647430439950000, -70.46565918721690025 ) ) ;
#19041=CARTESIAN_POINT ( 'NONE',  ( 71.38053669821270830, 1.187415670095769871, -70.58414947367050729 ) ) ;
#19047=LINE ( 'NONE', #3594, #44876 ) ;
#19049=CARTESIAN_POINT ( 'NONE',  ( 71.58179376171669617, 0.9036513197889539661, -70.56049771322810216 ) ) ;
#19062=ORIENTED_EDGE ( 'NONE', *, *, #31618, .T. ) ;
#19072=CARTESIAN_POINT ( 'NONE',  ( 63.19468704395289649, 0.8986939045430389905, -69.05651959838648679 ) ) ;
#19088=CARTESIAN_POINT ( 'NONE',  ( 64.81454860220658531, 1.096305581841150012, -60.69897858480909747 ) ) ;
#19097=CARTESIAN_POINT ( 'NONE',  ( 72.71656993463119534, 0.9860880133275228276, -69.52393415259180642 ) ) ;
#19120=CARTESIAN_POINT ( 'NONE',  ( 73.04666255914109740, 0.9369374701296400154, -62.20531809130540069 ) ) ;
#19123=DIRECTION ( 'NONE',  ( 0.000000000000000000, 1.000000000000000000, 0.000000000000000000 ) ) ;
#19126=CIRCLE ( 'NONE', #48420, 5.500000000000005329 ) ;
#19147=VERTEX_POINT ( 'NONE', #41732 ) ;
#19172=LINE ( 'NONE', #26508, #20978 ) ;
#19182=CARTESIAN_POINT ( 'NONE',  ( 65.13393739769620083, 1.383811055320669947, -65.65000000000000568 ) ) ;
#19184=CARTESIAN_POINT ( 'NONE',  ( 71.03049636386479904, 1.383411777981069957, -60.92458877361669778 ) ) ;
#19186=CARTESIAN_POINT ( 'NONE',  ( 72.31167251984919631, 1.116860450401449878, -61.34995363534049773 ) ) ;
#19199=AXIS2_PLACEMENT_3D ( 'NONE', #11682, #19279, #27649 ) ;
#19212=CARTESIAN_POINT ( 'NONE',  ( 63.13228119804391270, 0.8904513541338849869, -62.33586013860640662 ) ) ;
#19232=CIRCLE ( 'NONE', #16729, 0.4999999999999935052 ) ;
#19233=CARTESIAN_POINT ( 'NONE',  ( 63.04573361361109818, 1.102581332775290024, -62.55748568903120344 ) ) ;
#19245=CARTESIAN_POINT ( 'NONE',  ( 63.47253245025149937, 1.367958924391579956, -62.34793560868030227 ) ) ;
#19249=CARTESIAN_POINT ( 'NONE',  ( 73.01236646462280078, 1.336371993404959824, -68.64083569922701145 ) ) ;
#19279=DIRECTION ( 'NONE',  ( 0.000000000000000000, 1.000000000000000000, 0.000000000000000000 ) ) ;
#19289=CARTESIAN_POINT ( 'NONE',  ( 71.85583611592080899, 1.158194067775949909, -70.31019080967980983 ) ) ;
#19293=SURFACE_STYLE_FILL_AREA ( #19546 ) ;
#19325=CARTESIAN_POINT ( 'NONE',  ( 71.40227520965750330, 1.367045641526529964, -60.97477925803730159 ) ) ;
#19335=LINE ( 'NONE', #35581, #42704 ) ;
#19348=ORIENTED_EDGE ( 'NONE', *, *, #47152, .T. ) ;
#19350=CARTESIAN_POINT ( 'NONE',  ( 64.85894149894409111, 0.8879664753683469414, -60.62259972594610247 ) ) ;
#19380=CARTESIAN_POINT ( 'NONE',  ( 72.75389709491450674, 1.389468113695450091, -62.45014271800210537 ) ) ;
#19398=DIRECTION ( 'NONE',  ( 1.000000000000000000, 0.000000000000000000, 0.000000000000000000 ) ) ;
#19426=CARTESIAN_POINT ( 'NONE',  ( 63.09706677394889596, 1.198183261254770038, -68.71131498411249083 ) ) ;
#19427=CARTESIAN_POINT ( 'NONE',  ( 68.13393739769630031, 1.883811055320669947, -70.34999999999999432 ) ) ;
#19431=ADVANCED_FACE ( 'NONE', ( #50634 ), #30701, .F. ) ;
#19445=CARTESIAN_POINT ( 'NONE',  ( 71.26464087954850868, 1.328073773609220076, -60.83220757462540007 ) ) ;
#19447=CARTESIAN_POINT ( 'NONE',  ( 72.80625431757680133, 1.063298638255719908, -61.89539269462630244 ) ) ;
#19450=VERTEX_POINT ( 'NONE', #22574 ) ;
#19491=CARTESIAN_POINT ( 'NONE',  ( 63.40197747243239945, 1.383811055320669947, -62.77400398868049081 ) ) ;
#19494=DIRECTION ( 'NONE',  ( 0.000000000000000000, -0.7071067811865162644, -0.7071067811865786590 ) ) ;
#19509=CARTESIAN_POINT ( 'NONE',  ( 72.97487308438059017, 1.330484379554840002, -68.72860478453370092 ) ) ;
#19510=CARTESIAN_POINT ( 'NONE',  ( 73.24758132965840218, 0.8838110553206759423, -62.51131646858519275 ) ) ;
#19541=CIRCLE ( 'NONE', #9502, 5.499999999999998224 ) ;
#19543=FACE_OUTER_BOUND ( 'NONE', #48788, .T. ) ;
#19546=FILL_AREA_STYLE ('',( #27915 ) ) ;
#19562=CARTESIAN_POINT ( 'NONE',  ( 71.37283554222209148, 1.371509258145880095, -70.32114135108689368 ) ) ;
#19588=DIRECTION ( 'NONE',  ( 0.8133188816852265912, 0.000000000000000000, 0.5818181818182487364 ) ) ;
#19607=CARTESIAN_POINT ( 'NONE',  ( 65.05904174327510248, 1.369885150286779929, -60.91305399111080021 ) ) ;
#19621=ORIENTED_EDGE ( 'NONE', *, *, #2313, .T. ) ;
#19636=ORIENTED_EDGE ( 'NONE', *, *, #2822, .T. ) ;
#19639=CARTESIAN_POINT ( 'NONE',  ( 73.07317914023670369, 1.000225705806889964, -62.25573873525459589 ) ) ;
#19644=CARTESIAN_POINT ( 'NONE',  ( 64.76223432283450165, 1.187296498006430001, -70.50955232519169158 ) ) ;
#19659=CARTESIAN_POINT ( 'NONE',  ( 68.13393739769620083, 0.8838110553206759423, -65.65000000000000568 ) ) ;
#19677=CARTESIAN_POINT ( 'NONE',  ( 63.36863247553639411, 1.371651820402789879, -68.64970267437179530 ) ) ;
#19703=CARTESIAN_POINT ( 'NONE',  ( 71.37757697660960332, 1.096291039689149871, -60.65158056017160249 ) ) ;
#19705=CARTESIAN_POINT ( 'NONE',  ( 72.61824171362239611, 1.332297898505919953, -61.86173543814949483 ) ) ;
#19717=ORIENTED_EDGE ( 'NONE', *, *, #22457, .F. ) ;
#19747=CARTESIAN_POINT ( 'NONE',  ( 63.18711801607420142, 1.188042061556800144, -62.42534911081870064 ) ) ;
#19765=CARTESIAN_POINT ( 'NONE',  ( 72.87088340658550578, 1.369885150286800135, -68.72489565442110404 ) ) ;
#19788=EDGE_CURVE ( 'NONE', #13020, #11637, #32027, .T. ) ;
#19802=CARTESIAN_POINT ( 'NONE',  ( 72.44676906758759571, 1.345243094457279964, -69.65815164399170101 ) ) ;
#19805=SURFACE_SIDE_STYLE ('',( #19293 ) ) ;
#19816=CARTESIAN_POINT ( 'NONE',  ( 64.69709925250680271, 1.229987811083060212, -60.86278414758729838 ) ) ;
#19824=DIRECTION ( 'NONE',  ( 0.000000000000000000, 0.000000000000000000, -1.000000000000000000 ) ) ;
#19887=CARTESIAN_POINT ( 'NONE',  ( 72.99790115655470402, 1.264791438333819906, -62.42094564213650187 ) ) ;
#19905=CARTESIAN_POINT ( 'NONE',  ( 68.13393739769620083, -42.11618894467930119, -60.14999999999999858 ) ) ;
#19926=CARTESIAN_POINT ( 'NONE',  ( 63.10820510261260097, 1.196343736543249880, -68.73232403594570883 ) ) ;
#19948=CARTESIAN_POINT ( 'NONE',  ( 71.48855272380100701, 0.8936201581567889685, -60.67538646459720297 ) ) ;
#19950=CARTESIAN_POINT ( 'NONE',  ( 72.06219320706279063, 1.440335647928530083, -61.41002653287189617 ) ) ;
#19954=FACE_OUTER_BOUND ( 'NONE', #36488, .T. ) ;
#19960=CARTESIAN_POINT ( 'NONE',  ( 72.18749078828946608, 11.23736444591397543, -67.25000000000000000 ) ) ;
#19990=CARTESIAN_POINT ( 'NONE',  ( 63.43729419656740731, 1.382840740411490188, -62.66598281567230089 ) ) ;
#20000=B_SPLINE_CURVE_WITH_KNOTS ( 'NONE', 3,
 ( #51222, #31786, #7452, #7718, #7195, #15575, #22895, #27865, #39167, #39425, #43359, #7963, #43865, #35744, #47301, #31269, #27353, #39677, #31531, #51727 ),
 .UNSPECIFIED., .F., .F.,
 ( 4, 2, 2, 2, 2, 2, 2, 2, 2, 4 ),
 ( -1.826192301619919967, -1.710015269418689865, -1.458000257329579830, -1.209852399823200031, -1.027233169661210033, -0.9130961508099619817, -0.6848221131074718748, -0.4130753771390969220, -0.1614840352205790808, 0.000000000000000000 ),
 .UNSPECIFIED. ) ;
#20002=AXIS2_PLACEMENT_3D ( 'NONE', #36722, #21249, #44864 ) ;
#20004=ORIENTED_EDGE ( 'NONE', *, *, #4012, .T. ) ;
#20008=AXIS2_PLACEMENT_3D ( 'NONE', #31268, #15315, #19494 ) ;
#20047=CARTESIAN_POINT ( 'NONE',  ( 72.12133632587820387, 1.039769764133249952, -70.13448369263871029 ) ) ;
#20056=CARTESIAN_POINT ( 'NONE',  ( 64.07670260090860381, 1.019777262794749895, -70.07076857027371375 ) ) ;
#20063=CARTESIAN_POINT ( 'NONE',  ( 71.58938403497960223, 1.005545696829380109, -70.54702908378739323 ) ) ;
#20073=CARTESIAN_POINT ( 'NONE',  ( 71.33393739769628894, 1.383811055320669947, -68.84999999999999432 ) ) ;
#20099=ADVANCED_FACE ( 'NONE', ( #32360 ), #26213, .T. ) ;
#20106=CARTESIAN_POINT ( 'NONE',  ( 71.29447239804829906, 1.393731187554809958, -70.25064478522961053 ) ) ;
#20148=ORIENTED_EDGE ( 'NONE', *, *, #50658, .F. ) ;
#20154=CARTESIAN_POINT ( 'NONE',  ( 63.54731047306190561, 1.396834109478129804, -62.44999999999999574 ) ) ;
#20158=ORIENTED_EDGE ( 'NONE', *, *, #21292, .T. ) ;
#20181=CARTESIAN_POINT ( 'NONE',  ( 63.35267264707980672, 1.373356196620459935, -68.60593141770759473 ) ) ;
#20194=CARTESIAN_POINT ( 'NONE',  ( 71.00993340901570150, 1.383811055320669947, -70.38195992526379996 ) ) ;
#20205=CARTESIAN_POINT ( 'NONE',  ( 71.20900144662560649, 1.388715606738720076, -61.01996879627380110 ) ) ;
#20207=CARTESIAN_POINT ( 'NONE',  ( 72.04429487089811346, 1.454949836291180132, -61.42720652002459758 ) ) ;
#20209=CARTESIAN_POINT ( 'NONE',  ( 65.21909306016200958, 1.375383258925270136, -70.44587820682191648 ) ) ;
#20234=CARTESIAN_POINT ( 'NONE',  ( 64.42805214825888527, 1.442148388150169991, -70.01405398929449575 ) ) ;
#20247=CARTESIAN_POINT ( 'NONE',  ( 63.26414124932220062, 1.334812829108570131, -62.63859554625260273 ) ) ;
#20248=CARTESIAN_POINT ( 'NONE',  ( 68.13393739769620083, 0.8838110553206759423, -59.64999999999999858 ) ) ;
#20252=DIRECTION ( 'NONE',  ( 0.000000000000000000, 0.000000000000000000, -1.000000000000000000 ) ) ;
#20256=CARTESIAN_POINT ( 'NONE',  ( 64.72196861157989645, 1.188860127980290171, -60.81548205241750082 ) ) ;
#20269=ORIENTED_EDGE ( 'NONE', *, *, #33185, .F. ) ;
#20283=CARTESIAN_POINT ( 'NONE',  ( 72.72056432233058842, 1.396834109478129804, -62.44999999999999574 ) ) ;
#20290=AXIS2_PLACEMENT_3D ( 'NONE', #45899, #9986, #35039 ) ;
#20292=AXIS2_PLACEMENT_3D ( 'NONE', #37513, #33572, #26219 ) ;
#20300=CARTESIAN_POINT ( 'NONE',  ( 72.49406130868889875, 1.342503070345580030, -69.60129888054170522 ) ) ;
#20314=CARTESIAN_POINT ( 'NONE',  ( 64.61436174452420289, 1.028860820851879909, -60.80092091627260231 ) ) ;
#20315=CARTESIAN_POINT ( 'NONE',  ( 71.52819866244169589, 1.000225705806889964, -70.58924174254049433 ) ) ;
#20347=CARTESIAN_POINT ( 'NONE',  ( 64.66447934098378880, 0.9065823421260920112, -70.54525856488091051 ) ) ;
#20356=CARTESIAN_POINT ( 'NONE',  ( 71.31427394968270050, 1.395196698723390138, -70.24366017557039754 ) ) ;
#20406=ORIENTED_EDGE ( 'NONE', *, *, #42114, .F. ) ;
#20408=CARTESIAN_POINT ( 'NONE',  ( 66.53393739769619231, 10.88381105532070059, -69.34999999999999432 ) ) ;
#20409=CARTESIAN_POINT ( 'NONE',  ( 68.13393739769630031, 1.883811055320669947, -70.34999999999999432 ) ) ;
#20410=DIRECTION ( 'NONE',  ( 0.000000000000000000, 1.000000000000000000, 0.000000000000000000 ) ) ;
#20424=CARTESIAN_POINT ( 'NONE',  ( 71.01106396815980304, 1.383811055320669947, -60.95624653118409242 ) ) ;
#20435=CARTESIAN_POINT ( 'NONE',  ( 63.26414124932220062, 1.334812829108570131, -68.66140445374750811 ) ) ;
#20447=CARTESIAN_POINT ( 'NONE',  ( 71.13364007206789097, 1.371651820402789879, -70.41530492215990478 ) ) ;
#20455=CARTESIAN_POINT ( 'NONE',  ( 71.38783905025799470, 1.187237555532410171, -60.72008782705600538 ) ) ;
#20457=CARTESIAN_POINT ( 'NONE',  ( 72.07170057178599620, 1.030858001320090089, -61.12206023519150477 ) ) ;
#20459=CARTESIAN_POINT ( 'NONE',  ( 64.92397392854900318, 1.188582381068110205, -70.60520998597918663 ) ) ;
#20462=CIRCLE ( 'NONE', #50643, 6.000000000000005329 ) ;
#20466=ORIENTED_EDGE ( 'NONE', *, *, #29963, .F. ) ;
#20483=B_SPLINE_CURVE_WITH_KNOTS ( 'NONE', 3,
 ( #50920, #46230, #27061, #26280, #38351, #6641, #22347, #30728, #14244, #18684, #10835, #24067, #34658, #50664, #14759, #3938 ),
 .UNSPECIFIED., .F., .F.,
 ( 4, 2, 2, 2, 2, 2, 2, 4 ),
 ( -8.880243999999999390E-15, 0.07216186899280199740, 0.1546325764131560032, 0.2061767685508779924, 0.2319488646197390147, 0.2731842183299159621, 0.3391607842661999994, 0.4123535371017650331 ),
 .UNSPECIFIED. ) ;
#20501=CARTESIAN_POINT ( 'NONE',  ( 63.15706468848460275, 1.190292248953970011, -62.47835652209879953 ) ) ;
#20507=CARTESIAN_POINT ( 'NONE',  ( 72.70504696988909643, 1.400446703427080219, -62.40275391609110756 ) ) ;
#20510=CARTESIAN_POINT ( 'NONE',  ( 64.97340239734420209, 1.393731187554809958, -61.04935521477050031 ) ) ;
#20520=ORIENTED_EDGE ( 'NONE', *, *, #2718, .T. ) ;
#20522=ORIENTED_EDGE ( 'NONE', *, *, #43940, .F. ) ;
#20539=ORIENTED_EDGE ( 'NONE', *, *, #39154, .T. ) ;
#20555=CARTESIAN_POINT ( 'NONE',  ( 72.36538891291519349, 1.347758125946150187, -69.74822197408450108 ) ) ;
#20561=EDGE_CURVE ( 'NONE', #2182, #48970, #10336, .T. ) ;
#20571=CARTESIAN_POINT ( 'NONE',  ( 64.14956774380819127, 1.407740700961959801, -61.39510741658510540 ) ) ;
#20597=DIRECTION ( 'NONE',  ( 0.000000000000000000, 0.000000000000000000, 1.000000000000000000 ) ) ;
#20602=CARTESIAN_POINT ( 'NONE',  ( 64.85894149894419058, 0.8879664753683389478, -70.67740027405400838 ) ) ;
#20607=DIRECTION ( 'NONE',  ( 0.000000000000000000, 1.000000000000000000, 0.000000000000000000 ) ) ;
#20615=EDGE_CURVE ( 'NONE', #9229, #23989, #36300, .T. ) ;
#20616=CARTESIAN_POINT ( 'NONE',  ( 64.07626989212400304, 1.443555451352130037, -69.77608189653500403 ) ) ;
#20641=CARTESIAN_POINT ( 'NONE',  ( 64.93393739769599904, 1.396834109478129804, -61.06337307536569625 ) ) ;
#20646=CARTESIAN_POINT ( 'NONE',  ( 70.99050876911339003, 1.383811055320669947, -70.34999999999999432 ) ) ;
#20651=ORIENTED_EDGE ( 'NONE', *, *, #38931, .T. ) ;
#20654=CARTESIAN_POINT ( 'NONE',  ( 73.01625195241490474, 1.007912009470880221, -62.17370354086050099 ) ) ;
#20667=DIRECTION ( 'NONE',  ( 0.000000000000000000, 0.7071067811865492381, -0.7071067811865457964 ) ) ;
#20690=CARTESIAN_POINT ( 'NONE',  ( 63.13973003289760300, 0.9958340104639701318, -68.96201750760249638 ) ) ;
#20704=CARTESIAN_POINT ( 'NONE',  ( 71.19526263826620038, 1.274277262446069869, -70.59881390902160092 ) ) ;
#20710=CARTESIAN_POINT ( 'NONE',  ( 73.08848314165430793, 0.9307121176571799825, -69.03423516236559010 ) ) ;
#20713=CARTESIAN_POINT ( 'NONE',  ( 73.26121012496899709, 0.8838110553206759423, -62.53374032209040223 ) ) ;
#20716=CARTESIAN_POINT ( 'NONE',  ( 71.32344782937069283, 1.326324093417210248, -60.85906821647699871 ) ) ;
#20717=CYLINDRICAL_SURFACE ( 'NONE', #7432, 0.4999999999999994449 ) ;
#20718=CARTESIAN_POINT ( 'NONE',  ( 72.00787155028980635, 0.9860880133278678850, -61.06736746306660280 ) ) ;
#20719=AXIS2_PLACEMENT_3D ( 'NONE', #38940, #51751, #11934 ) ;
#20722=CARTESIAN_POINT ( 'NONE',  ( 64.93204900141920177, 0.9940695285616559795, -70.71491496446259362 ) ) ;
#20764=CARTESIAN_POINT ( 'NONE',  ( 63.10653712364238999, 0.8879664753683469414, -62.37500410124779648 ) ) ;
#20771=DIRECTION ( 'NONE',  ( 1.000000000000000000, 0.000000000000000000, 0.000000000000000000 ) ) ;
#20772=CARTESIAN_POINT ( 'NONE',  ( 64.84535060374940940, 1.263738073398970041, -60.81786852648419028 ) ) ;
#20803=VERTEX_POINT ( 'NONE', #24224 ) ;
#20819=CARTESIAN_POINT ( 'NONE',  ( 72.40645806407979990, 1.061268603384970088, -69.86275902853338948 ) ) ;
#20833=CARTESIAN_POINT ( 'NONE',  ( 63.94990637464889716, 1.033013263524900083, -61.34874638836240024 ) ) ;
#20882=CARTESIAN_POINT ( 'NONE',  ( 63.95121251289828734, 1.060191874549210045, -69.95192703337309581 ) ) ;
#20885=ORIENTED_EDGE ( 'NONE', *, *, #35907, .F. ) ;
#20903=CARTESIAN_POINT ( 'NONE',  ( 65.11747358718548639, 1.386342629514219826, -61.00047607903670155 ) ) ;
#20920=DIRECTION ( 'NONE',  ( 1.000000000000000000, 0.000000000000000000, 0.000000000000000000 ) ) ;
#20940=AXIS2_PLACEMENT_3D ( 'NONE', #26546, #22357, #18694 ) ;
#20956=CARTESIAN_POINT ( 'NONE',  ( 63.15096886846589541, 0.8925687589132640376, -68.99219224778180148 ) ) ;
#20959=ORIENTED_EDGE ( 'NONE', *, *, #47696, .T. ) ;
#20967=CARTESIAN_POINT ( 'NONE',  ( 71.16987874477759135, 1.383357884654609959, -70.32891903079600127 ) ) ;
#20975=CARTESIAN_POINT ( 'NONE',  ( 73.04666255914109740, 0.9369374701296400154, -69.09468190869459647 ) ) ;
#20977=CARTESIAN_POINT ( 'NONE',  ( 72.82137280411760116, 1.383928098097870096, -62.75238677440889035 ) ) ;
#20978=VECTOR ( 'NONE', #30952, 1000.000000000000000 ) ;
#20980=CARTESIAN_POINT ( 'NONE',  ( 71.56838563924230812, 1.003508719580009867, -60.73835207042080242 ) ) ;
#20983=CARTESIAN_POINT ( 'NONE',  ( 72.18032112064790340, 1.107037132887370046, -61.22623577547380336 ) ) ;
#20987=CARTESIAN_POINT ( 'NONE',  ( 64.87536617802101091, 1.096110717717199812, -70.63920630446280313 ) ) ;
#21020=DIRECTION ( 'NONE',  ( -1.000000000000000000, 0.000000000000000000, 0.000000000000000000 ) ) ;
#21026=CARTESIAN_POINT ( 'NONE',  ( 63.52011431889719972, 1.391252479931859964, -62.52735703481241103 ) ) ;
#21037=CARTESIAN_POINT ( 'NONE',  ( 68.13393739769620083, 0.8838110553206759423, -65.65000000000000568 ) ) ;
#21060=EDGE_LOOP ( 'NONE', ( #5287, #46698, #43179, #51347 ) ) ;
#21080=CARTESIAN_POINT ( 'NONE',  ( 72.88570115400611371, 0.9405967369906069742, -69.31454995071659653 ) ) ;
#21095=CARTESIAN_POINT ( 'NONE',  ( 64.02475525337911222, 1.458407608744489936, -61.60944193589799767 ) ) ;
#21117=VERTEX_POINT ( 'NONE', #47494 ) ;
#21124=CARTESIAN_POINT ( 'NONE',  ( 64.43393739769619799, 10.88381105532070059, -62.44999999999999574 ) ) ;
#21135=CARTESIAN_POINT ( 'NONE',  ( 71.65889518049858964, 0.9150552061894319245, -60.79444388203420147 ) ) ;
#21137=CARTESIAN_POINT ( 'NONE',  ( 64.07915002758259959, 1.048864949068049945, -70.07302479646419613 ) ) ;
#21144=DIRECTION ( 'NONE',  ( 0.000000000000000000, 0.000000000000000000, -1.000000000000000000 ) ) ;
#21148=PLANE ( 'NONE',  #18898 ) ;
#21203=CARTESIAN_POINT ( 'NONE',  ( 65.25681082723269810, 1.383811055320669947, -60.95624653118409242 ) ) ;
#21210=FACE_OUTER_BOUND ( 'NONE', #27996, .T. ) ;
#21221=CARTESIAN_POINT ( 'NONE',  ( 71.27241355379879906, 0.9209567800143640959, -70.76376997076650355 ) ) ;
#21227=EDGE_CURVE ( 'NONE', #29784, #23138, #13773, .T. ) ;
#21228=CARTESIAN_POINT ( 'NONE',  ( 72.88423911510749065, 1.325841671674440114, -68.92527065596381419 ) ) ;
#21235=CARTESIAN_POINT ( 'NONE',  ( 71.59408232549860429, 1.419970371292400113, -61.16051820649249748 ) ) ;
#21238=CARTESIAN_POINT ( 'NONE',  ( 64.97332050699269246, 0.9209334348186318797, -70.75011546227260339 ) ) ;
#21241=EDGE_CURVE ( 'NONE', #41111, #23933, #17950, .T. ) ;
#21249=DIRECTION ( 'NONE',  ( -1.930570877714250223E-11, -1.000000000000000000, 6.141198660767589922E-12 ) ) ;
#21251=FACE_OUTER_BOUND ( 'NONE', #37446, .T. ) ;
#21282=CARTESIAN_POINT ( 'NONE',  ( 63.17541640582520301, 1.096153228089719933, -62.34242842016509201 ) ) ;
#21287=CARTESIAN_POINT ( 'NONE',  ( 72.83393739769620367, 1.883811055320669947, -68.84999999999999432 ) ) ;
#21292=EDGE_CURVE ( 'NONE', #24662, #26724, #48080, .T. ) ;
#21293=CARTESIAN_POINT ( 'NONE',  ( 63.37498668061930829, 1.231980177647109986, -69.13347842061430981 ) ) ;
#21311=AXIS2_PLACEMENT_3D ( 'NONE', #21037, #24696, #33084 ) ;
#21314=EDGE_LOOP ( 'NONE', ( #17780, #3739, #17270, #17084 ) ) ;
#21321=CARTESIAN_POINT ( 'NONE',  ( 72.77398937677050128, 1.387412027389909985, -62.60488565353588797 ) ) ;
#21325=CIRCLE ( 'NONE', #14645, 5.999999999999998224 ) ;
#21336=CARTESIAN_POINT ( 'NONE',  ( 73.26121012496899709, 0.8838110553206759423, -62.53374032209040223 ) ) ;
#21338=CARTESIAN_POINT ( 'NONE',  ( 72.83400132021240836, 0.9897451961558710876, -69.38063463722799895 ) ) ;
#21351=CARTESIAN_POINT ( 'NONE',  ( 64.63032832047218790, 1.424120032878319897, -61.18002170558170150 ) ) ;
#21380=CARTESIAN_POINT ( 'NONE',  ( 63.43393739769620510, 1.883811055320669947, -65.65000000000000568 ) ) ;
#21389=CARTESIAN_POINT ( 'NONE',  ( 72.07540109225739400, 1.000506532484820132, -61.12530190143370135 ) ) ;
#21392=CARTESIAN_POINT ( 'NONE',  ( 63.97401018632380243, 1.443559287490330023, -69.67384056315309238 ) ) ;
#21449=FACE_OUTER_BOUND ( 'NONE', #3157, .T. ) ;
#21464=CARTESIAN_POINT ( 'NONE',  ( 65.12253294394879788, 1.334812829108570131, -60.78020385162600547 ) ) ;
#21467=VECTOR ( 'NONE', #43729, 1000.000000000000000 ) ;
#21470=FACE_OUTER_BOUND ( 'NONE', #9668, .T. ) ;
#21491=CARTESIAN_POINT ( 'NONE',  ( 73.07318775143950518, 0.8986939045430379913, -69.05651959838648679 ) ) ;
#21494=CARTESIAN_POINT ( 'NONE',  ( 73.18852689059310990, 0.9219904752505979628, -62.41704322431660046 ) ) ;
#21496=CARTESIAN_POINT ( 'NONE',  ( 71.62124566564099837, 0.9425424353906030062, -60.76751081460630388 ) ) ;
#21498=CARTESIAN_POINT ( 'NONE',  ( 71.58063725038380198, 1.374525224580329885, -61.05282258189939881 ) ) ;
#21500=CARTESIAN_POINT ( 'NONE',  ( 64.89668540611309311, 1.325715844996850024, -70.41854262496009653 ) ) ;
#21516=AXIS2_PLACEMENT_3D ( 'NONE', #12048, #16740, #4167 ) ;
#21542=CARTESIAN_POINT ( 'NONE',  ( 63.26997363883779713, 1.264791438333809914, -62.42094564213650187 ) ) ;
#21550=VECTOR ( 'NONE', #22842, 1000.000000000000000 ) ;
#21552=CARTESIAN_POINT ( 'NONE',  ( 63.41196002899340556, 0.9486721756287949114, -69.35284629089670716 ) ) ;
#21591=CARTESIAN_POINT ( 'NONE',  ( 72.79534234514369473, 1.367958924391410092, -68.95206439131310105 ) ) ;
#21594=CARTESIAN_POINT ( 'NONE',  ( 71.33393739770049535, 11.38381105532070059, -69.34999999999999432 ) ) ;
#21601=DIRECTION ( 'NONE',  ( 0.000000000000000000, 0.000000000000000000, 1.000000000000000000 ) ) ;
#21604=CARTESIAN_POINT ( 'NONE',  ( 64.60333993882289860, 1.138495779907959804, -60.85329768958769847 ) ) ;
#21628=LINE ( 'NONE', #49959, #43665 ) ;
#21633=CARTESIAN_POINT ( 'NONE',  ( 63.93393739769619089, 1.883811055320669947, -68.84999999999999432 ) ) ;
#21643=CARTESIAN_POINT ( 'NONE',  ( 63.90184877270480257, 1.348268598598709955, -69.74930279100139785 ) ) ;
#21663=AXIS2_PLACEMENT_3D ( 'NONE', #18885, #23568, #34866 ) ;
#21675=EDGE_LOOP ( 'NONE', ( #20406, #20959, #18222, #40587 ) ) ;
#21684=CIRCLE ( 'NONE', #6678, 0.5000000000000000000 ) ;
#21698=DIRECTION ( 'NONE',  ( 1.000000000000000000, 0.000000000000000000, 0.000000000000000000 ) ) ;
#21699=DIRECTION ( 'NONE',  ( 0.000000000000000000, 0.000000000000000000, 1.000000000000000000 ) ) ;
#21712=CARTESIAN_POINT ( 'NONE',  ( 64.97332050699269246, 0.9209334348186318797, -60.54988453772739376 ) ) ;
#21713=CIRCLE ( 'NONE', #31850, 1.000000000000001332 ) ;
#21722=CARTESIAN_POINT ( 'NONE',  ( 71.60339545440879760, 0.9065823421260940096, -60.75474143511929981 ) ) ;
#21740=CARTESIAN_POINT ( 'NONE',  ( 64.74970223533068747, 0.9307121176571799825, -60.69545425604199806 ) ) ;
#21745=CARTESIAN_POINT ( 'NONE',  ( 73.04596072059979406, 1.186701509386330011, -68.93447492634859941 ) ) ;
#21748=CARTESIAN_POINT ( 'NONE',  ( 73.18334309134580451, 0.9940423591679348192, -62.42346963566990325 ) ) ;
#21750=CARTESIAN_POINT ( 'NONE',  ( 71.46077416446640029, 1.263823323415690147, -60.83883010097409993 ) ) ;
#21756=CARTESIAN_POINT ( 'NONE',  ( 64.81979753630270125, 0.8904513541338849869, -70.65165619965239330 ) ) ;
#21770=DIRECTION ( 'NONE',  ( 0.000000000000000000, 1.000000000000000000, 0.000000000000000000 ) ) ;
#21803=CARTESIAN_POINT ( 'NONE',  ( 63.27438507250460020, 1.187296498006449985, -62.27829692513819992 ) ) ;
#21813=CARTESIAN_POINT ( 'NONE',  ( 63.67878178145871004, 1.266076204815560047, -69.56702768459580000 ) ) ;
#21818=CARTESIAN_POINT ( 'NONE',  ( 72.99206043124139853, 1.132579237369250036, -62.21177178793440277 ) ) ;
#21857=CARTESIAN_POINT ( 'NONE',  ( 72.96823525485120854, 0.9577391936075758672, -69.20405718729148248 ) ) ;
#21863=CARTESIAN_POINT ( 'NONE',  ( 71.33393739769628894, 10.88381105532070059, -69.34999999999999432 ) ) ;
#21870=CARTESIAN_POINT ( 'NONE',  ( 63.81514305365840301, 1.404167647216139958, -61.74627665679799549 ) ) ;
#21892=DIRECTION ( 'NONE',  ( 0.000000000000000000, 1.000000000000000000, 0.000000000000000000 ) ) ;
#21901=CARTESIAN_POINT ( 'NONE',  ( 72.00787155028989162, 0.9860880133278648874, -61.06736746306670227 ) ) ;
#21904=CARTESIAN_POINT ( 'NONE',  ( 64.56875406779060711, 1.236296663685629849, -70.35802301309989559 ) ) ;
#21917=CARTESIAN_POINT ( 'NONE',  ( 63.19277908840750513, 0.9325382164350239922, -69.05375146239639150 ) ) ;
#21947=CARTESIAN_POINT ( 'NONE',  ( 64.93393739769709327, 10.88381105532040038, -69.84999999999999432 ) ) ;
#21959=DIRECTION ( 'NONE',  ( -0.7071067811864684138, -0.7071067811866267316, 0.000000000000000000 ) ) ;
#21974=CARTESIAN_POINT ( 'NONE',  ( 65.25794138637670017, 1.383811055320669947, -60.91804007473620430 ) ) ;
#21988=ORIENTED_EDGE ( 'NONE', *, *, #18189, .F. ) ;
#22006=CARTESIAN_POINT ( 'NONE',  ( 72.86255183691179127, 1.369664981662529923, -62.55358821066108987 ) ) ;
#22010=CARTESIAN_POINT ( 'NONE',  ( 71.44807725908989937, 0.8904513541338849869, -60.64834380034769623 ) ) ;
#22012=CARTESIAN_POINT ( 'NONE',  ( 64.89338513303370348, 1.264489825601020190, -70.50788383491540401 ) ) ;
#22056=CARTESIAN_POINT ( 'NONE',  ( 63.19468704395299596, 0.8986939045430379913, -62.24348040161360274 ) ) ;
#22067=CARTESIAN_POINT ( 'NONE',  ( 63.45871665573360332, 1.367045641526529964, -68.91833781196129394 ) ) ;
#22096=EDGE_CURVE ( 'NONE', #27414, #8004, #27787, .T. ) ;
#22108=PLANE ( 'NONE',  #50657 ) ;
#22112=CARTESIAN_POINT ( 'NONE',  ( 72.65628610108569774, 1.412203896155640015, -69.03044017489760620 ) ) ;
#22128=CARTESIAN_POINT ( 'NONE',  ( 63.91114391772079273, 1.454949836291180132, -61.73964252679819964 ) ) ;
#22129=EDGE_LOOP ( 'NONE', ( #22775, #33491, #5534, #46223 ) ) ;
#22148=DIRECTION ( 'NONE',  ( -1.000000000000000000, 0.000000000000000000, 0.000000000000000000 ) ) ;
#22161=CARTESIAN_POINT ( 'NONE',  ( 64.59295435006930575, 1.031625743333890011, -70.48352829009921550 ) ) ;
#22173=CARTESIAN_POINT ( 'NONE',  ( 63.47152504824990160, 1.384378348444520013, -68.73316704115080711 ) ) ;
#22183=CARTESIAN_POINT ( 'NONE',  ( 71.40678801050209756, 1.186856010528209993, -70.56885973566780024 ) ) ;
#22191=CARTESIAN_POINT ( 'NONE',  ( 71.45588032111149346, 0.8910129994591539093, -70.64647704525299332 ) ) ;
#22197=ORIENTED_EDGE ( 'NONE', *, *, #5561, .T. ) ;
#22211=EDGE_CURVE ( 'NONE', #20803, #46160, #7755, .T. ) ;
#22214=ADVANCED_FACE ( 'NONE', ( #21251 ), #50440, .T. ) ;
#22229=ADVANCED_FACE ( 'NONE', ( #37780 ), #29384, .T. ) ;
#22234=CARTESIAN_POINT ( 'NONE',  ( 65.00022493107950083, 0.9952464559119579279, -60.54306244337860221 ) ) ;
#22251=CIRCLE ( 'NONE', #32265, 0.5000000000000004441 ) ;
#22265=CARTESIAN_POINT ( 'NONE',  ( 73.04943094402750603, 1.269319268680890067, -62.52104542963419931 ) ) ;
#22271=CARTESIAN_POINT ( 'NONE',  ( 65.11747358718560008, 1.386342629514219826, -70.29952392096339508 ) ) ;
#22327=CARTESIAN_POINT ( 'NONE',  ( 63.59767441460930115, 1.382577763791200010, -69.21733240916789498 ) ) ;
#22332=CARTESIAN_POINT ( 'NONE',  ( 72.94908864064930754, 0.9618757110850010283, -62.06981987203609918 ) ) ;
#22347=CARTESIAN_POINT ( 'NONE',  ( 63.48441347673288959, 1.386342629514219826, -68.66646381051069170 ) ) ;
#22357=DIRECTION ( 'NONE',  ( 0.000000000000000000, 0.000000000000000000, 1.000000000000000000 ) ) ;
#22359=CARTESIAN_POINT ( 'NONE',  ( 63.93393739769619089, 1.883811055320669947, -62.44999999999999574 ) ) ;
#22365=AXIS2_PLACEMENT_3D ( 'NONE', #781, #32214, #8404 ) ;
#22378=CARTESIAN_POINT ( 'NONE',  ( 63.54731047306190561, 1.396834109478129804, -68.84999999999999432 ) ) ;
#22380=CARTESIAN_POINT ( 'NONE',  ( 65.25681082723269810, 1.383811055320669947, -70.34375346881599000 ) ) ;
#22389=CARTESIAN_POINT ( 'NONE',  ( 63.58579710287288833, 1.402020837643050077, -62.24736188354039257 ) ) ;
#22423=CARTESIAN_POINT ( 'NONE',  ( 64.62814679718090360, 1.136680095839029958, -70.46339166529689635 ) ) ;
#22432=CARTESIAN_POINT ( 'NONE',  ( 63.15863832053869942, 1.096036836948800053, -68.93088433361418765 ) ) ;
#22435=EDGE_CURVE ( 'NONE', #7479, #19147, #11947, .T. ) ;
#22442=CARTESIAN_POINT ( 'NONE',  ( 71.22849534471220068, 1.384708701328909886, -70.30837376962780638 ) ) ;
#22457=EDGE_CURVE ( 'NONE', #49949, #45766, #18633, .T. ) ;
#22492=CARTESIAN_POINT ( 'NONE',  ( 64.81394005445639550, 0.9259537755896120048, -60.65222959644560063 ) ) ;
#22525=CARTESIAN_POINT ( 'NONE',  ( 72.95172982307090592, 1.328073773609220076, -62.51929651814780442 ) ) ;
#22532=CARTESIAN_POINT ( 'NONE',  ( 64.73018593529990028, 0.9325382164350189962, -70.59115830928880087 ) ) ;
#22538=CARTESIAN_POINT ( 'NONE',  ( 64.93393739769619799, 10.88381105532070059, -61.44999999999999574 ) ) ;
#22567=ADVANCED_FACE ( 'NONE', ( #21449 ), #14114, .F. ) ;
#22568=CARTESIAN_POINT ( 'NONE',  ( 63.24698825150780124, 1.338092079250050137, -68.62019553714330300 ) ) ;
#22574=CARTESIAN_POINT ( 'NONE',  ( 72.83393739769620367, 1.383811055320669947, -68.50657137141709541 ) ) ;
#22575=CARTESIAN_POINT ( 'NONE',  ( 63.39331655121669939, 1.326134026835559920, -62.35486255807249734 ) ) ;
#22576=DIRECTION ( 'NONE',  ( -3.885780586188051426E-13, 0.9739538916850928318, 0.2267461507313025260 ) ) ;
#22589=CARTESIAN_POINT ( 'NONE',  ( 71.23944111523938716, 1.270877794983130027, -60.72281693841739525 ) ) ;
#22612=FACE_OUTER_BOUND ( 'NONE', #46771, .T. ) ;
#22649=CARTESIAN_POINT ( 'NONE',  ( 63.72368862820488999, 1.434949534324519993, -62.02708488646099738 ) ) ;
#22653=CARTESIAN_POINT ( 'NONE',  ( 73.13312216970089708, 0.9955677559369568996, -68.95442834019429768 ) ) ;
#22657=ORIENTED_EDGE ( 'NONE', *, *, #44404, .F. ) ;
#22674=EDGE_CURVE ( 'NONE', #23933, #23138, #6000, .T. ) ;
#22681=CARTESIAN_POINT ( 'NONE',  ( 64.74323834027589442, 1.229084191802189974, -70.46414972969270707 ) ) ;
#22689=CARTESIAN_POINT ( 'NONE',  ( 71.45220707235199598, 1.395841836298969962, -70.23186791216220115 ) ) ;
#22696=CARTESIAN_POINT ( 'NONE',  ( 63.32276749867028798, 1.263823323415670163, -68.97683676677020514 ) ) ;
#22703=B_SPLINE_CURVE_WITH_KNOTS ( 'NONE', 3,
 ( #24796, #21135, #16975, #40803, #32920, #21901, #21389, #41578, #2006, #1236, #41841, #37394, #37913, #33446, #17226, #49206, #17988, #29259, #1496, #25053 ),
 .UNSPECIFIED., .F., .F.,
 ( 4, 2, 2, 2, 2, 2, 2, 2, 2, 4 ),
 ( -1.826192301619909975, -1.710015269444949970, -1.458000257333699867, -1.209852399823190039, -1.027233169661200041, -0.9130961508099529889, -0.6848221131074649914, -0.4130753771364510385, -0.1614840352283428704, 0.000000000000000000 ),
 .UNSPECIFIED. ) ;
#22705=CARTESIAN_POINT ( 'NONE',  ( 71.29701819511369365, 1.369719003397489976, -70.35226930031730319 ) ) ;
#22711=CARTESIAN_POINT ( 'NONE',  ( 71.48855272380090753, 0.8936201581567910779, -70.62461353540280129 ) ) ;
#22718=DIRECTION ( 'NONE',  ( 3.281478866952075176E-28, -2.435884827299240233E-11, -1.000000000000000000 ) ) ;
#22731=AXIS2_PLACEMENT_3D ( 'NONE', #43308, #3472, #15771 ) ;
#22744=CARTESIAN_POINT ( 'NONE',  ( 71.03155062328740144, 1.383928098097870096, -70.33743540642140601 ) ) ;
#22749=CARTESIAN_POINT ( 'NONE',  ( 65.13185782384009315, 1.385888765344509999, -60.99577487439199786 ) ) ;
#22775=ORIENTED_EDGE ( 'NONE', *, *, #31874, .F. ) ;
#22780=CARTESIAN_POINT ( 'NONE',  ( 73.04443511092439678, 0.9036513197889520788, -62.20214363597960272 ) ) ;
#22787=CARTESIAN_POINT ( 'NONE',  ( 64.72196861157999592, 1.188860127980290171, -70.48451794758260291 ) ) ;
#22791=ORIENTED_EDGE ( 'NONE', *, *, #14250, .F. ) ;
#22829=DIRECTION ( 'NONE',  ( -0.7071067811864684138, -0.7071067811866267316, 0.000000000000000000 ) ) ;
#22842=DIRECTION ( 'NONE',  ( 1.000000000000000000, 0.000000000000000000, 0.000000000000000000 ) ) ;
#22843=CARTESIAN_POINT ( 'NONE',  ( 71.25020460053529803, 1.328674444234389851, -60.82574149480920056 ) ) ;
#22872=CARTESIAN_POINT ( 'NONE',  ( 63.13746035244320609, 0.8910129994591539093, -62.32805707658469885 ) ) ;
#22895=CARTESIAN_POINT ( 'NONE',  ( 63.60923929913089836, 1.000506532485009981, -61.70853630543769697 ) ) ;
#22903=CARTESIAN_POINT ( 'NONE',  ( 63.61601920124529386, 1.328802495350130064, -61.91104772260080580 ) ) ;
#22906=CARTESIAN_POINT ( 'NONE',  ( 73.12399047084761605, 1.191644800533219861, -68.79793125682789423 ) ) ;
#22923=CARTESIAN_POINT ( 'NONE',  ( 71.83393739769618946, 10.88381105532070059, -68.84999999999999432 ) ) ;
#22943=CARTESIAN_POINT ( 'NONE',  ( 71.33393739769670105, 1.396834109478129804, -70.23662692463440749 ) ) ;
#22944=EDGE_CURVE ( 'NONE', #5288, #11422, #35584, .T. ) ;
#22957=CARTESIAN_POINT ( 'NONE',  ( 71.19853741683878923, 1.383922910988889976, -70.31893907080630868 ) ) ;
#22970=CIRCLE ( 'NONE', #29671, 0.9999999999999964473 ) ;
#22999=CARTESIAN_POINT ( 'NONE',  ( 71.20900144662560649, 1.388715606738730068, -70.28003120372629553 ) ) ;
#23005=CARTESIAN_POINT ( 'NONE',  ( 65.00039235738410071, 1.369544300367010026, -60.93595317393490518 ) ) ;
#23035=CARTESIAN_POINT ( 'NONE',  ( 72.72056432233058842, 1.396834109478120034, -68.84999999999999432 ) ) ;
#23037=CARTESIAN_POINT ( 'NONE',  ( 72.74776047649520194, 1.391252479931859964, -62.52735703481241103 ) ) ;
#23045=CARTESIAN_POINT ( 'NONE',  ( 64.68608103367590445, 0.9036513197889380899, -70.56049771322820163 ) ) ;
#23046=ORIENTED_EDGE ( 'NONE', *, *, #5718, .F. ) ;
#23084=ORIENTED_EDGE ( 'NONE', *, *, #5561, .F. ) ;
#23087=CARTESIAN_POINT ( 'NONE',  ( 72.83393739769620367, 1.883811055320669947, -65.65000000000000568 ) ) ;
#23088=CARTESIAN_POINT ( 'NONE',  ( 63.23690831390890565, 1.005545696829380109, -62.19455336271669665 ) ) ;
#23098=CARTESIAN_POINT ( 'NONE',  ( 71.62484648860579739, 0.9098571636355720083, -70.52991329011129551 ) ) ;
#23101=CARTESIAN_POINT ( 'NONE',  ( 71.31531788893299506, 1.266538207494809942, -60.76118683403129950 ) ) ;
#23103=CARTESIAN_POINT ( 'NONE',  ( 72.26754656970919655, 1.277124412296160028, -61.38619408099160069 ) ) ;
#23128=( NAMED_UNIT ( * ) PLANE_ANGLE_UNIT ( ) SI_UNIT ( $, .RADIAN. ) );
#23138=VERTEX_POINT ( 'NONE', #21633 ) ;
#23142=CARTESIAN_POINT ( 'NONE',  ( 68.13393739769620083, 1.883811055320669947, -60.94999999999999574 ) ) ;
#23157=CARTESIAN_POINT ( 'NONE',  ( 63.51710413059809213, 1.389801772588449946, -62.42722031148289830 ) ) ;
#23161=CARTESIAN_POINT ( 'NONE',  ( 73.19885236215881719, 0.9940695285616559795, -68.85188839627709001 ) ) ;
#23194=CARTESIAN_POINT ( 'NONE',  ( 72.08589079625491536, 1.185470598955550292, -70.12663493719820451 ) ) ;
#23204=CARTESIAN_POINT ( 'NONE',  ( 63.46802213033259221, 0.9644268476137549673, -69.42324179401769868 ) ) ;
#23241=CARTESIAN_POINT ( 'NONE',  ( 63.06393505168800573, 0.8850831926798620186, -68.85873448833349642 ) ) ;
#23252=TOROIDAL_SURFACE ( 'NONE', #49261, 5.500000000000000000, 0.5000000000000000000 ) ;
#23258=CARTESIAN_POINT ( 'NONE',  ( 64.78158399514478560, 0.9281439705311279598, -60.67386159597580075 ) ) ;
#23275=DIRECTION ( 'NONE',  ( 1.000000000000000000, 0.000000000000000000, 0.000000000000000000 ) ) ;
#23286=CARTESIAN_POINT ( 'NONE',  ( 72.96606887121211571, 1.263738073398980033, -62.36141320605320004 ) ) ;
#23293=CARTESIAN_POINT ( 'NONE',  ( 64.67849076041298417, 1.005545696829380109, -70.54702908378739323 ) ) ;
#23350=CARTESIAN_POINT ( 'NONE',  ( 71.42462519098069151, 0.8888742037077609348, -60.63285689971630177 ) ) ;
#23351=CARTESIAN_POINT ( 'NONE',  ( 72.34252581843109908, 1.117797034538490220, -61.38010380652460185 ) ) ;
#23367=AXIS2_PLACEMENT_3D ( 'NONE', #35992, #27611, #43617 ) ;
#23378=DIRECTION ( 'NONE',  ( 0.000000000000000000, -1.000000000000000000, 0.000000000000000000 ) ) ;
#23394=CARTESIAN_POINT ( 'NONE',  ( 71.33393739769628894, 1.530257664727400879, -61.30355339059330078 ) ) ;
#23398=CARTESIAN_POINT ( 'NONE',  ( 63.33805919087440373, 1.375383258925270136, -62.73515566246579311 ) ) ;
#23414=CARTESIAN_POINT ( 'NONE',  ( 63.29751574937540681, 1.134292167764730186, -62.17859900726310229 ) ) ;
#23418=CARTESIAN_POINT ( 'NONE',  ( 73.17063711417530669, 1.097895768572089814, -68.83057487531520735 ) ) ;
#23424=VERTEX_POINT ( 'NONE', #11886 ) ;
#23436=CARTESIAN_POINT ( 'NONE',  ( 72.78816252330430814, 1.385888765344509999, -62.64792042614379852 ) ) ;
#23450=CARTESIAN_POINT ( 'NONE',  ( 71.88854470306299049, 1.063298638254559947, -70.32231691988620526 ) ) ;
#23459=CARTESIAN_POINT ( 'NONE',  ( 64.46842165375500144, 0.9408120350972789536, -70.40100145642890084 ) ) ;
#23461=EDGE_CURVE ( 'NONE', #49612, #33931, #40406, .T. ) ;
#23466=CARTESIAN_POINT ( 'NONE',  ( 64.86559958573499785, 1.367045641526529964, -60.97477925803730159 ) ) ;
#23486=CARTESIAN_POINT ( 'NONE',  ( 71.65445125112970004, 0.9525601718068800183, -60.79122054831070443 ) ) ;
#23494=CYLINDRICAL_SURFACE ( 'NONE', #6566, 0.5000000000000049960 ) ;
#23515=CARTESIAN_POINT ( 'NONE',  ( 64.96708350509689467, 1.267233196669030004, -60.75373513970999539 ) ) ;
#23545=CARTESIAN_POINT ( 'NONE',  ( 72.83620669801349834, 1.369719003397489976, -62.48691920258249155 ) ) ;
#23549=LINE ( 'NONE', #30903, #3354 ) ;
#23550=AXIS2_PLACEMENT_3D ( 'NONE', #45338, #33261, #4204 ) ;
#23568=DIRECTION ( 'NONE',  ( 0.000000000000000000, 1.000000000000000000, 0.000000000000000000 ) ) ;
#23587=CARTESIAN_POINT ( 'NONE',  ( 63.13551795786779053, 1.096291039689149871, -68.89363957891330870 ) ) ;
#23608=CARTESIAN_POINT ( 'NONE',  ( 71.40893329644839582, 0.8879664753683469414, -60.62259972594610247 ) ) ;
#23610=CARTESIAN_POINT ( 'NONE',  ( 72.34709478978140851, 1.033004162168289941, -61.37787765298320153 ) ) ;
#23615=EDGE_CURVE ( 'NONE', #51085, #41914, #22703, .T. ) ;
#23631=DIRECTION ( 'NONE',  ( 0.7071067811865475727, 0.000000000000000000, 0.7071067811865475727 ) ) ;
#23634=EDGE_CURVE ( 'NONE', #37946, #46311, #30020, .T. ) ;
#23647=DIRECTION ( 'NONE',  ( -0.000000000000000000, 1.000000000000000000, 0.000000000000000000 ) ) ;
#23658=CARTESIAN_POINT ( 'NONE',  ( 63.29300171101180439, 1.330484379554849994, -62.57139521546640992 ) ) ;
#23670=CARTESIAN_POINT ( 'NONE',  ( 63.25101889642220954, 0.9479899806831150189, -62.16329186921600325 ) ) ;
#23674=CARTESIAN_POINT ( 'NONE',  ( 72.85934862407960111, 1.383411777981069957, -68.54655896616850441 ) ) ;
#23712=CARTESIAN_POINT ( 'NONE',  ( 72.42083049230619451, 1.199410787637519960, -69.81037093930601145 ) ) ;
#23715=( LENGTH_UNIT ( ) NAMED_UNIT ( * ) SI_UNIT ( .MILLI., .METRE. ) );
#23721=CARTESIAN_POINT ( 'NONE',  ( 63.25402410758490390, 0.9098571636355720083, -69.14090909090960224 ) ) ;
#23727=CARTESIAN_POINT ( 'NONE',  ( 71.33393739769660158, 1.396834109478120034, -70.23662692463440749 ) ) ;
#23756=DIRECTION ( 'NONE',  ( 0.7071067811865656694, -0.7071067811865292541, 0.000000000000000000 ) ) ;
#23803=CARTESIAN_POINT ( 'NONE',  ( 73.05279713336409486, 1.186856010528209993, -62.37714938719420132 ) ) ;
#23839=CARTESIAN_POINT ( 'NONE',  ( 63.11947343109709863, 1.194703186106690129, -68.75325824359919125 ) ) ;
#23863=CARTESIAN_POINT ( 'NONE',  ( 71.37448966235888292, 1.264489825601020190, -60.79211616508469973 ) ) ;
#23866=CARTESIAN_POINT ( 'NONE',  ( 72.34669642622959884, 1.061268603384970088, -61.37747933361649899 ) ) ;
#23908=CARTESIAN_POINT ( 'NONE',  ( 63.25550833076970747, 1.336371993404949832, -62.65916430077300703 ) ) ;
#23922=CARTESIAN_POINT ( 'NONE',  ( 63.25402410758490390, 0.9098571636355720083, -62.15909090909049439 ) ) ;
#23933=VERTEX_POINT ( 'NONE', #1667 ) ;
#23937=ORIENTED_EDGE ( 'NONE', *, *, #15601, .T. ) ;
#23951=FACE_OUTER_BOUND ( 'NONE', #13007, .T. ) ;
#23963=CARTESIAN_POINT ( 'NONE',  ( 72.31717656023090512, 1.061277144319840104, -69.95204556025490206 ) ) ;
#23976=CARTESIAN_POINT ( 'NONE',  ( 71.58179376171669617, 0.9036513197889520788, -70.56049771322810216 ) ) ;
#23989=VERTEX_POINT ( 'NONE', #38613 ) ;
#23997=VECTOR ( 'NONE', #16223, 1000.000000000000000 ) ;
#24028=TOROIDAL_SURFACE ( 'NONE', #34079, 1.499999999905649917, 0.4999999999954780061 ) ;
#24031=CARTESIAN_POINT ( 'NONE',  ( 72.55472656186499592, 1.019773975906290042, -69.70721229073478753 ) ) ;
#24056=CARTESIAN_POINT ( 'NONE',  ( 73.01385068780759013, 0.9098571636355680115, -62.15909090909049439 ) ) ;
#24067=CARTESIAN_POINT ( 'NONE',  ( 63.51391054266390768, 1.390208944942409985, -68.75457626026799574 ) ) ;
#24093=CARTESIAN_POINT ( 'NONE',  ( 63.45501836690030473, 1.383357884654609959, -68.68594134708139620 ) ) ;
#24106=CARTESIAN_POINT ( 'NONE',  ( 71.26289196806200721, 1.269319268680890067, -70.56549354633131088 ) ) ;
#24115=CARTESIAN_POINT ( 'NONE',  ( 71.45332619318591583, 1.096305581841150012, -60.69897858480909747 ) ) ;
#24117=CARTESIAN_POINT ( 'NONE',  ( 72.33986051001160433, 1.456055805561079941, -61.71730126733579169 ) ) ;
#24119=CARTESIAN_POINT ( 'NONE',  ( 65.12253294394879788, 1.334812829108570131, -70.51979614837409827 ) ) ;
#24122=CARTESIAN_POINT ( 'NONE',  ( 72.33393739769574893, 11.38368607098449914, -62.44999999999853202 ) ) ;
#24124=ORIENTED_EDGE ( 'NONE', *, *, #17615, .F. ) ;
#24163=CARTESIAN_POINT ( 'NONE',  ( 63.34531745652139989, 1.374300485541529948, -62.71457717039259450 ) ) ;
#24176=CARTESIAN_POINT ( 'NONE',  ( 63.37668255464280520, 1.045341414535140068, -62.00499031178430442 ) ) ;
#24216=CARTESIAN_POINT ( 'NONE',  ( 72.40210087067039524, 1.451792515613489876, -69.49977495595670973 ) ) ;
#24224=CARTESIAN_POINT ( 'NONE',  ( 71.33393739769628894, 11.38381102407070067, -69.35012499995160340 ) ) ;
#24228=CARTESIAN_POINT ( 'NONE',  ( 64.75444473847480253, 1.309114013480900063, -60.92108349576849946 ) ) ;
#24230=CARTESIAN_POINT ( 'NONE',  ( 71.53768886009270034, 0.9325382164350239922, -70.59115830928880087 ) ) ;
#24258=ADVANCED_FACE ( 'NONE', ( #19954 ), #39449, .F. ) ;
#24267=CARTESIAN_POINT ( 'NONE',  ( 64.64302830678670375, 0.9098571636355720083, -70.52991329011129551 ) ) ;
#24289=VECTOR ( 'NONE', #27573, 1000.000000000000000 ) ;
#24324=CARTESIAN_POINT ( 'NONE',  ( 72.72056432233058842, 1.396834109478129804, -68.84999999999999432 ) ) ;
#24344=B_SPLINE_CURVE_WITH_KNOTS ( 'NONE', 3,
 ( #44037, #40359, #29077, #36162, #39851, #3958, #270, #12857, #36671, #35910, #32209, #44550, #12327, #31955, #20424, #36412 ),
 .UNSPECIFIED., .F., .F.,
 ( 4, 2, 2, 2, 2, 2, 2, 4 ),
 ( -8.604228000000000152E-15, 0.07319275283555599920, 0.1391693187718399949, 0.1804046724820189962, 0.2061767685508799908, 0.2577209606886020077, 0.3401916681089580119, 0.4123535371017689743 ),
 .UNSPECIFIED. ) ;
#24352=CARTESIAN_POINT ( 'NONE',  ( 63.25402410758490390, 0.9098571636355720083, -69.14090909090960224 ) ) ;
#24354=CARTESIAN_POINT ( 'NONE',  ( 63.46757340380580814, 1.384887413063060180, -68.61455525072810246 ) ) ;
#24364=CIRCLE ( 'NONE', #15206, 0.5000000000000004441 ) ;
#24368=CARTESIAN_POINT ( 'NONE',  ( 71.31451227301140250, 1.097895768572089814, -70.68669971647908312 ) ) ;
#24377=CARTESIAN_POINT ( 'NONE',  ( 71.47772926835831697, 0.9971903505820688407, -60.67679930835159752 ) ) ;
#24379=CARTESIAN_POINT ( 'NONE',  ( 71.36792781540339092, 1.399433130755050048, -61.07453677926569924 ) ) ;
#24381=CARTESIAN_POINT ( 'NONE',  ( 65.14992021336850314, 1.382840740411480196, -70.34664320112889868 ) ) ;
#24423=CARTESIAN_POINT ( 'NONE',  ( 63.17514626975080461, 1.276058558775519991, -62.60937635806730839 ) ) ;
#24438=AXIS2_PLACEMENT_3D ( 'NONE', #36997, #21770, #18112 ) ;
#24454=DIRECTION ( 'NONE',  ( 1.000000000000000000, -0.000000000000000000, 1.224646799147353207E-16 ) ) ;
#24478=CARTESIAN_POINT ( 'NONE',  ( 72.23325239345169280, 1.348268854479550027, -69.88207728865640433 ) ) ;
#24491=CARTESIAN_POINT ( 'NONE',  ( 64.93393739769578588, 1.396834109478129804, -61.06337307536569625 ) ) ;
#24520=ORIENTED_EDGE ( 'NONE', *, *, #23461, .T. ) ;
#24534=CARTESIAN_POINT ( 'NONE',  ( 63.86970618309410952, 1.277726045464569804, -69.78446896035558211 ) ) ;
#24576=ADVANCED_FACE ( 'NONE', ( #14879 ), #50159, .F. ) ;
#24614=CARTESIAN_POINT ( 'NONE',  ( 63.20402522475220053, 1.187237555532410171, -68.90390165256179955 ) ) ;
#24616=DIRECTION ( 'NONE',  ( 0.2267461507312891755, 0.9739538916850959405, 3.885780586188060513E-13 ) ) ;
#24627=FACE_OUTER_BOUND ( 'NONE', #8058, .T. ) ;
#24631=DIRECTION ( 'NONE',  ( 0.000000000000000000, 0.000000000000000000, 1.000000000000000000 ) ) ;
#24632=CARTESIAN_POINT ( 'NONE',  ( 73.06384957064030061, 1.187237555532410171, -68.90390165256179955 ) ) ;
#24635=CARTESIAN_POINT ( 'NONE',  ( 73.01236646462280078, 1.336371993404949832, -62.65916430077300703 ) ) ;
#24638=CARTESIAN_POINT ( 'NONE',  ( 71.25801539443460797, 1.385702546077159925, -61.00218178904909649 ) ) ;
#24640=CARTESIAN_POINT ( 'NONE',  ( 72.03766074089830340, 1.404167647216139958, -61.33120565596220075 ) ) ;
#24643=CARTESIAN_POINT ( 'NONE',  ( 64.90740703336619788, 0.9940423591679298232, -70.69940569364969463 ) ) ;
#24644=ORIENTED_EDGE ( 'NONE', *, *, #3666, .F. ) ;
#24662=VERTEX_POINT ( 'NONE', #47383 ) ;
#24683=CARTESIAN_POINT ( 'NONE',  ( 63.09723768121719445, 1.097895768572089814, -62.46942512468480402 ) ) ;
#24691=CARTESIAN_POINT ( 'NONE',  ( 64.66786723518751501, 0.9395704634982890990, -60.75234178971950172 ) ) ;
#24696=DIRECTION ( 'NONE',  ( 0.000000000000000000, 1.000000000000000000, 0.000000000000000000 ) ) ;
#24735=AXIS2_PLACEMENT_3D ( 'NONE', #19427, #27284, #37 ) ;
#24741=CARTESIAN_POINT ( 'NONE',  ( 72.33301759304930556, 1.348264851907009731, -69.78229850496350650 ) ) ;
#24755=CARTESIAN_POINT ( 'NONE',  ( 64.10467614833328298, 1.346167254499869959, -61.35479024022959749 ) ) ;
#24781=DIRECTION ( 'NONE',  ( 0.000000000000000000, 1.000000000000000000, 0.000000000000000000 ) ) ;
#24792=VECTOR ( 'NONE', #49083, 1000.000000000000000 ) ;
#24796=CARTESIAN_POINT ( 'NONE',  ( 71.62484648860579739, 0.9098571636355720083, -60.77008670988870165 ) ) ;
#24798=CARTESIAN_POINT ( 'NONE',  ( 64.00031433471698961, 1.277124716467510135, -69.91379268075820619 ) ) ;
#24811=CARTESIAN_POINT ( 'NONE',  ( 65.13393739769620083, -42.61618894467930119, -65.65000000000000568 ) ) ;
#24845=CARTESIAN_POINT ( 'NONE',  ( 71.80939745721281042, 1.439519383694590093, -70.03165268182070236 ) ) ;
#24846=CARTESIAN_POINT ( 'NONE',  ( 63.51391054266390768, 1.390208944942419755, -62.54542373973200142 ) ) ;
#24874=CARTESIAN_POINT ( 'NONE',  ( 63.15779899367210248, 0.9281439705311279598, -69.00235340255139249 ) ) ;
#24885=CARTESIAN_POINT ( 'NONE',  ( 71.40029138921259744, 0.9945465939392450494, -70.67393287070269992 ) ) ;
#24890=CARTESIAN_POINT ( 'NONE',  ( 72.90248002265630589, 1.325715844996850024, -68.88725199158319867 ) ) ;
#24893=CARTESIAN_POINT ( 'NONE',  ( 73.17080802144350571, 1.198183261254780030, -62.58868501588759869 ) ) ;
#24895=CARTESIAN_POINT ( 'NONE',  ( 71.44150897753121399, 1.096153228089719933, -60.69147900812899366 ) ) ;
#24897=CARTESIAN_POINT ( 'NONE',  ( 71.50039957044630512, 1.308983041454300000, -60.91458334016920162 ) ) ;
#24900=CARTESIAN_POINT ( 'NONE',  ( 65.13185782384009315, 1.385888765344500007, -70.30422512560809878 ) ) ;
#24931=EDGE_CURVE ( 'NONE', #7479, #4963, #17072, .T. ) ;
#24942=CARTESIAN_POINT ( 'NONE',  ( 63.49266932922240159, 1.386446979194299933, -62.50785065198430601 ) ) ;
#24945=DIRECTION ( 'NONE',  ( 0.000000000000000000, 1.000000000000000000, 0.000000000000000000 ) ) ;
#24947=CARTESIAN_POINT ( 'NONE',  ( 71.40255948545589604, 1.402336724396250123, -61.08651255177160522 ) ) ;
#24961=EDGE_LOOP ( 'NONE', ( #19009, #2644, #35889, #49267 ) ) ;
#24968=CARTESIAN_POINT ( 'NONE',  ( 63.91114391772079273, 1.454949836291180132, -61.73964252679819964 ) ) ;
#24969=EDGE_LOOP ( 'NONE', ( #43369, #42386, #49324, #42661 ) ) ;
#24981=ORIENTED_EDGE ( 'NONE', *, *, #48316, .T. ) ;
#24997=CARTESIAN_POINT ( 'NONE',  ( 72.70940061843029412, 1.399433130755119992, -68.88399041770809106 ) ) ;
#25011=CARTESIAN_POINT ( 'NONE',  ( 64.11008412164950698, 1.443559558797649967, -61.49008420214889981 ) ) ;
#25053=CARTESIAN_POINT ( 'NONE',  ( 73.01385068780759013, 0.9098571636355720083, -62.15909090909049439 ) ) ;
#25055=CARTESIAN_POINT ( 'NONE',  ( 64.20565978367740456, 1.440336511345229997, -69.88995585498329888 ) ) ;
#25089=CARTESIAN_POINT ( 'NONE',  ( 72.82137280411760116, 1.383928098097870096, -68.54761322559109260 ) ) ;
#25090=B_SPLINE_SURFACE_WITH_KNOTS ( 'NONE', 3, 3, ( 
 ( #37731, #37470, #17559, #32461, #36949, #13131, #25138, #45076, #9185, #51738 ),
 ( #27622, #15064, #18730, #46795, #27112, #42861, #19249, #3539, #23674, #47315 ),
 ( #34968, #15833, #38673, #34709, #47816, #10887, #39691, #47562, #50965, #43372 ),
 ( #39178, #12616, #23161, #23418, #22906, #51238, #44576, #11657, #38924, #3273 ),
 ( #2758, #14808, #43115, #11142, #47058, #7206, #19509, #3796, #50709, #35231 ),
 ( #30773, #51489, #26850, #6956, #15329, #3016, #18987, #35499, #15589, #31282 ),
 ( #11403, #31032, #7464, #31543, #43628, #27365, #39439, #19765, #7731, #35756 ),
 ( #31798, #28576, #22653, #13905, #25675, #8680, #45616, #49045, #9468, #33289 ),
 ( #40903, #40645, #29358, #49305, #24632, #45364, #41677, #25416, #45099, #41418 ),
 ( #13652, #5785, #9716, #5277, #1336, #28840, #16803, #1851, #13151, #17829 ),
 ( #13400, #29613, #4743, #29863, #21745, #32752, #37753, #33802, #49813, #17068 ),
 ( #41165, #20710, #36701, #25158, #5536, #803, #36974, #17579, #33549, #44843 ),
 ( #21491, #33020, #17326, #48778, #12884, #8948, #24890, #29101, #5013, #37491 ),
 ( #37238, #20975, #1591, #1071, #9206, #49566, #21228, #46668, #26982, #25932 ),
 ( #2892, #11011, #50842, #6046, #30128, #42731, #42207, #42989, #30386, #46410 ),
 ( #10498, #26712, #38271, #26196, #9970, #14933, #6305, #34581, #7085, #23035 ) ),
 .UNSPECIFIED., .F., .F., .F.,
 ( 4, 2, 2, 2, 2, 2, 2, 4 ),
 ( 4, 1, 1, 1, 1, 1, 1, 4 ),
 ( -1.183080999999999906E-15, 0.07216186899280699341, 0.1546325764131580016, 0.2061767685508779924, 0.2319488646197380155, 0.2731842183299139637, 0.3391607842661950034, 0.4123535371017569839 ),
 ( 0.000000000000000000, 0.1428571428571430157, 0.2857142857142860315, 0.4285714285714289917, 0.5714285714285709528, 0.7142857142857139685, 0.8571428571428569843, 1.000000000000000000 ),
 .UNSPECIFIED. ) ;
#25093=ORIENTED_EDGE ( 'NONE', *, *, #51402, .F. ) ;
#25125=CIRCLE ( 'NONE', #13453, 0.5000000000000004441 ) ;
#25133=FACE_OUTER_BOUND ( 'NONE', #30588, .T. ) ;
#25138=CARTESIAN_POINT ( 'NONE',  ( 73.02088654388471411, 1.338092079250050137, -68.62019553714330300 ) ) ;
#25152=CARTESIAN_POINT ( 'NONE',  ( 71.01106396815980304, 1.383811055320669947, -70.34375346881599000 ) ) ;
#25158=CARTESIAN_POINT ( 'NONE',  ( 73.06536971133249381, 1.096932441169210071, -69.00001114258428458 ) ) ;
#25161=CARTESIAN_POINT ( 'NONE',  ( 73.02088654388471411, 1.338092079250050137, -62.67980446285670126 ) ) ;
#25164=CARTESIAN_POINT ( 'NONE',  ( 71.33393739769660158, 1.396834109478129804, -61.06337307536559678 ) ) ;
#25166=CARTESIAN_POINT ( 'NONE',  ( 71.99615133745550111, 1.261444690199579943, -61.15177544325119641 ) ) ;
#25167=AXIS2_PLACEMENT_3D ( 'NONE', #20409, #28019, #40599 ) ;
#25170=CARTESIAN_POINT ( 'NONE',  ( 65.25681082723269810, 1.383811055320669947, -70.34375346881599000 ) ) ;
#25175=VERTEX_POINT ( 'NONE', #50719 ) ;
#25211=CARTESIAN_POINT ( 'NONE',  ( 63.36539477273620236, 1.325715844996850024, -62.41274800841679848 ) ) ;
#25216=CARTESIAN_POINT ( 'NONE',  ( 72.33986051001160433, 1.456055805561079941, -61.71730126733579169 ) ) ;
#25221=CARTESIAN_POINT ( 'NONE',  ( 63.30597626835550784, 1.134959972145540119, -69.13433375889879073 ) ) ;
#25241=DIRECTION ( 'NONE',  ( 0.000000000000000000, 0.000000000000000000, 1.000000000000000000 ) ) ;
#25243=CIRCLE ( 'NONE', #15205, 0.5000000000000045519 ) ;
#25280=CARTESIAN_POINT ( 'NONE',  ( 64.50758838025409148, 1.321111291668120025, -61.05922999307440335 ) ) ;
#25310=AXIS2_PLACEMENT_3D ( 'NONE', #37195, #21699, #21959 ) ;
#25320=CARTESIAN_POINT ( 'NONE',  ( 64.40830624361899481, 1.428532738834869864, -70.03330250477451102 ) ) ;
#25332=DIRECTION ( 'NONE',  ( 0.000000000000000000, 0.000000000000000000, -1.000000000000000000 ) ) ;
#25351=CARTESIAN_POINT ( 'NONE',  ( 72.74776047649530142, 1.391252479931859964, -68.77264296518760034 ) ) ;
#25389=CARTESIAN_POINT ( 'NONE',  ( 64.98600614086828386, 1.191644800533210091, -60.65994692684869705 ) ) ;
#25416=CARTESIAN_POINT ( 'NONE',  ( 72.85976395805219852, 1.369613126987639928, -68.75357062980060618 ) ) ;
#25421=CARTESIAN_POINT ( 'NONE',  ( 71.35301946752790059, 1.370853092582090094, -60.97060118797210038 ) ) ;
#25423=CARTESIAN_POINT ( 'NONE',  ( 71.51437757259260763, 1.412203896155519889, -61.12765129660999719 ) ) ;
#25425=DIRECTION ( 'NONE',  ( 0.000000000000000000, 0.000000000000000000, -1.000000000000000000 ) ) ;
#25426=CARTESIAN_POINT ( 'NONE',  ( 64.88733809717990653, 1.187415670095769871, -70.58414947367060677 ) ) ;
#25429=DIRECTION ( 'NONE',  ( 0.000000000000000000, -1.000000000000000000, 0.000000000000000000 ) ) ;
#25467=CARTESIAN_POINT ( 'NONE',  ( 63.18115153217100755, 0.8966068345641580173, -62.26318953425310099 ) ) ;
#25479=CARTESIAN_POINT ( 'NONE',  ( 63.31978766800369840, 1.229084191802120030, -69.04069905742069579 ) ) ;
#25486=EDGE_CURVE ( 'NONE', #26724, #43577, #29399, .T. ) ;
#25492=AXIS2_PLACEMENT_3D ( 'NONE', #30236, #25520, #37586 ) ;
#25499=CARTESIAN_POINT ( 'NONE',  ( 63.72368862820488999, 1.434949534324519993, -62.02708488646099738 ) ) ;
#25507=CARTESIAN_POINT ( 'NONE',  ( 73.02919596257699197, 0.9065823421260940096, -69.11945805671248877 ) ) ;
#25520=DIRECTION ( 'NONE',  ( 0.000000000000000000, 1.000000000000000000, 0.000000000000000000 ) ) ;
#25523=DIRECTION ( 'NONE',  ( -1.000000000000000000, 0.000000000000000000, 0.000000000000000000 ) ) ;
#25524=CARTESIAN_POINT ( 'NONE',  ( 72.90864092247801409, 1.230946250268279973, -69.10734940427019524 ) ) ;
#25537=CARTESIAN_POINT ( 'NONE',  ( 64.14653846951229355, 1.039769764133499974, -61.16551630736319822 ) ) ;
#25545=DIRECTION ( 'NONE',  ( 1.000000000000000000, 0.000000000000000000, 0.000000000000000000 ) ) ;
#25563=DIRECTION ( 'NONE',  ( 0.000000000000000000, 0.000000000000000000, 1.000000000000000000 ) ) ;
#25575=CARTESIAN_POINT ( 'NONE',  ( 63.65729443213299987, 1.185469602160369895, -69.60194394625881387 ) ) ;
#25643=CARTESIAN_POINT ( 'NONE',  ( 66.53393739769619231, 11.23736444591397543, -69.70355339059327093 ) ) ;
#25647=CARTESIAN_POINT ( 'NONE',  ( 65.01767771978660448, 0.8838110553206759423, -60.52272727272730179 ) ) ;
#25675=CARTESIAN_POINT ( 'NONE',  ( 73.06808687136680192, 1.187415670095769871, -68.89659930051639947 ) ) ;
#25678=CARTESIAN_POINT ( 'NONE',  ( 73.13041444294920268, 0.8910129994591549085, -62.32805707658469885 ) ) ;
#25680=CARTESIAN_POINT ( 'NONE',  ( 71.54590618381259048, 1.188860127980290171, -60.81548205241750082 ) ) ;
#25685=CARTESIAN_POINT ( 'NONE',  ( 65.05904174327520195, 1.369885150286800135, -70.38694600888931063 ) ) ;
#25725=CARTESIAN_POINT ( 'NONE',  ( 63.24043675930629860, 1.099344084866029858, -62.24193811877859162 ) ) ;
#25735=CARTESIAN_POINT ( 'NONE',  ( 63.78870119449619835, 1.432915709213359978, -69.43629025642729857 ) ) ;
#25745=ORIENTED_EDGE ( 'NONE', *, *, #26755, .F. ) ;
#25747=ORIENTED_EDGE ( 'NONE', *, *, #35434, .F. ) ;
#25754=B_SPLINE_SURFACE_WITH_KNOTS ( 'NONE', 3, 3, ( 
 ( #24491, #4596, #23466, #32098, #43675, #46662, #16399, #48117, #28178 ),
 ( #40508, #31588, #44180, #24228, #19816, #40253, #20314, #35804, #28439 ),
 ( #30638, #50578, #42723, #41800, #49682, #21604, #45225, #13775, #44698 ),
 ( #29729, #17187, #13522, #41025, #1453, #5394, #28696, #45745, #25791 ),
 ( #21351, #33408, #28961, #25280, #1195, #9839, #33666, #37098, #37354 ),
 ( #37608, #5141, #32875, #934, #666, #44960, #45485, #41284, #49171 ),
 ( #13006, #1714, #9062, #17697, #49426, #48909, #13263, #25537, #17442 ),
 ( #12741, #8803, #20571, #24755, #29480, #9583, #41541, #36564, #5657 ),
 ( #4866, #25011, #29218, #9333, #16656, #32613, #48640, #40765, #20833 ),
 ( #21095, #36831, #16931, #33144, #34175, #50454, #46791, #46536, #5907 ),
 ( #38920, #26578, #42331, #42594, #15060, #42067, #14804, #26059, #6169 ),
 ( #22128, #14028, #50961, #10361, #31028, #38135, #10624, #10883, #37881 ),
 ( #47053, #6952, #21870, #18472, #50705, #6691, #18726, #1973, #34705 ),
 ( #46009, #6430, #10100, #2235, #2754, #17952, #49937, #29986, #27108 ),
 ( #22649, #30769, #26846, #22903, #42856, #18211, #50194, #46275, #14544 ),
 ( #11138, #3012, #33920, #18983, #14286, #34964, #26322, #38668, #30513 ),
 ( #30253, #22389, #38393, #2492, #34445, #27872, #24176, #11919, #27618 ),
 ( #361, #27361, #114, #11399, #43368, #43624, #43875, #7972, #31794 ),
 ( #36250, #40199, #19245, #47311, #3792, #23414, #15325, #7202, #31278 ),
 ( #43111, #23157, #39435, #39174, #3269, #35227, #4287, #23670, #23922 ) ),
 .UNSPECIFIED., .F., .F., .F.,
 ( 4, 2, 2, 2, 2, 2, 2, 2, 2, 4 ),
 ( 4, 1, 1, 1, 1, 1, 4 ),
 ( -1.826192301619919967, -1.664708266399350212, -1.413116924480830150, -1.141370188512450090, -0.9130961508099619817, -0.7989591319587170393, -0.6163399017967240434, -0.3681920442903470203, -0.1161770322012310036, 0.000000000000000000 ),
 ( 0.000000000000000000, 0.1666666666666670182, 0.3333333333333329818, 0.5000000000000000000, 0.6666666666666670737, 0.8333333333333330373, 1.000000000000000000 ),
 .UNSPECIFIED. ) ;
#25791=CARTESIAN_POINT ( 'NONE',  ( 64.43108017310198932, 0.9486745332807529074, -60.92803123004440380 ) ) ;
#25811=ORIENTED_EDGE ( 'NONE', *, *, #31664, .T. ) ;
#25828=CARTESIAN_POINT ( 'NONE',  ( 64.62407509413539231, 1.313826662893059938, -70.30919366152539851 ) ) ;
#25840=CARTESIAN_POINT ( 'NONE',  ( 63.35681832276381442, 1.325839985408290067, -68.86912414701170349 ) ) ;
#25885=EDGE_LOOP ( 'NONE', ( #16026, #4818, #12948, #11400 ) ) ;
#25925=CARTESIAN_POINT ( 'NONE',  ( 64.83879995576869248, 1.326134026835569912, -60.90937915352040477 ) ) ;
#25932=CARTESIAN_POINT ( 'NONE',  ( 72.73458218292580568, 1.393731187554809958, -68.81053500035210391 ) ) ;
#25934=CARTESIAN_POINT ( 'NONE',  ( 73.18782247527531126, 0.8859637708054489691, -62.41593972647849853 ) ) ;
#25938=CARTESIAN_POINT ( 'NONE',  ( 71.40893329644849530, 0.8879664753683469414, -60.62259972594619484 ) ) ;
#25940=CARTESIAN_POINT ( 'NONE',  ( 64.78392625511199299, 1.096932441169210071, -70.58143231363629866 ) ) ;
#25965=VERTEX_POINT ( 'NONE', #50982 ) ;
#25988=CARTESIAN_POINT ( 'NONE',  ( 63.20250508406000023, 1.096932441169210071, -62.29998885741579784 ) ) ;
#26000=CARTESIAN_POINT ( 'NONE',  ( 63.62896973943209389, 1.416241615474740145, -69.07296579632759403 ) ) ;
#26005=CARTESIAN_POINT ( 'NONE',  ( 72.71069314568710240, 1.377110276564839975, -62.16153651468360408 ) ) ;
#26017=CARTESIAN_POINT ( 'NONE',  ( 63.54731047306190561, 1.396834109478129804, -62.44999999999999574 ) ) ;
#26018=ORIENTED_EDGE ( 'NONE', *, *, #47852, .F. ) ;
#26021=EDGE_CURVE ( 'NONE', #11422, #6409, #46188, .T. ) ;
#26042=CARTESIAN_POINT ( 'NONE',  ( 72.64733618323120368, 1.408710407022059963, -69.13189173240590435 ) ) ;
#26048=CARTESIAN_POINT ( 'NONE',  ( 64.95360084570988590, 1.395196698723379924, -70.24366017557039754 ) ) ;
#26059=CARTESIAN_POINT ( 'NONE',  ( 63.83199809114920242, 1.060191324942699964, -61.46728771041559725 ) ) ;
#26097=CARTESIAN_POINT ( 'NONE',  ( 64.93393739769619799, 1.396834109478129804, -70.23662692463440749 ) ) ;
#26106=CARTESIAN_POINT ( 'NONE',  ( 63.46249669555339779, 1.383767307422960169, -68.70744520365728647 ) ) ;
#26117=CARTESIAN_POINT ( 'NONE',  ( 71.42298070439039748, 0.9242073871622918935, -70.66822101033309877 ) ) ;
#26125=CARTESIAN_POINT ( 'NONE',  ( 71.47612964547808190, 0.8925687589132609290, -70.63296852923029689 ) ) ;
#26140=CARTESIAN_POINT ( 'NONE',  ( 64.43393739769679485, 11.38381105532070059, -68.84999999999999432 ) ) ;
#26161=EDGE_CURVE ( 'NONE', #4963, #10362, #14373, .T. ) ;
#26167=CARTESIAN_POINT ( 'NONE',  ( 65.16374186055298878, 1.338092079250050137, -60.76305085381149951 ) ) ;
#26192=CARTESIAN_POINT ( 'NONE',  ( 64.78711365736010919, 1.264121749638659864, -60.84994802006399794 ) ) ;
#26196=CARTESIAN_POINT ( 'NONE',  ( 73.00002125581650603, 1.102139304147779830, -69.09899266709390986 ) ) ;
#26198=CARTESIAN_POINT ( 'NONE',  ( 72.79634974714259954, 1.384378348444520013, -62.56683295884919715 ) ) ;
#26204=CARTESIAN_POINT ( 'NONE',  ( 65.07649219403899110, 1.383767307422960169, -70.32144070214289400 ) ) ;
#26213=TOROIDAL_SURFACE ( 'NONE', #46326, 5.500000000000000000, 0.5000000000000000000 ) ;
#26219=DIRECTION ( 'NONE',  ( 0.7071067811865475727, 0.000000000000000000, -0.7071067811865475727 ) ) ;
#26234=EDGE_CURVE ( 'NONE', #34442, #34264, #4304, .T. ) ;
#26244=PLANE ( 'NONE',  #8786 ) ;
#26267=FACE_OUTER_BOUND ( 'NONE', #181, .T. ) ;
#26280=CARTESIAN_POINT ( 'NONE',  ( 63.46018632244250313, 1.384447124000270035, -68.59133994763901399 ) ) ;
#26285=ORIENTED_EDGE ( 'NONE', *, *, #43084, .F. ) ;
#26295=ADVANCED_FACE ( 'NONE', ( #42535 ), #2694, .T. ) ;
#26303=DIRECTION ( 'NONE',  ( 1.000000000000000000, 0.000000000000000000, 0.000000000000000000 ) ) ;
#26311=CARTESIAN_POINT ( 'NONE',  ( 65.27736602627911111, 1.383811055320669947, -70.34999999999999432 ) ) ;
#26312=ADVANCED_FACE ( 'NONE', ( #48006 ), #44065, .T. ) ;
#26322=CARTESIAN_POINT ( 'NONE',  ( 63.43155684671108929, 1.056975075120689889, -61.93355797292380061 ) ) ;
#26335=DIRECTION ( 'NONE',  ( 1.000000000000000000, 0.000000000000000000, 0.000000000000000000 ) ) ;
#26351=CARTESIAN_POINT ( 'NONE',  ( 64.80088823274410004, 1.308647200627879981, -70.40208447574109130 ) ) ;
#26360=CARTESIAN_POINT ( 'NONE',  ( 63.49266932922240159, 1.386446979194299933, -68.79214934801569825 ) ) ;
#26371=CARTESIAN_POINT ( 'NONE',  ( 71.36299175555980412, 1.264791438333819906, -70.51396375885850887 ) ) ;
#26404=ORIENTED_EDGE ( 'NONE', *, *, #11230, .F. ) ;
#26424=CARTESIAN_POINT ( 'NONE',  ( 65.06933737855371191, 1.383922910988889976, -60.98106092919370269 ) ) ;
#26456=CARTESIAN_POINT ( 'NONE',  ( 72.76779797359338886, 1.388189907116970101, -62.58632377286669879 ) ) ;
#26464=CARTESIAN_POINT ( 'NONE',  ( 64.97085660027880749, 1.369719003397489976, -70.35226930031740267 ) ) ;
#26508=CARTESIAN_POINT ( 'NONE',  ( 72.33393739769618946, 1.883811055320669947, -68.84999999999999432 ) ) ;
#26520=CARTESIAN_POINT ( 'NONE',  ( 71.34180821298970443, 0.9214125008369580261, -60.57945272938810177 ) ) ;
#26522=CARTESIAN_POINT ( 'NONE',  ( 72.76657796014310975, 1.245299373075410054, -61.97143377409609855 ) ) ;
#26528=ADVANCED_FACE ( 'NONE', ( #40107 ), #1050, .T. ) ;
#26542=EDGE_LOOP ( 'NONE', ( #49259, #16184, #45831, #42499, #557, #12311 ) ) ;
#26546=CARTESIAN_POINT ( 'NONE',  ( 0.000000000000000000, 0.000000000000000000, 0.000000000000000000 ) ) ;
#26551=ADVANCED_FACE ( 'NONE', ( #4984 ), #12859, .T. ) ;
#26554=DIRECTION ( 'NONE',  ( 0.000000000000000000, 1.000000000000000000, 0.000000000000000000 ) ) ;
#26571=DIRECTION ( 'NONE',  ( -0.5818181818182643905, 0.000000000000000000, 0.8133188816852151559 ) ) ;
#26578=CARTESIAN_POINT ( 'NONE',  ( 63.97507082502400522, 1.443019669817199979, -61.62767282824479764 ) ) ;
#26587=EDGE_CURVE ( 'NONE', #17335, #9073, #25243, .T. ) ;
#26606=DIRECTION ( 'NONE',  ( 0.000000000000000000, 0.000000000000000000, -1.000000000000000000 ) ) ;
#26613=CARTESIAN_POINT ( 'NONE',  ( 64.73247919242599835, 1.309849225219359869, -70.36735971887151209 ) ) ;
#26620=CARTESIAN_POINT ( 'NONE',  ( 71.57216560976189612, 1.132579237369250036, -70.50812303354520338 ) ) ;
#26625=CARTESIAN_POINT ( 'NONE',  ( 63.38363568028490391, 1.325841671674429900, -68.92527065596381419 ) ) ;
#26633=CARTESIAN_POINT ( 'NONE',  ( 71.38783905025809418, 1.187237555532410171, -70.57991217294409125 ) ) ;
#26678=CARTESIAN_POINT ( 'NONE',  ( 64.88003574513449223, 1.187237555532410171, -60.72008782705600538 ) ) ;
#26712=CARTESIAN_POINT ( 'NONE',  ( 73.01642658308999501, 0.9425424353906030062, -69.13730826794480322 ) ) ;
#26714=CARTESIAN_POINT ( 'NONE',  ( 72.82889308507860449, 1.369976237678190101, -62.46883854029779570 ) ) ;
#26724=VERTEX_POINT ( 'NONE', #2606 ) ;
#26746=CIRCLE ( 'NONE', #51040, 0.5000000000000004441 ) ;
#26755=EDGE_CURVE ( 'NONE', #48585, #20803, #46590, .T. ) ;
#26782=CARTESIAN_POINT ( 'NONE',  ( 71.27241355379879906, 0.9209567800143640959, -60.53623002923360730 ) ) ;
#26784=CARTESIAN_POINT ( 'NONE',  ( 72.92115325010770732, 1.229987811083100180, -62.21316185480839778 ) ) ;
#26795=ORIENTED_EDGE ( 'NONE', *, *, #26021, .T. ) ;
#26826=CARTESIAN_POINT ( 'NONE',  ( 68.13393739769620083, 1.383811055320669947, -65.65000000000000568 ) ) ;
#26846=CARTESIAN_POINT ( 'NONE',  ( 63.66432091401989624, 1.390572245144690022, -61.96641623988760017 ) ) ;
#26850=CARTESIAN_POINT ( 'NONE',  ( 73.15787026839889506, 0.9945465939392541532, -68.91635399151641650 ) ) ;
#26856=ORIENTED_EDGE ( 'NONE', *, *, #34670, .F. ) ;
#26864=CIRCLE ( 'NONE', #32669, 6.000000000000005329 ) ;
#26878=CARTESIAN_POINT ( 'NONE',  ( 64.70947553222160309, 1.229745425602249975, -70.44444055526530235 ) ) ;
#26886=CARTESIAN_POINT ( 'NONE',  ( 71.81250362359278938, 1.245299373074770122, -70.28264056245218683 ) ) ;
#26895=CARTESIAN_POINT ( 'NONE',  ( 63.23867883281550206, 0.9065823421260970072, -69.11945805671260246 ) ) ;
#26903=CARTESIAN_POINT ( 'NONE',  ( 71.48629080024771554, 0.9281439705311279598, -70.62613840402418930 ) ) ;
#26912=EDGE_CURVE ( 'NONE', #32793, #4963, #3898, .T. ) ;
#26925=CARTESIAN_POINT ( 'NONE',  ( 63.93393739769609141, 10.88381105532060111, -68.84999999999999432 ) ) ;
#26951=CARTESIAN_POINT ( 'NONE',  ( 64.79174514991440503, 0.8925687589132640376, -60.66703147076970737 ) ) ;
#26964=AXIS2_PLACEMENT_3D ( 'NONE', #47882, #39243, #43942 ) ;
#26982=CARTESIAN_POINT ( 'NONE',  ( 72.76128204928129151, 1.388313565858570131, -68.83005089568659685 ) ) ;
#26984=CARTESIAN_POINT ( 'NONE',  ( 72.72056432233058842, 1.396834109478120034, -62.44999999999999574 ) ) ;
#27022=CIRCLE ( 'NONE', #31192, 0.4999999999999865663 ) ;
#27049=CARTESIAN_POINT ( 'NONE',  ( 71.41555540048999262, 0.9948723650351710690, -60.63592931576840073 ) ) ;
#27051=CARTESIAN_POINT ( 'NONE',  ( 72.36601468635269896, 1.348268854479560019, -61.55068500424459899 ) ) ;
#27061=CARTESIAN_POINT ( 'NONE',  ( 63.44650199127489998, 1.383928098097870096, -68.54761322559109260 ) ) ;
#27073=CARTESIAN_POINT ( 'NONE',  ( 63.03407832914049891, 0.8840451408750739093, -62.48896739026420022 ) ) ;
#27086=ORIENTED_EDGE ( 'NONE', *, *, #36261, .F. ) ;
#27087=DIRECTION ( 'NONE',  ( 1.000000000000000000, 0.000000000000000000, 0.000000000000000000 ) ) ;
#27094=CARTESIAN_POINT ( 'NONE',  ( 63.00666467042349694, 0.8838110553206759423, -62.53374032209040223 ) ) ;
#27108=CARTESIAN_POINT ( 'NONE',  ( 63.60923929913089836, 1.000506532485009981, -61.70853630543769697 ) ) ;
#27111=CARTESIAN_POINT ( 'NONE',  ( 64.43393739769619799, 11.38381105532070059, -62.44999999999999574 ) ) ;
#27112=CARTESIAN_POINT ( 'NONE',  ( 73.15966969277990017, 1.196343736543249880, -68.73232403594570883 ) ) ;
#27120=ORIENTED_EDGE ( 'NONE', *, *, #9652, .F. ) ;
#27129=DIRECTION ( 'NONE',  ( 1.000000000000000000, 0.000000000000000000, 0.000000000000000000 ) ) ;
#27144=ORIENTED_EDGE ( 'NONE', *, *, #23461, .F. ) ;
#27147=CARTESIAN_POINT ( 'NONE',  ( 72.04719216831770723, 1.025918948571509892, -70.19928925136699149 ) ) ;
#27153=CARTESIAN_POINT ( 'NONE',  ( 63.65233837787879878, 1.010052234904250001, -69.64061050479490689 ) ) ;
#27158=CARTESIAN_POINT ( 'NONE',  ( 71.26748243800840044, 1.369544300367010026, -70.36404682606520566 ) ) ;
#27163=DIRECTION ( 'NONE',  ( 0.000000000000000000, 1.000000000000000000, 0.000000000000000000 ) ) ;
#27174=CARTESIAN_POINT ( 'NONE',  ( 71.33393739766809460, 1.883811055273910018, -68.84999999991929087 ) ) ;
#27177=ORIENTED_EDGE ( 'NONE', *, *, #6654, .T. ) ;
#27204=CARTESIAN_POINT ( 'NONE',  ( 64.90740703336619788, 0.9940423591679348192, -60.60059430635039490 ) ) ;
#27211=CARTESIAN_POINT ( 'NONE',  ( 71.83679462228410273, 0.9486745332793850016, -70.37196876996070216 ) ) ;
#27233=CARTESIAN_POINT ( 'NONE',  ( 72.99348972288790094, 1.187296498006439993, -62.27829692513819992 ) ) ;
#27239=CARTESIAN_POINT ( 'NONE',  ( 64.85866674173250601, 1.325841671674429900, -70.40030171741140919 ) ) ;
#27284=DIRECTION ( 'NONE',  ( 1.000000000000000000, 0.000000000000000000, 0.000000000000000000 ) ) ;
#27289=CARTESIAN_POINT ( 'NONE',  ( 63.29941945011370308, 1.188860127980290171, -62.23803121388370130 ) ) ;
#27302=CARTESIAN_POINT ( 'NONE',  ( 71.09849264842429761, 1.384887413063060180, -60.98363600610959878 ) ) ;
#27304=CARTESIAN_POINT ( 'NONE',  ( 72.32557311402300115, 1.409766894666529824, -61.59342351728570009 ) ) ;
#27328=CARTESIAN_POINT ( 'NONE',  ( 63.15932386229340523, 0.8936201581567960739, -62.29538467389520662 ) ) ;
#27341=ORIENTED_EDGE ( 'NONE', *, *, #35012, .T. ) ;
#27353=CARTESIAN_POINT ( 'NONE',  ( 64.43108017310198932, 0.9486745332807529074, -60.92803123004440380 ) ) ;
#27361=CARTESIAN_POINT ( 'NONE',  ( 63.54193824524709555, 1.394012070864489861, -62.35876656057820355 ) ) ;
#27365=CARTESIAN_POINT ( 'NONE',  ( 73.02275056366489991, 1.266538207494809942, -68.83138049123679991 ) ) ;
#27381=EDGE_LOOP ( 'NONE', ( #8439, #48703, #18932, #30840 ) ) ;
#27388=CARTESIAN_POINT ( 'NONE',  ( 72.82137280411760116, 1.383928098097870096, -62.75238677440889035 ) ) ;
#27401=CARTESIAN_POINT ( 'NONE',  ( 71.65899916879679665, 1.412342135319139880, -70.14294384383438796 ) ) ;
#27414=VERTEX_POINT ( 'NONE', #9514 ) ;
#27456=CARTESIAN_POINT ( 'NONE',  ( 71.33393739769650210, 1.396834109478129804, -70.23662692463440749 ) ) ;
#27461=CARTESIAN_POINT ( 'NONE',  ( 65.01767019485720311, 1.328674444234379859, -60.82574149480920056 ) ) ;
#27492=CARTESIAN_POINT ( 'NONE',  ( 73.07318775143950518, 0.8986939045430379913, -62.24348040161360274 ) ) ;
#27494=DIRECTION ( 'NONE',  ( -0.7071067811865475727, 0.000000000000000000, -0.7071067811865475727 ) ) ;
#27497=VECTOR ( 'NONE', #3501, 1000.000000000000000 ) ;
#27499=ORIENTED_EDGE ( 'NONE', *, *, #43713, .T. ) ;
#27528=TOROIDAL_SURFACE ( 'NONE', #19199, 5.500000000000000000, 0.5000000000000000000 ) ;
#27536=CARTESIAN_POINT ( 'NONE',  ( 63.42952807919409253, 1.382830464309369844, -68.61079447352989291 ) ) ;
#27556=CARTESIAN_POINT ( 'NONE',  ( 71.15687762518609816, 1.370937308141420230, -60.89332811547459556 ) ) ;
#27558=CARTESIAN_POINT ( 'NONE',  ( 72.22406619500640090, 1.409763019284739904, -61.49193411207189541 ) ) ;
#27573=DIRECTION ( 'NONE',  ( 0.000000000000000000, 0.000000000000000000, 1.000000000000000000 ) ) ;
#27606=CARTESIAN_POINT ( 'NONE',  ( 63.18512348867459849, 1.274277262446050107, -62.58867475943009850 ) ) ;
#27611=DIRECTION ( 'NONE',  ( -1.000000000000000000, 0.000000000000000000, 0.000000000000000000 ) ) ;
#27618=CARTESIAN_POINT ( 'NONE',  ( 63.38217364139809007, 0.9405967369938039724, -61.98545004926849344 ) ) ;
#27621=CARTESIAN_POINT ( 'NONE',  ( 68.13393739769620083, -42.11618894467930119, -71.65000000000000568 ) ) ;
#27622=CARTESIAN_POINT ( 'NONE',  ( 73.24758132965840218, 0.8838110553206759423, -68.78868353141480441 ) ) ;
#27630=ORIENTED_EDGE ( 'NONE', *, *, #45187, .F. ) ;
#27649=DIRECTION ( 'NONE',  ( 0.000000000000000000, 0.000000000000000000, 1.000000000000000000 ) ) ;
#27658=CARTESIAN_POINT ( 'NONE',  ( 71.70128097442669457, 1.382578538659040124, -70.18625692817499839 ) ) ;
#27664=CARTESIAN_POINT ( 'NONE',  ( 63.22228946811700467, 1.003508719580009867, -69.08444824154609876 ) ) ;
#27667=CARTESIAN_POINT ( 'NONE',  ( 63.95040967837099544, 1.031857118852239852, -69.95114096137160686 ) ) ;
#27703=CARTESIAN_POINT ( 'NONE',  ( 63.93393739769594930, 10.88381105532010551, -61.44999999999983231 ) ) ;
#27704=LINE ( 'NONE', #51316, #37636 ) ;
#27730=CARTESIAN_POINT ( 'NONE',  ( 72.88570115400600002, 0.9405967369906039766, -69.31454995071669600 ) ) ;
#27754=CARTESIAN_POINT ( 'NONE',  ( 73.05322604375929529, 1.097545367735389910, -62.28124518314879765 ) ) ;
#27762=CARTESIAN_POINT ( 'NONE',  ( 64.97340239734430156, 1.393731187554809958, -70.25064478522961053 ) ) ;
#27787=CIRCLE ( 'NONE', #30327, 6.000000000000005329 ) ;
#27791=ADVANCED_FACE ( 'NONE', ( #31970 ), #39355, .F. ) ;
#27796=CARTESIAN_POINT ( 'NONE',  ( 63.15706468848460275, 1.190292248953970011, -68.82164347790129000 ) ) ;
#27815=CARTESIAN_POINT ( 'NONE',  ( 71.25658036288379549, 1.391252479931859964, -61.03617692120100457 ) ) ;
#27817=CARTESIAN_POINT ( 'NONE',  ( 72.49434596780521645, 1.056850087111250058, -61.52764073002409617 ) ) ;
#27821=ORIENTED_EDGE ( 'NONE', *, *, #22096, .F. ) ;
#27829=ORIENTED_EDGE ( 'NONE', *, *, #41647, .F. ) ;
#27836=EDGE_CURVE ( 'NONE', #51003, #34442, #47990, .T. ) ;
#27841=CARTESIAN_POINT ( 'NONE',  ( 63.06393505168800573, 0.8850831926798620186, -62.44126551166660022 ) ) ;
#27847=CARTESIAN_POINT ( 'NONE',  ( 63.75227860486319997, 1.439518482450359960, -69.32544932539248350 ) ) ;
#27861=CARTESIAN_POINT ( 'NONE',  ( 63.15863832053869942, 1.096036836948800053, -62.36911566638589477 ) ) ;
#27865=CARTESIAN_POINT ( 'NONE',  ( 63.71314823352740575, 1.019773975906300034, -61.59278770926519542 ) ) ;
#27872=CARTESIAN_POINT ( 'NONE',  ( 63.39226695650439325, 1.145379646619560043, -62.03974443815909723 ) ) ;
#27913=CARTESIAN_POINT ( 'NONE',  ( 72.51712974994539707, 1.428542319231139945, -69.37578972296869040 ) ) ;
#27915=FILL_AREA_STYLE_COLOUR ( '', #18884 ) ;
#27927=CARTESIAN_POINT ( 'NONE',  ( 71.46077416446640029, 1.263823323415670163, -70.46116989902598959 ) ) ;
#27952=CARTESIAN_POINT ( 'NONE',  ( 63.10653712364229762, 0.8879664753683499390, -68.92499589875220067 ) ) ;
#27954=CARTESIAN_POINT ( 'NONE',  ( 64.99525386628130263, 0.8838110553206740549, -70.76364393196210756 ) ) ;
#27996=EDGE_LOOP ( 'NONE', ( #25811, #30437, #44826, #37046, #11559 ) ) ;
#28002=CARTESIAN_POINT ( 'NONE',  ( 64.93393739769619799, 10.88381105532070059, -68.84999999999999432 ) ) ;
#28019=DIRECTION ( 'NONE',  ( 1.000000000000000000, 0.000000000000000000, 0.000000000000000000 ) ) ;
#28041=CARTESIAN_POINT ( 'NONE',  ( 63.11000452699359897, 0.9945465939392450494, -68.91635399151641650 ) ) ;
#28055=CARTESIAN_POINT ( 'NONE',  ( 71.09849264842429761, 1.384887413063060180, -70.31636399389039127 ) ) ;
#28064=CARTESIAN_POINT ( 'NONE',  ( 71.57861930639089110, 0.9369374701296400154, -60.73727483855509490 ) ) ;
#28066=CARTESIAN_POINT ( 'NONE',  ( 72.35687375404550892, 1.441354674475110009, -61.69957420032910278 ) ) ;
#28068=CARTESIAN_POINT ( 'NONE',  ( 65.02843368015321346, 1.270877794983130027, -70.57718306158270138 ) ) ;
#28072=CARTESIAN_POINT ( 'NONE',  ( 72.33393739769906006, 10.88381105532050164, -61.44999999999760831 ) ) ;
#28089=LINE ( 'NONE', #40674, #29204 ) ;
#28111=CARTESIAN_POINT ( 'NONE',  ( 63.11986671346460298, 0.9948723650351710690, -62.36838199720629916 ) ) ;
#28142=VERTEX_POINT ( 'NONE', #28956 ) ;
#28164=CARTESIAN_POINT ( 'NONE',  ( 72.29500244193140190, 1.200163167270710041, -69.93714187953969486 ) ) ;
#28178=CARTESIAN_POINT ( 'NONE',  ( 64.64302830678670375, 0.9098571636355720083, -60.77008670988870165 ) ) ;
#28180=CARTESIAN_POINT ( 'NONE',  ( 71.40920805366010882, 1.325841671674429900, -70.40030171741129550 ) ) ;
#28187=CARTESIAN_POINT ( 'NONE',  ( 71.25019707560589666, 0.8838110553206759423, -70.77727272727270247 ) ) ;
#28202=CARTESIAN_POINT ( 'NONE',  ( 71.25019707560579718, 0.8838110553206759423, -60.52272727272730179 ) ) ;
#28210=FACE_OUTER_BOUND ( 'NONE', #17188, .T. ) ;
#28243=VERTEX_POINT ( 'NONE', #48114 ) ;
#28268=CARTESIAN_POINT ( 'NONE',  ( 71.42967573711919727, 1.404650034021559968, -70.20402782815220633 ) ) ;
#28276=DIRECTION ( 'NONE',  ( -0.8545454545454587159, 0.000000000000000000, -0.5193766129849277657 ) ) ;
#28295=CARTESIAN_POINT ( 'NONE',  ( 63.04573361361109818, 1.102581332775300016, -68.74251431096891451 ) ) ;
#28312=CARTESIAN_POINT ( 'NONE',  ( 71.03155062328740144, 1.383928098097870096, -70.33743540642140601 ) ) ;
#28320=CARTESIAN_POINT ( 'NONE',  ( 71.41841232404479456, 1.186701509386330011, -60.73797667709639825 ) ) ;
#28322=CARTESIAN_POINT ( 'NONE',  ( 71.64275587478520890, 1.313759828078409964, -60.99019652856610207 ) ) ;
#28325=CARTESIAN_POINT ( 'NONE',  ( 64.99525386628140211, 0.8838110553206759423, -70.76364393196210756 ) ) ;
#28334=ORIENTED_EDGE ( 'NONE', *, *, #20561, .T. ) ;
#28341=ORIENTED_EDGE ( 'NONE', *, *, #35012, .F. ) ;
#28345=ADVANCED_FACE ( 'NONE', ( #6166 ), #16423, .T. ) ;
#28353=CARTESIAN_POINT ( 'NONE',  ( 63.56282646728049457, 1.400446387219270061, -68.89724194849250694 ) ) ;
#28367=CARTESIAN_POINT ( 'NONE',  ( 63.04027743911709791, 0.9947083095259759977, -62.49453424214399888 ) ) ;
#28371=FACE_OUTER_BOUND ( 'NONE', #48910, .T. ) ;
#28373=CARTESIAN_POINT ( 'NONE',  ( 71.98371235365300436, 1.451792515613489876, -61.38183652702590365 ) ) ;
#28376=CARTESIAN_POINT ( 'NONE',  ( 64.64302830678678902, 0.9098571636355680115, -60.77008670988870165 ) ) ;
#28378=DIRECTION ( 'NONE',  ( 0.000000000000000000, -1.000000000000000000, 0.000000000000000000 ) ) ;
#28399=CARTESIAN_POINT ( 'NONE',  ( 68.13393739769620083, -42.11618894467930119, -71.15000000000000568 ) ) ;
#28426=CARTESIAN_POINT ( 'NONE',  ( 72.66187716250549045, 1.030858001319959971, -69.58776317408900525 ) ) ;
#28433=CARTESIAN_POINT ( 'NONE',  ( 71.33393739769628894, 1.883811055320669947, -61.44999999999999574 ) ) ;
#28439=CARTESIAN_POINT ( 'NONE',  ( 64.59570122278479687, 0.9170823515331248954, -60.80394275157770068 ) ) ;
#28455=CIRCLE ( 'NONE', #39334, 6.000000000000005329 ) ;
#28509=CARTESIAN_POINT ( 'NONE',  ( 65.16938214696820353, 1.384887413063060180, -60.98363600610959878 ) ) ;
#28558=CARTESIAN_POINT ( 'NONE',  ( 63.18711801607420142, 1.188042061556800144, -68.87465088918141021 ) ) ;
#28572=CARTESIAN_POINT ( 'NONE',  ( 71.12477309692330607, 1.336371993404949832, -70.52842906692660563 ) ) ;
#28576=CARTESIAN_POINT ( 'NONE',  ( 73.13683269167130163, 0.9254905997697669973, -68.96226957534490509 ) ) ;
#28582=CARTESIAN_POINT ( 'NONE',  ( 71.45393474093610564, 0.9259537755896120048, -60.65222959644560063 ) ) ;
#28584=CARTESIAN_POINT ( 'NONE',  ( 71.64047750585169183, 1.027568165751340024, -60.79177686748120379 ) ) ;
#28585=DIRECTION ( 'NONE',  ( -1.000000000000000000, 0.000000000000000000, 0.000000000000000000 ) ) ;
#28586=CARTESIAN_POINT ( 'NONE',  ( 65.03067915409710054, 1.194703186106680137, -70.66446396659920026 ) ) ;
#28627=CARTESIAN_POINT ( 'NONE',  ( 63.11947343109709863, 1.194703186106690129, -62.54674175640080591 ) ) ;
#28632=CARTESIAN_POINT ( 'NONE',  ( 72.17449546179830122, 1.458407608744489936, -61.54081785568290286 ) ) ;
#28661=DIRECTION ( 'NONE',  ( 1.000000000000000000, 0.000000000000000000, 0.000000000000000000 ) ) ;
#28682=CARTESIAN_POINT ( 'NONE',  ( 72.47840029513230320, 1.274155933524790063, -69.69643145772678849 ) ) ;
#28696=CARTESIAN_POINT ( 'NONE',  ( 64.45046735905599178, 1.051325075268649822, -60.92209273815699788 ) ) ;
#28744=CARTESIAN_POINT ( 'NONE',  ( 64.28413441608979895, 1.451794159057709921, -69.91814348332408713 ) ) ;
#28747=ORIENTED_EDGE ( 'NONE', *, *, #11532, .T. ) ;
#28789=DIRECTION ( 'NONE',  ( 0.000000000000000000, -1.000000000000000000, 0.000000000000000000 ) ) ;
#28820=CARTESIAN_POINT ( 'NONE',  ( 63.13104210372130609, 0.9254905997697669973, -68.96226957534490509 ) ) ;
#28832=CARTESIAN_POINT ( 'NONE',  ( 71.09473187122610227, 1.382830464309369844, -70.35440931850220636 ) ) ;
#28840=CARTESIAN_POINT ( 'NONE',  ( 72.99790115655470402, 1.264791438333819906, -68.87905435786350949 ) ) ;
#28845=CARTESIAN_POINT ( 'NONE',  ( 71.23034918703520191, 1.369664981662519931, -60.92138556078450051 ) ) ;
#28847=CARTESIAN_POINT ( 'NONE',  ( 71.43600178900840092, 1.367958924391370124, -60.98859505255219915 ) ) ;
#28849=CARTESIAN_POINT ( 'NONE',  ( 65.21688447373020381, 1.383136297697689976, -70.36878149631539259 ) ) ;
#28884=FACE_OUTER_BOUND ( 'NONE', #35093, .T. ) ;
#28890=CARTESIAN_POINT ( 'NONE',  ( 63.25085271618998917, 1.186614556332920234, -62.31696408872340243 ) ) ;
#28895=CARTESIAN_POINT ( 'NONE',  ( 72.46078431608199821, 1.446932438105759999, -61.88285690311300158 ) ) ;
#28899=CARTESIAN_POINT ( 'NONE',  ( 64.70533732122679282, 1.100585178972000033, -60.77016257896750062 ) ) ;
#28944=CARTESIAN_POINT ( 'NONE',  ( 72.40605974471309025, 1.033004162168289941, -69.86315739208521336 ) ) ;
#28956=CARTESIAN_POINT ( 'NONE',  ( 64.93393739769619799, 1.530257664727400879, -61.30355339059330078 ) ) ;
#28961=CARTESIAN_POINT ( 'NONE',  ( 64.56659382095870114, 1.382578538659519962, -61.11374307182889254 ) ) ;
#28999=AXIS2_PLACEMENT_3D ( 'NONE', #41291, #33927, #37361 ) ;
#29007=CARTESIAN_POINT ( 'NONE',  ( 63.95040967837109491, 1.031857118852239852, -69.95114096137160686 ) ) ;
#29039=CARTESIAN_POINT ( 'NONE',  ( 72.76396860142250489, 1.388715606738730068, -68.72506404892941134 ) ) ;
#29053=CARTESIAN_POINT ( 'NONE',  ( 72.24311954201340313, 1.458407608744489936, -69.69055806410209186 ) ) ;
#29055=CARTESIAN_POINT ( 'NONE',  ( 63.48441347673288959, 1.386342629514219826, -62.63353618948930546 ) ) ;
#29077=CARTESIAN_POINT ( 'NONE',  ( 71.29447239804829906, 1.393731187554809958, -61.04935521477050031 ) ) ;
#29095=CARTESIAN_POINT ( 'NONE',  ( 71.34267188602969156, 0.8850831926798630178, -70.72000234600830026 ) ) ;
#29101=CARTESIAN_POINT ( 'NONE',  ( 72.82889308507860449, 1.369976237678180109, -68.83116145970220146 ) ) ;
#29104=CARTESIAN_POINT ( 'NONE',  ( 73.23405285996879854, 0.9209334348186318797, -62.48938310929649731 ) ) ;
#29108=CARTESIAN_POINT ( 'NONE',  ( 72.12565519439380068, 1.270920007605170099, -61.25800542990180730 ) ) ;
#29111=CARTESIAN_POINT ( 'NONE',  ( 65.19851456808879675, 1.374300485541529948, -70.43861994117489189 ) ) ;
#29150=CARTESIAN_POINT ( 'NONE',  ( 63.40811083734029552, 1.369613126987619944, -62.54642937019949755 ) ) ;
#29151=DIRECTION ( 'NONE',  ( 0.000000000000000000, 1.000000000000000000, 0.000000000000000000 ) ) ;
#29155=EDGE_CURVE ( 'NONE', #50553, #16762, #16734, .T. ) ;
#29160=EDGE_CURVE ( 'NONE', #51314, #309, #35658, .T. ) ;
#29200=CARTESIAN_POINT ( 'NONE',  ( 73.10855093309899644, 0.8936201581567920771, -62.29538467389520662 ) ) ;
#29204=VECTOR ( 'NONE', #37003, 1000.000000000000000 ) ;
#29206=FACE_OUTER_BOUND ( 'NONE', #42715, .T. ) ;
#29218=CARTESIAN_POINT ( 'NONE',  ( 64.07736091498190945, 1.409766894666529824, -61.45836428367329773 ) ) ;
#29235=ORIENTED_EDGE ( 'NONE', *, *, #21227, .T. ) ;
#29236=ORIENTED_EDGE ( 'NONE', *, *, #131, .F. ) ;
#29250=CIRCLE ( 'NONE', #8347, 0.5000000000000004441 ) ;
#29259=CARTESIAN_POINT ( 'NONE',  ( 72.94555459751978788, 0.9254890127240629205, -62.06507410682309711 ) ) ;
#29262=CARTESIAN_POINT ( 'NONE',  ( 64.27186769037609793, 1.261434405545410087, -70.14834382225429010 ) ) ;
#29268=CARTESIAN_POINT ( 'NONE',  ( 63.78749078828948882, 1.530257664727401767, -65.65000000000000568 ) ) ;
#29292=DIRECTION ( 'NONE',  ( 1.000000000000000000, 0.000000000000000000, 0.000000000000000000 ) ) ;
#29307=CARTESIAN_POINT ( 'NONE',  ( 70.99050876911339003, 1.383811055320669947, -70.34999999999999432 ) ) ;
#29315=DIRECTION ( 'NONE',  ( 0.000000000000000000, 0.000000000000000000, -1.000000000000000000 ) ) ;
#29329=TOROIDAL_SURFACE ( 'NONE', #46948, 5.500000000000000000, 0.5000000000000000000 ) ;
#29335=CARTESIAN_POINT ( 'NONE',  ( 64.99878011502339348, 1.099973129953850215, -60.58645605602389850 ) ) ;
#29340=CARTESIAN_POINT ( 'NONE',  ( 64.66447934098370354, 0.9065823421260940096, -60.75474143511929981 ) ) ;
#29345=ORIENTED_EDGE ( 'NONE', *, *, #18189, .T. ) ;
#29353=CARTESIAN_POINT ( 'NONE',  ( 71.45393474093620512, 0.9259537755896120048, -70.64777040355440363 ) ) ;
#29358=CARTESIAN_POINT ( 'NONE',  ( 73.12814476249489815, 0.9958340104639701318, -68.96201750760249638 ) ) ;
#29361=CARTESIAN_POINT ( 'NONE',  ( 72.85934862407960111, 1.383411777981069957, -62.75344103383148564 ) ) ;
#29366=CARTESIAN_POINT ( 'NONE',  ( 71.87288967509290671, 1.328802495349950208, -61.13208180354720156 ) ) ;
#29372=CARTESIAN_POINT ( 'NONE',  ( 64.80222656955079685, 0.9966178393190270324, -70.63122704464430512 ) ) ;
#29384=CYLINDRICAL_SURFACE ( 'NONE', #45432, 1.000000000000000888 ) ;
#29386=B_SPLINE_CURVE_WITH_KNOTS ( 'NONE', 3,
 ( #6757, #42136, #19049, #6235, #35024, #22711, #26125, #22191, #34511, #38201, #18270, #50775, #14865, #40007, #31859, #28187 ),
 .UNSPECIFIED., .F., .F.,
 ( 4, 2, 2, 2, 2, 2, 2, 4 ),
 ( -1.892930000000000094E-14, 0.07319275283554899092, 0.1391693187718359981, 0.1804046724820149994, 0.2061767685508769932, 0.2577209606886010085, 0.3401916681089590111, 0.4123535371017730267 ),
 .UNSPECIFIED. ) ;
#29399=CIRCLE ( 'NONE', #43640, 5.500000000000005329 ) ;
#29412=CARTESIAN_POINT ( 'NONE',  ( 63.32276749867028798, 1.263823323415670163, -62.32316323322979912 ) ) ;
#29419=PLANE ( 'NONE',  #3880 ) ;
#29421=CARTESIAN_POINT ( 'NONE',  ( 63.56282646728049457, 1.400446387219270061, -68.89724194849250694 ) ) ;
#29424=FACE_OUTER_BOUND ( 'NONE', #21675, .T. ) ;
#29465=CARTESIAN_POINT ( 'NONE',  ( 72.68863061175819951, 1.254613999359699861, -69.43746191119949174 ) ) ;
#29480=CARTESIAN_POINT ( 'NONE',  ( 64.06712595014920453, 1.275252243133929930, -61.32327465822529433 ) ) ;
#29488=CARTESIAN_POINT ( 'NONE',  ( 71.83393739769618946, 10.88381105532070059, -68.84999999999999432 ) ) ;
#29520=CARTESIAN_POINT ( 'NONE',  ( 63.78541443256050059, 1.197079622115780007, -69.74590901733688497 ) ) ;
#29528=LINE ( 'NONE', #29268, #35635 ) ;
#29548=CARTESIAN_POINT ( 'NONE',  ( 72.78346131865960444, 1.386342629514219826, -68.66646381051069170 ) ) ;
#29551=ADVANCED_FACE ( 'NONE', ( #40010 ), #4097, .T. ) ;
#29570=CARTESIAN_POINT ( 'NONE',  ( 68.13393739769620083, 0.8838110553206759423, -65.65000000000000568 ) ) ;
#29586=CARTESIAN_POINT ( 'NONE',  ( 65.05533261316259086, 1.330484379554840002, -60.80906431331560213 ) ) ;
#29598=ORIENTED_EDGE ( 'NONE', *, *, #48869, .F. ) ;
#29613=CARTESIAN_POINT ( 'NONE',  ( 73.11007580172049813, 0.9281439705311279598, -69.00235340255149197 ) ) ;
#29616=CARTESIAN_POINT ( 'NONE',  ( 73.19885236215881719, 0.9940695285616559795, -62.44811160372290004 ) ) ;
#29624=CARTESIAN_POINT ( 'NONE',  ( 64.79388653638659434, 0.9272522097097989358, -70.63440435907199344 ) ) ;
#29663=CARTESIAN_POINT ( 'NONE',  ( 63.32591849070559675, 1.327322800621349996, -62.49772215509980100 ) ) ;
#29671=AXIS2_PLACEMENT_3D ( 'NONE', #38694, #46042, #2785 ) ;
#29673=CARTESIAN_POINT ( 'NONE',  ( 63.28456881472469320, 0.9543419100865909721, -69.18369337885960135 ) ) ;
#29684=ORIENTED_EDGE ( 'NONE', *, *, #43084, .T. ) ;
#29707=AXIS2_PLACEMENT_3D ( 'NONE', #18693, #14769, #30737 ) ;
#29716=CARTESIAN_POINT ( 'NONE',  ( 73.02919596257699197, 0.9065823421260940096, -62.18054194328749418 ) ) ;
#29717=DIRECTION ( 'NONE',  ( 0.000000000000000000, 0.000000000000000000, 1.000000000000000000 ) ) ;
#29718=CARTESIAN_POINT ( 'NONE',  ( 73.01385068780759013, 0.9098571636355720083, -69.14090909090960224 ) ) ;
#29729=CARTESIAN_POINT ( 'NONE',  ( 64.71095929546520154, 1.416242794300709873, -61.14503753232310146 ) ) ;
#29741=EDGE_LOOP ( 'NONE', ( #17108, #233, #13367, #2972 ) ) ;
#29765=CARTESIAN_POINT ( 'NONE',  ( 63.94229026696169882, 1.409766646916870148, -69.70656394866479388 ) ) ;
#29777=CARTESIAN_POINT ( 'NONE',  ( 63.36539477273620236, 1.325715844996850024, -68.88725199158329815 ) ) ;
#29784=VERTEX_POINT ( 'NONE', #30424 ) ;
#29836=CARTESIAN_POINT ( 'NONE',  ( 64.95336252238109864, 1.097895768572089814, -60.61330028352099930 ) ) ;
#29841=CARTESIAN_POINT ( 'NONE',  ( 71.62484648860579739, 0.9098571636355720083, -60.77008670988870165 ) ) ;
#29849=VERTEX_POINT ( 'NONE', #30351 ) ;
#29857=CARTESIAN_POINT ( 'NONE',  ( 64.91441195039588763, 1.390806392144110060, -61.03748192468240319 ) ) ;
#29863=CARTESIAN_POINT ( 'NONE',  ( 73.08495881288720852, 1.096305581841150012, -68.96938879548969226 ) ) ;
#29865=CARTESIAN_POINT ( 'NONE',  ( 72.87088340658550578, 1.369885150286800135, -62.57510434557890733 ) ) ;
#29867=CARTESIAN_POINT ( 'NONE',  ( 71.31427394968270050, 1.395196698723390138, -61.05633982442969909 ) ) ;
#29872=CARTESIAN_POINT ( 'NONE',  ( 65.00039235738410071, 1.369544300367000034, -70.36404682606520566 ) ) ;
#29886=VECTOR ( 'NONE', #16513, 1000.000000000000000 ) ;
#29917=CARTESIAN_POINT ( 'NONE',  ( 63.46499832689001153, 1.383922910988889976, -62.58539998085741018 ) ) ;
#29920=DIRECTION ( 'NONE',  ( 0.000000000000000000, -1.000000000000000000, 0.000000000000000000 ) ) ;
#29927=CARTESIAN_POINT ( 'NONE',  ( 63.51710413059809213, 1.389801772588449946, -68.87277968851719834 ) ) ;
#29933=CARTESIAN_POINT ( 'NONE',  ( 72.60391569211400054, 1.424120032878380071, -62.14639092277510457 ) ) ;
#29963=EDGE_CURVE ( 'NONE', #51314, #48585, #37459, .T. ) ;
#29965=CARTESIAN_POINT ( 'NONE',  ( 68.13393739769620083, 0.8838110553206759423, -65.65000000000000568 ) ) ;
#29973=CARTESIAN_POINT ( 'NONE',  ( 72.88952751928479756, 0.9755120847786619143, -69.30957930923889876 ) ) ;
#29978=CARTESIAN_POINT ( 'NONE',  ( 65.11747358718560008, 1.386342629514219826, -70.29952392096339508 ) ) ;
#29986=CARTESIAN_POINT ( 'NONE',  ( 63.60599763288880837, 1.030858001320269945, -61.71223682590910187 ) ) ;
#29995=AXIS2_PLACEMENT_3D ( 'NONE', #40586, #4945, #20920 ) ;
#30013=LINE ( 'NONE', #14052, #3274 ) ;
#30020=LINE ( 'NONE', #9618, #47127 ) ;
#30024=CARTESIAN_POINT ( 'NONE',  ( 64.60839616882741154, 0.9151442779661249638, -70.50513874227569033 ) ) ;
#30036=CARTESIAN_POINT ( 'NONE',  ( 63.46499832688989784, 1.383922910988889976, -68.71460001914260829 ) ) ;
#30095=CARTESIAN_POINT ( 'NONE',  ( 65.23632417210509971, 1.383928098097870096, -60.96256459357869772 ) ) ;
#30123=CARTESIAN_POINT ( 'NONE',  ( 64.81933968820109726, 1.186515949276290227, -60.75583815301620660 ) ) ;
#30128=CARTESIAN_POINT ( 'NONE',  ( 72.98101631171969927, 1.187931651339009909, -69.04190732916428885 ) ) ;
#30130=CARTESIAN_POINT ( 'NONE',  ( 72.78346131865960444, 1.386342629514219826, -62.63353618948930546 ) ) ;
#30132=CARTESIAN_POINT ( 'NONE',  ( 71.37283554222209148, 1.371509258145880095, -60.97885864891310348 ) ) ;
#30136=CARTESIAN_POINT ( 'NONE',  ( 64.82950905750199411, 0.9955677559369519036, -70.64918477200470193 ) ) ;
#30173=EDGE_LOOP ( 'NONE', ( #20522, #12435, #38797, #5105 ) ) ;
#30197=CARTESIAN_POINT ( 'NONE',  ( 63.75227860486319997, 1.439518482450359960, -69.32544932539248350 ) ) ;
#30198=CARTESIAN_POINT ( 'NONE',  ( 64.43393739769619799, 10.88381105532070059, -68.84999999999999432 ) ) ;
#30231=CARTESIAN_POINT ( 'NONE',  ( 71.33393739769628894, 1.883811055320669947, -60.94999999999999574 ) ) ;
#30236=CARTESIAN_POINT ( 'NONE',  ( 71.33393739769628894, 10.88381105532070059, -68.84999999999999432 ) ) ;
#30239=CARTESIAN_POINT ( 'NONE',  ( 72.99271684938489102, 0.9525601718070090262, -69.17051385343440018 ) ) ;
#30249=DIRECTION ( 'NONE',  ( 0.000000000000000000, 1.000000000000000000, 0.000000000000000000 ) ) ;
#30253=CARTESIAN_POINT ( 'NONE',  ( 63.61158869431360330, 1.412203896157240068, -62.26955982508579979 ) ) ;
#30291=CARTESIAN_POINT ( 'NONE',  ( 64.67544096520701657, 1.230988031922719994, -70.42401535379970312 ) ) ;
#30301=CARTESIAN_POINT ( 'NONE',  ( 63.17939165373819321, 0.9307121176571799825, -69.03423516236559010 ) ) ;
#30310=CARTESIAN_POINT ( 'NONE',  ( 71.29339335573889969, 1.327097482837290121, -70.45474866971780159 ) ) ;
#30322=ORIENTED_EDGE ( 'NONE', *, *, #43013, .F. ) ;
#30327=AXIS2_PLACEMENT_3D ( 'NONE', #47014, #11102, #39644 ) ;
#30338=EDGE_LOOP ( 'NONE', ( #13230, #48652, #34357, #422 ) ) ;
#30351=CARTESIAN_POINT ( 'NONE',  ( 71.33393739769628894, 1.883811055320669947, -69.84999999999999432 ) ) ;
#30386=CARTESIAN_POINT ( 'NONE',  ( 72.75389709491450674, 1.389468113695450091, -68.84985728199801258 ) ) ;
#30388=CARTESIAN_POINT ( 'NONE',  ( 73.10923647485390120, 1.096036836948820037, -62.36911566638589477 ) ) ;
#30397=CARTESIAN_POINT ( 'NONE',  ( 64.85305306408218939, 1.096036836948810045, -70.62529907715770605 ) ) ;
#30402=ORIENTED_EDGE ( 'NONE', *, *, #49903, .T. ) ;
#30424=CARTESIAN_POINT ( 'NONE',  ( 63.78749078828948882, 1.530257664727401767, -68.84999999999999432 ) ) ;
#30436=AXIS2_PLACEMENT_3D ( 'NONE', #41661, #17811, #47927 ) ;
#30437=ORIENTED_EDGE ( 'NONE', *, *, #22096, .T. ) ;
#30451=CARTESIAN_POINT ( 'NONE',  ( 63.57990658082609770, 1.404649297339839897, -68.94572984764299406 ) ) ;
#30454=CARTESIAN_POINT ( 'NONE',  ( 71.18923915728029783, 1.331842543267529821, -60.79893402932049895 ) ) ;
#30456=CARTESIAN_POINT ( 'NONE',  ( 72.68796522584510456, 1.404650034022369987, -62.35426166056780062 ) ) ;
#30457=CARTESIAN_POINT ( 'NONE',  ( 71.33393739769628894, 11.23736444591397543, -69.70355339059327093 ) ) ;
#30470=CARTESIAN_POINT ( 'NONE',  ( 68.13393739769620083, -42.11618894467930119, -65.65000000000000568 ) ) ;
#30500=CARTESIAN_POINT ( 'NONE',  ( 63.24698825150780124, 1.338092079250050137, -62.67980446285670126 ) ) ;
#30513=CARTESIAN_POINT ( 'NONE',  ( 63.43778145654719935, 0.9561296872662339297, -61.91446069548659636 ) ) ;
#30523=ADVANCED_FACE ( 'NONE', ( #37651 ), #5947, .T. ) ;
#30543=CARTESIAN_POINT ( 'NONE',  ( 64.40305624006870744, 0.9897936423439808173, -70.34985062917159837 ) ) ;
#30551=CARTESIAN_POINT ( 'NONE',  ( 71.68355379101700464, 1.316034553465529999, -70.28644130772840981 ) ) ;
#30554=DIRECTION ( 'NONE',  ( 0.000000000000000000, 1.000000000000000000, 0.000000000000000000 ) ) ;
#30559=CARTESIAN_POINT ( 'NONE',  ( 63.53329261246669546, 1.393731187554809958, -68.81053500035210391 ) ) ;
#30568=CARTESIAN_POINT ( 'NONE',  ( 71.47772926835831697, 0.9971903505820688407, -70.62320069164850622 ) ) ;
#30570=CARTESIAN_POINT ( 'NONE',  ( 71.33393739883419471, 11.38381102407070067, -61.94987500004730663 ) ) ;
#30577=B_SPLINE_SURFACE_WITH_KNOTS ( 'NONE', 3, 3, ( 
 ( #27094, #7448, #7191, #19233, #11387, #6676, #30500, #23398, #19491, #34433 ),
 ( #50442, #44628, #48570, #4030, #12673, #24423, #23908, #24163, #598, #346 ),
 ( #16583, #44374, #28367, #48308, #28627, #27606, #20247, #4529, #8733, #32536 ),
 ( #31782, #8477, #43861, #24683, #32033, #48056, #4797, #12155, #40436, #39933 ),
 ( #11641, #35987, #36239, #16075, #20501, #40697, #23658, #16856, #19990, #36493 ),
 ( #20764, #103, #36752, #863, #47545, #43611, #44118, #40186, #7714, #39673 ),
 ( #51723, #16332, #28111, #4277, #19747, #3779, #35740, #15816, #8217, #47799 ),
 ( #32286, #12403, #11905, #27861, #7959, #37809, #29663, #13709, #33602, #13961 ),
 ( #5588, #41733, #49868, #1904, #44893, #17119, #45671, #29150, #29917, #17373 ),
 ( #45935, #32804, #17883, #21282, #49616, #21542, #33072, #37287, #49100, #33340 ),
 ( #48831, #17634, #10024, #1644, #49355, #9774, #42001, #13202, #5838, #1124 ),
 ( #25467, #45151, #40953, #25988, #1386, #6100, #9263, #37538, #33853, #12934 ),
 ( #22056, #5070, #38067, #2163, #28890, #41216, #25211, #8998, #24942, #21026 ),
 ( #5330, #37026, #13456, #25725, #21803, #29412, #45416, #9521, #41472, #39107 ),
 ( #47234, #7136, #23088, #10551, #14215, #42258, #22575, #38323, #14731, #50894 ),
 ( #42783, #11325, #6357, #51158, #27289, #30702, #11068, #38592, #14986, #2939 ) ),
 .UNSPECIFIED., .F., .F., .F.,
 ( 4, 2, 2, 2, 2, 2, 2, 4 ),
 ( 4, 1, 1, 1, 1, 1, 1, 4 ),
 ( -8.523275000000000432E-16, 0.07216186899280999101, 0.1546325764131659952, 0.2061767685508879844, 0.2319488646197490067, 0.2731842183299269533, 0.3391607842662109906, 0.4123535371017769680 ),
 ( 0.000000000000000000, 0.1428571428571430157, 0.2857142857142860315, 0.4285714285714289917, 0.5714285714285709528, 0.7142857142857139685, 0.8571428571428569843, 1.000000000000000000 ),
 .UNSPECIFIED. ) ;
#30588=EDGE_LOOP ( 'NONE', ( #47444, #44462, #18208, #2917 ) ) ;
#30590=CARTESIAN_POINT ( 'NONE',  ( 71.52463645511689094, 1.229084191802120030, -60.83585027030739667 ) ) ;
#30610=CARTESIAN_POINT ( 'NONE',  ( 70.99050876911339003, 1.383811055320669947, -70.34999999999999432 ) ) ;
#30615=CARTESIAN_POINT ( 'NONE',  ( 64.87536617802101091, 1.096110717717199812, -60.66079369553730061 ) ) ;
#30619=DIRECTION ( 'NONE',  ( 0.000000000000000000, 0.000000000000000000, -1.000000000000000000 ) ) ;
#30638=CARTESIAN_POINT ( 'NONE',  ( 64.83819905826869956, 1.404650034021960092, -61.09597217184949614 ) ) ;
#30647=CARTESIAN_POINT ( 'NONE',  ( 73.16231026946078941, 0.9234936569010840923, -62.37649816534809588 ) ) ;
#30701=CYLINDRICAL_SURFACE ( 'NONE', #48796, 0.4999999999999364397 ) ;
#30702=CARTESIAN_POINT ( 'NONE',  ( 63.34508830662979761, 1.264689361399209844, -62.28332989495390137 ) ) ;
#30714=CARTESIAN_POINT ( 'NONE',  ( 71.28186865452410359, 1.191644800533210091, -60.65994692684869705 ) ) ;
#30716=CARTESIAN_POINT ( 'NONE',  ( 72.62688124152660407, 1.412342135319809788, -62.12493822889140205 ) ) ;
#30728=CARTESIAN_POINT ( 'NONE',  ( 63.49151163952229382, 1.387131204727280132, -68.68796153961081075 ) ) ;
#30737=DIRECTION ( 'NONE',  ( 0.7071067811865457964, 0.7071067811865492381, 0.000000000000000000 ) ) ;
#30741=CARTESIAN_POINT ( 'NONE',  ( 63.25402410758490390, 0.9098571636355720083, -62.15909090909049439 ) ) ;
#30769=CARTESIAN_POINT ( 'NONE',  ( 63.70304491682400538, 1.421976796946359922, -62.00656477358510443 ) ) ;
#30773=CARTESIAN_POINT ( 'NONE',  ( 73.16133767175020353, 0.8879664753683469414, -68.92499589875220067 ) ) ;
#30783=TOROIDAL_SURFACE ( 'NONE', #40003, 1.499999999717960053, 0.4999999999863239952 ) ;
#30784=ORIENTED_EDGE ( 'NONE', *, *, #44030, .T. ) ;
#30799=CARTESIAN_POINT ( 'NONE',  ( 64.30690765430760791, 1.170657617701480024, -70.22888111369030639 ) ) ;
#30808=CARTESIAN_POINT ( 'NONE',  ( 71.38118348160060123, 1.400446703426730055, -70.22110957219430816 ) ) ;
#30822=CARTESIAN_POINT ( 'NONE',  ( 71.52074786344320501, 0.8966068345641440285, -70.60278586552529134 ) ) ;
#30840=ORIENTED_EDGE ( 'NONE', *, *, #15949, .T. ) ;
#30859=AXIS2_PLACEMENT_3D ( 'NONE', #21287, #20252, #48313 ) ;
#30860=DIRECTION ( 'NONE',  ( 0.000000000000000000, 1.000000000000000000, 0.000000000000000000 ) ) ;
#30863=CARTESIAN_POINT ( 'NONE',  ( 71.17905174416029013, 1.387412027389909985, -70.29005197907430613 ) ) ;
#30869=CARTESIAN_POINT ( 'NONE',  ( 64.81979753630260177, 0.8904513541338849869, -60.64834380034769623 ) ) ;
#30900=CARTESIAN_POINT ( 'NONE',  ( 73.02919596257699197, 0.9065823421260970072, -62.18054194328749418 ) ) ;
#30903=CARTESIAN_POINT ( 'NONE',  ( 71.33393739769628894, 4.883811055320659733, -61.44999999999999574 ) ) ;
#30906=CARTESIAN_POINT ( 'NONE',  ( 64.64662912975160225, 0.9425424353905850205, -70.53248918539379986 ) ) ;
#30952=DIRECTION ( 'NONE',  ( 0.000000000000000000, 1.000000000000000000, 0.000000000000000000 ) ) ;
#30966=CARTESIAN_POINT ( 'NONE',  ( 71.26289196806200721, 1.269319268680890067, -60.73450645366870049 ) ) ;
#30968=CARTESIAN_POINT ( 'NONE',  ( 72.65319675752509454, 1.258806274519030044, -61.81501369061300721 ) ) ;
#30971=AXIS2_PLACEMENT_3D ( 'NONE', #28399, #24454, #4827 ) ;
#30989=EDGE_CURVE ( 'NONE', #41820, #8182, #3746, .T. ) ;
#31001=CIRCLE ( 'NONE', #11768, 5.500000000000005329 ) ;
#31003=CIRCLE ( 'NONE', #15992, 0.9999999999999964473 ) ;
#31028=CARTESIAN_POINT ( 'NONE',  ( 63.78947450026019084, 1.274155933524790063, -61.60356854227319445 ) ) ;
#31032=CARTESIAN_POINT ( 'NONE',  ( 73.15215840802929392, 0.9242073871622918935, -68.93904330669420233 ) ) ;
#31059=CARTESIAN_POINT ( 'NONE',  ( 64.27705669950368872, 1.080042774363660030, -70.23909358936700187 ) ) ;
#31066=CARTESIAN_POINT ( 'NONE',  ( 71.80939745721281042, 1.439519383694590093, -70.03165268182070236 ) ) ;
#31070=CARTESIAN_POINT ( 'NONE',  ( 63.26785353957599511, 1.102139304147789822, -69.09899266709390986 ) ) ;
#31080=CARTESIAN_POINT ( 'NONE',  ( 71.46564822584178955, 0.9966178393190270324, -70.63122704464430512 ) ) ;
#31111=CARTESIAN_POINT ( 'NONE',  ( 63.23867883281540969, 0.9065823421260940096, -69.11945805671248877 ) ) ;
#31127=CARTESIAN_POINT ( 'NONE',  ( 64.92925538503580185, 1.097085799869280009, -60.62778596399619602 ) ) ;
#31158=CARTESIAN_POINT ( 'NONE',  ( 73.10713808934470137, 0.9971903505820729485, -62.30620812933800323 ) ) ;
#31164=CARTESIAN_POINT ( 'NONE',  ( 64.80710063092610085, 1.263823323415690147, -70.46116989902610328 ) ) ;
#31192=AXIS2_PLACEMENT_3D ( 'NONE', #5126, #29717, #25523 ) ;
#31221=CARTESIAN_POINT ( 'NONE',  ( 71.08986881540380409, 1.373356196620449943, -60.86873524938349789 ) ) ;
#31224=CARTESIAN_POINT ( 'NONE',  ( 72.53531777184440443, 1.426105412860890098, -61.95447814822819765 ) ) ;
#31243=DIRECTION ( 'NONE',  ( 0.000000000000000000, 1.000000000000000000, 0.000000000000000000 ) ) ;
#31245=CARTESIAN_POINT ( 'NONE',  ( 72.33393739769618946, 10.88381105532070059, -62.44999999999999574 ) ) ;
#31260=DIRECTION ( 'NONE',  ( 0.000000000000000000, -0.7071067811865162644, -0.7071067811865786590 ) ) ;
#31268=CARTESIAN_POINT ( 'NONE',  ( 68.13393739769620083, 1.883811055320669947, -60.94999999999999574 ) ) ;
#31269=CARTESIAN_POINT ( 'NONE',  ( 64.36068579096159681, 0.9644290104359670712, -60.98409269229870233 ) ) ;
#31272=AXIS2_PLACEMENT_3D ( 'NONE', #47635, #28661, #11743 ) ;
#31278=CARTESIAN_POINT ( 'NONE',  ( 63.27838127973599569, 0.9150552061906049861, -62.12504221718990038 ) ) ;
#31282=CARTESIAN_POINT ( 'NONE',  ( 72.78816252330430814, 1.385888765344509999, -68.65207957385619864 ) ) ;
#31298=EDGE_LOOP ( 'NONE', ( #3873, #17261, #42760, #3609, #29684, #40018 ) ) ;
#31321=CARTESIAN_POINT ( 'NONE',  ( 71.40386387224138787, 1.392490173687920052, -70.25015106115239405 ) ) ;
#31330=CARTESIAN_POINT ( 'NONE',  ( 63.92076813643380007, 1.033004454759739899, -69.92211063522330505 ) ) ;
#31343=VERTEX_POINT ( 'NONE', #39028 ) ;
#31358=CARTESIAN_POINT ( 'NONE',  ( 68.13393739769620083, 1.383811055320669947, -65.65000000000000568 ) ) ;
#31379=ORIENTED_EDGE ( 'NONE', *, *, #7219, .F. ) ;
#31382=CARTESIAN_POINT ( 'NONE',  ( 64.93084822843239579, 1.265664290790580182, -60.77244468760530083 ) ) ;
#31402=DIRECTION ( 'NONE',  ( 0.000000000000000000, 1.000000000000000000, 0.000000000000000000 ) ) ;
#31412=CARTESIAN_POINT ( 'NONE',  ( 72.92278648876258274, 1.264689361399219836, -62.28332989495380190 ) ) ;
#31445=( BOUNDED_SURFACE ( )  B_SPLINE_SURFACE ( 2, 2, ( 
 ( #11488, #27703, #39771 ),
 ( #7290, #39257, #36085 ),
 ( #192, #43701, #3360 ) ),
 .UNSPECIFIED., .F., .F., .T. ) 
 B_SPLINE_SURFACE_WITH_KNOTS ( ( 3, 3 ),
 ( 3, 3 ),
 ( 3.075382746042809996E-13, 1.570796326795540043 ),
 ( -1.570796326795069975, 2.603505476660149968E-13 ),
 .UNSPECIFIED. ) 
 GEOMETRIC_REPRESENTATION_ITEM ( )  RATIONAL_B_SPLINE_SURFACE ( (
 ( 1.000000000000000000, 0.7071067811863940289, 1.000000000000000000),
 ( 0.7071067811864010233, 0.4999999999997879474, 0.7071067811864010233),
 ( 1.000000000000000000, 0.7071067811863940289, 1.000000000000000000) ) ) 
 REPRESENTATION_ITEM ( '' )  SURFACE ( )  );
#31456=CARTESIAN_POINT ( 'NONE',  ( 63.02016742692980245, 0.9209567800143640959, -68.78847615610249022 ) ) ;
#31475=CARTESIAN_POINT ( 'NONE',  ( 71.06936022730370439, 1.374300485541529948, -60.86138005882520474 ) ) ;
#31477=CARTESIAN_POINT ( 'NONE',  ( 72.67981544229699864, 0.9952277120690129486, -61.73279890693489591 ) ) ;
#31481=ORIENTED_EDGE ( 'NONE', *, *, #42309, .T. ) ;
#31485=ORIENTED_EDGE ( 'NONE', *, *, #41272, .T. ) ;
#31495=AXIS2_PLACEMENT_3D ( 'NONE', #51141, #34880, #34615 ) ;
#31531=CARTESIAN_POINT ( 'NONE',  ( 64.59570122278479687, 0.9170823515331258946, -60.80394275157760831 ) ) ;
#31543=CARTESIAN_POINT ( 'NONE',  ( 73.12314370215899828, 1.096110717717199812, -68.90857121967530929 ) ) ;
#31575=CARTESIAN_POINT ( 'NONE',  ( 71.81740743633011448, 1.051325075267619980, -70.37790726184800860 ) ) ;
#31580=CARTESIAN_POINT ( 'NONE',  ( 63.23627918741579634, 0.9395704634982890990, -69.11607016250880520 ) ) ;
#31588=CARTESIAN_POINT ( 'NONE',  ( 64.86401092314891059, 1.392490173688039956, -61.04984893884839892 ) ) ;
#31590=CARTESIAN_POINT ( 'NONE',  ( 71.54045699608269615, 0.8986939045430379913, -70.58925035374331003 ) ) ;
#31618=EDGE_CURVE ( 'NONE', #34264, #309, #18402, .T. ) ;
#31637=CARTESIAN_POINT ( 'NONE',  ( 64.82950905750189463, 0.9955677559369568996, -60.65081522799539471 ) ) ;
#31664=EDGE_CURVE ( 'NONE', #14121, #27414, #10902, .T. ) ;
#31667=CARTESIAN_POINT ( 'NONE',  ( 72.84798422376138660, 1.369544300367010026, -62.51645495968789845 ) ) ;
#31674=CARTESIAN_POINT ( 'NONE',  ( 64.95360084570988590, 1.395196698723379924, -70.24366017557039754 ) ) ;
#31707=CARTESIAN_POINT ( 'NONE',  ( 63.01386660552499563, 0.9960089569207349891, -68.76188247756290650 ) ) ;
#31727=CARTESIAN_POINT ( 'NONE',  ( 71.50269221454749413, 1.097545367735389910, -60.73071135393699649 ) ) ;
#31729=CARTESIAN_POINT ( 'NONE',  ( 72.80373209685389213, 0.9973858971044751165, -61.88154445005670112 ) ) ;
#31755=ADVANCED_FACE ( 'NONE', ( #22612 ), #2720, .T. ) ;
#31765=CARTESIAN_POINT ( 'NONE',  ( 64.28413441608979895, 1.451794159057709921, -69.91814348332408713 ) ) ;
#31782=CARTESIAN_POINT ( 'NONE',  ( 63.06393505168800573, 0.8850831926798630178, -62.44126551166660022 ) ) ;
#31785=DIRECTION ( 'NONE',  ( 0.000000000000000000, 1.000000000000000000, 0.000000000000000000 ) ) ;
#31786=CARTESIAN_POINT ( 'NONE',  ( 63.27838127973589621, 0.9150552061906049861, -62.12504221718980091 ) ) ;
#31794=CARTESIAN_POINT ( 'NONE',  ( 63.30304092011348871, 0.9208623934744509798, -62.09132346512829770 ) ) ;
#31796=CARTESIAN_POINT ( 'NONE',  ( 72.72056432233058842, 1.396834109478129804, -62.44999999999999574 ) ) ;
#31798=CARTESIAN_POINT ( 'NONE',  ( 73.13559359734860266, 0.8904513541338849869, -68.96413986139360475 ) ) ;
#31833=CARTESIAN_POINT ( 'NONE',  ( 72.39774331670469110, 1.277124412296150036, -69.78360917201301561 ) ) ;
#31837=CARTESIAN_POINT ( 'NONE',  ( 63.23690831390890565, 1.005545696829380109, -69.10544663728329340 ) ) ;
#31841=CARTESIAN_POINT ( 'NONE',  ( 64.57410506046470289, 0.9210617359723460851, -70.48005104816749622 ) ) ;
#31848=ORIENTED_EDGE ( 'NONE', *, *, #921, .F. ) ;
#31850=AXIS2_PLACEMENT_3D ( 'NONE', #48701, #13319, #49732 ) ;
#31859=CARTESIAN_POINT ( 'NONE',  ( 71.27262092911109903, 0.8838110553206740549, -70.76364393196210756 ) ) ;
#31874=EDGE_CURVE ( 'NONE', #49378, #46311, #49013, .T. ) ;
#31878=DIRECTION ( 'NONE',  ( 0.000000000000000000, 1.000000000000000000, 0.000000000000000000 ) ) ;
#31925=CARTESIAN_POINT ( 'NONE',  ( 73.08617409304301304, 0.9989215084294049696, -62.27490163988890259 ) ) ;
#31926=CIRCLE ( 'NONE', #149, 0.5000000000000000000 ) ;
#31955=CARTESIAN_POINT ( 'NONE',  ( 71.03155062328740144, 1.383928098097870096, -60.96256459357869772 ) ) ;
#31966=CARTESIAN_POINT ( 'NONE',  ( 63.08453170404659716, 0.9940423591679348192, -68.87653036433009390 ) ) ;
#31970=FACE_OUTER_BOUND ( 'NONE', #18810, .T. ) ;
#31980=CARTESIAN_POINT ( 'NONE',  ( 71.25019707560579718, 0.8838110553206759423, -70.77727272727280194 ) ) ;
#31983=DIRECTION ( 'NONE',  ( -0.7071067811865441310, 0.000000000000000000, 0.7071067811865510144 ) ) ;
#31988=CARTESIAN_POINT ( 'NONE',  ( 71.52819866244169589, 1.000225705806889964, -60.71075825745960231 ) ) ;
#31990=CARTESIAN_POINT ( 'NONE',  ( 72.26623590265971586, 1.348264851907009731, -61.45091980464700043 ) ) ;
#31995=CARTESIAN_POINT ( 'NONE',  ( 71.33393739769809372, 11.38368607098449914, -61.45000000000081286 ) ) ;
#32001=AXIS2_PLACEMENT_3D ( 'NONE', #19905, #36657, #44276 ) ;
#32015=EDGE_CURVE ( 'NONE', #51296, #42080, #6628, .T. ) ;
#32024=DIRECTION ( 'NONE',  ( 0.000000000000000000, -1.000000000000000000, 0.000000000000000000 ) ) ;
#32027=CIRCLE ( 'NONE', #5323, 0.4999999999999986677 ) ;
#32028=ORIENTED_EDGE ( 'NONE', *, *, #44738, .T. ) ;
#32033=CARTESIAN_POINT ( 'NONE',  ( 63.14388432454488509, 1.191644800533210091, -62.50206874317210293 ) ) ;
#32086=CARTESIAN_POINT ( 'NONE',  ( 72.55472656186499592, 1.019773975906300034, -69.70721229073478753 ) ) ;
#32088=( NAMED_UNIT ( * ) PLANE_ANGLE_UNIT ( ) SI_UNIT ( $, .RADIAN. ) );
#32098=CARTESIAN_POINT ( 'NONE',  ( 64.80088823274370213, 1.308647200627810259, -60.89791552425909771 ) ) ;
#32128=CARTESIAN_POINT ( 'NONE',  ( 63.15096886846589541, 0.8925687589132609290, -68.99219224778180148 ) ) ;
#32145=EDGE_LOOP ( 'NONE', ( #27120, #37898, #34719, #33918 ) ) ;
#32186=DIRECTION ( 'NONE',  ( -1.000000000000000000, 0.000000000000000000, 0.000000000000000000 ) ) ;
#32209=CARTESIAN_POINT ( 'NONE',  ( 71.13601697155240799, 1.385888765344509999, -60.99577487439199786 ) ) ;
#32214=DIRECTION ( 'NONE',  ( 0.000000000000000000, -1.000000000000000000, 0.000000000000000000 ) ) ;
#32216=CARTESIAN_POINT ( 'NONE',  ( 63.05799534064709633, 1.101170701158060039, -68.76387392617688477 ) ) ;
#32229=CARTESIAN_POINT ( 'NONE',  ( 71.33861941035669929, 1.097085799869280009, -70.67221403600389351 ) ) ;
#32238=CARTESIAN_POINT ( 'NONE',  ( 71.45588032111159293, 0.8910129994591549085, -60.65352295474710331 ) ) ;
#32240=CARTESIAN_POINT ( 'NONE',  ( 71.40255948545589604, 1.402336724396250123, -61.08651255177160522 ) ) ;
#32244=CARTESIAN_POINT ( 'NONE',  ( 65.16374186055298878, 1.338092079250050137, -70.53694914618849054 ) ) ;
#32265=AXIS2_PLACEMENT_3D ( 'NONE', #41795, #5651, #41277 ) ;
#32274=ORIENTED_EDGE ( 'NONE', *, *, #46040, .T. ) ;
#32286=CARTESIAN_POINT ( 'NONE',  ( 63.13228119804391270, 0.8904513541338849869, -62.33586013860640662 ) ) ;
#32287=DIRECTION ( 'NONE',  ( 0.000000000000000000, 1.000000000000000000, 0.000000000000000000 ) ) ;
#32295=CARTESIAN_POINT ( 'NONE',  ( 64.65764093855679562, 1.007912009470880221, -60.76768544528139415 ) ) ;
#32334=AXIS2_PLACEMENT_3D ( 'NONE', #15449, #23275, #31402 ) ;
#32342=CARTESIAN_POINT ( 'NONE',  ( 72.14060588395169304, 1.458412159422780130, -69.79309345819311261 ) ) ;
#32358=CARTESIAN_POINT ( 'NONE',  ( 71.35346284499661351, 1.390806392144110060, -70.26251807531768634 ) ) ;
#32360=FACE_OUTER_BOUND ( 'NONE', #24969, .T. ) ;
#32386=CARTESIAN_POINT ( 'NONE',  ( 64.72741779930989026, 0.8986939045430250017, -70.58925035374339529 ) ) ;
#32440=CARTESIAN_POINT ( 'NONE',  ( 63.49151163952229382, 1.387131204727290124, -62.61203846038919352 ) ) ;
#32461=CARTESIAN_POINT ( 'NONE',  ( 73.22214118178139586, 1.102581332775300016, -68.74251431096891451 ) ) ;
#32464=CARTESIAN_POINT ( 'NONE',  ( 63.07934790479939835, 0.9219904752505979628, -68.88295677568349618 ) ) ;
#32478=CARTESIAN_POINT ( 'NONE',  ( 71.34390086684349797, 1.188582381068100213, -70.60520998597918663 ) ) ;
#32489=CARTESIAN_POINT ( 'NONE',  ( 71.31202044992319600, 1.326578174762029994, -60.85378544217730479 ) ) ;
#32492=CARTESIAN_POINT ( 'NONE',  ( 71.53423548837180590, 1.309820314133740116, -60.93204159761199890 ) ) ;
#32496=CARTESIAN_POINT ( 'NONE',  ( 65.13423472332449649, 1.371651820402789879, -70.41530492215990478 ) ) ;
#32536=CARTESIAN_POINT ( 'NONE',  ( 63.44650199127489998, 1.383928098097870096, -62.75238677440889035 ) ) ;
#32544=CARTESIAN_POINT ( 'NONE',  ( 64.81907236522970095, 1.326666718054990035, -60.91913985162000245 ) ) ;
#32550=ORIENTED_EDGE ( 'NONE', *, *, #33050, .T. ) ;
#32555=VECTOR ( 'NONE', #14807, 1000.000000000000000 ) ;
#32600=CARTESIAN_POINT ( 'NONE',  ( 72.27589226135678757, 1.457833794292699992, -69.65505222163159260 ) ) ;
#32606=B_SPLINE_CURVE_WITH_KNOTS ( 'NONE', 3,
 ( #5875, #5629, #1426, #14513, #34413, #50424, #49905, #37326, #50160, #18436, #45712, #33640, #46503, #33380, #25507, #1945 ),
 .UNSPECIFIED., .F., .F.,
 ( 4, 2, 2, 2, 2, 2, 2, 4 ),
 ( -1.183080999999999906E-15, 0.07216186899280699341, 0.1546325764131580016, 0.2061767685508779924, 0.2319488646197380433, 0.2731842183299139637, 0.3391607842661950034, 0.4123535371017569839 ),
 .UNSPECIFIED. ) ;
#32613=CARTESIAN_POINT ( 'NONE',  ( 63.97287235346109213, 1.200163167270720033, -61.36285812046030230 ) ) ;
#32617=DIRECTION ( 'NONE',  ( 0.000000000000000000, 1.000000000000000000, 0.000000000000000000 ) ) ;
#32643=CARTESIAN_POINT ( 'NONE',  ( 64.08038400710292137, 11.23736444591397543, -62.44999999999999574 ) ) ;
#32647=CARTESIAN_POINT ( 'NONE',  ( 64.81979753630270125, 0.8904513541338869853, -70.65165619965239330 ) ) ;
#32650=PLANE ( 'NONE',  #45589 ) ;
#32655=CARTESIAN_POINT ( 'NONE',  ( 64.05763092918830637, 1.195687002465839921, -70.01615807439628725 ) ) ;
#32669=AXIS2_PLACEMENT_3D ( 'NONE', #29570, #9669, #21698 ) ;
#32687=EDGE_CURVE ( 'NONE', #2182, #33090, #4434, .T. ) ;
#32730=CARTESIAN_POINT ( 'NONE',  ( 63.18291598250529262, 1.096305581841150012, -68.96938879548969226 ) ) ;
#32745=CARTESIAN_POINT ( 'NONE',  ( 71.36046776202630326, 0.9940423591679348192, -70.69940569364969463 ) ) ;
#32752=CARTESIAN_POINT ( 'NONE',  ( 72.99182123261159916, 1.264489825601020190, -68.89055226466270199 ) ) ;
#32757=CARTESIAN_POINT ( 'NONE',  ( 71.25608535201600091, 1.369535599030039963, -60.93144909420819744 ) ) ;
#32758=CARTESIAN_POINT ( 'NONE',  ( 64.43393739769619799, 10.88381105532070059, -64.04999999999999716 ) ) ;
#32759=CARTESIAN_POINT ( 'NONE',  ( 71.83998266832981017, 1.442158793902750036, -61.28605443723469648 ) ) ;
#32761=CARTESIAN_POINT ( 'NONE',  ( 65.23632417210519918, 1.383928098097870096, -70.33743540642140601 ) ) ;
#32793=VERTEX_POINT ( 'NONE', #23098 ) ;
#32797=CARTESIAN_POINT ( 'NONE',  ( 63.43393739769620510, 1.883811055320669947, -68.84999999999999432 ) ) ;
#32804=CARTESIAN_POINT ( 'NONE',  ( 63.14953303862429124, 0.9272522097098079286, -62.30994913869029972 ) ) ;
#32810=CARTESIAN_POINT ( 'NONE',  ( 72.60391569211400054, 1.424120032878380071, -62.14639092277510457 ) ) ;
#32813=CARTESIAN_POINT ( 'NONE',  ( 64.64662912975151698, 0.9425424353906030062, -60.76751081460630388 ) ) ;
#32842=ORIENTED_EDGE ( 'NONE', *, *, #25486, .F. ) ;
#32860=CARTESIAN_POINT ( 'NONE',  ( 72.12455669199449915, 1.010053820890680187, -70.13159119767701100 ) ) ;
#32875=CARTESIAN_POINT ( 'NONE',  ( 64.39929874312750258, 1.394112346784160072, -61.21167439625769902 ) ) ;
#32880=CARTESIAN_POINT ( 'NONE',  ( 65.27736602627911111, 0.8838110553206759423, -60.94999999999999574 ) ) ;
#32883=DIRECTION ( 'NONE',  ( 1.000000000000000000, -1.040313928821094058E-14, -2.593849395860594704E-12 ) ) ;
#32911=DIRECTION ( 'NONE',  ( 0.7071067811865656694, -0.7071067811865292541, 0.000000000000000000 ) ) ;
#32920=CARTESIAN_POINT ( 'NONE',  ( 71.86947670220010309, 0.9561296872641460443, -60.95384405884320245 ) ) ;
#32923=CARTESIAN_POINT ( 'NONE',  ( 64.26570060236220172, 1.437402181457050121, -69.93576135023748463 ) ) ;
#32927=ORIENTED_EDGE ( 'NONE', *, *, #2063, .F. ) ;
#32953=CARTESIAN_POINT ( 'NONE',  ( 72.75396425272869294, 1.390208944942409985, -68.75457626026799574 ) ) ;
#32968=AXIS2_PLACEMENT_3D ( 'NONE', #41464, #9766, #1379 ) ;
#32997=CARTESIAN_POINT ( 'NONE',  ( 65.27736602627911111, 0.8838110553206759423, -70.34999999999999432 ) ) ;
#33014=CARTESIAN_POINT ( 'NONE',  ( 71.08986881540380409, 1.373356196620459935, -70.43126475061649217 ) ) ;
#33020=CARTESIAN_POINT ( 'NONE',  ( 73.07509570698499601, 0.9325382164350239922, -69.05375146239639150 ) ) ;
#33027=CARTESIAN_POINT ( 'NONE',  ( 71.85972712066590873, 1.428542319231199897, -61.26680764775160526 ) ) ;
#33029=CARTESIAN_POINT ( 'NONE',  ( 65.00022493107950083, 0.9952464559119579279, -70.75693755662150863 ) ) ;
#33050=EDGE_CURVE ( 'NONE', #37879, #28142, #5787, .T. ) ;
#33072=CARTESIAN_POINT ( 'NONE',  ( 63.33772283987349283, 1.326578174762029994, -62.47191694777300341 ) ) ;
#33077=CARTESIAN_POINT ( 'NONE',  ( 72.63889986537131449, 1.416242794301129981, -62.22702189776489945 ) ) ;
#33080=FACE_OUTER_BOUND ( 'NONE', #16941, .T. ) ;
#33084=DIRECTION ( 'NONE',  ( 0.000000000000000000, 0.000000000000000000, 1.000000000000000000 ) ) ;
#33090=VERTEX_POINT ( 'NONE', #11955 ) ;
#33128=CARTESIAN_POINT ( 'NONE',  ( 72.99216053021440587, 1.027568165751439944, -69.15654010815640618 ) ) ;
#33144=CARTESIAN_POINT ( 'NONE',  ( 63.93485720234319558, 1.348264851907009731, -61.51770149503649776 ) ) ;
#33148=CARTESIAN_POINT ( 'NONE',  ( 68.13393739769620083, 0.8838110553206759423, -65.65000000000000568 ) ) ;
#33166=EDGE_CURVE ( 'NONE', #37946, #25965, #27022, .T. ) ;
#33185=EDGE_CURVE ( 'NONE', #23933, #17827, #37920, .T. ) ;
#33189=CARTESIAN_POINT ( 'NONE',  ( 63.84678457914870364, 1.200162789678009823, -69.81105362774360401 ) ) ;
#33226=CARTESIAN_POINT ( 'NONE',  ( 73.01642658308999501, 0.9425424353906030062, -62.16269173205530763 ) ) ;
#33261=DIRECTION ( 'NONE',  ( 1.000000000000000000, 0.000000000000000000, 0.000000000000000000 ) ) ;
#33282=CARTESIAN_POINT ( 'NONE',  ( 71.42462519098069151, 0.8888742037077609348, -70.66714310028369539 ) ) ;
#33289=CARTESIAN_POINT ( 'NONE',  ( 72.77636315587029969, 1.387131204727280132, -68.68796153961081075 ) ) ;
#33292=CARTESIAN_POINT ( 'NONE',  ( 73.26121012496899709, 0.9212109678634080590, -62.53374032209040223 ) ) ;
#33296=CARTESIAN_POINT ( 'NONE',  ( 71.99113505772810129, 1.080095028449399974, -61.06117396776439676 ) ) ;
#33298=LINE ( 'NONE', #36709, #4234 ) ;
#33301=CARTESIAN_POINT ( 'NONE',  ( 64.97847163984020824, 0.9947083095259759977, -70.74365995857920097 ) ) ;
#33340=CARTESIAN_POINT ( 'NONE',  ( 63.50007682179899149, 1.388189907116970101, -62.58632377286669879 ) ) ;
#33349=CARTESIAN_POINT ( 'NONE',  ( 63.46413472570510095, 0.9973839016405651181, -69.41844569992100844 ) ) ;
#33380=CARTESIAN_POINT ( 'NONE',  ( 73.04443511092429731, 0.9036513197889520788, -69.09785636402040154 ) ) ;
#33393=CARTESIAN_POINT ( 'NONE',  ( 73.13559359734860266, 0.8904513541338869853, -62.33586013860640662 ) ) ;
#33395=CARTESIAN_POINT ( 'NONE',  ( 72.65185559415030525, 1.328802495349810098, -69.38895227739480731 ) ) ;
#33399=CARTESIAN_POINT ( 'NONE',  ( 72.33393739770319542, 11.38381105531869686, -69.85000000000681553 ) ) ;
#33408=CARTESIAN_POINT ( 'NONE',  ( 64.60887562658849959, 1.412342135319750058, -61.15705615616909796 ) ) ;
#33437=CYLINDRICAL_SURFACE ( 'NONE', #4053, 0.5000000000000049960 ) ;
#33446=CARTESIAN_POINT ( 'NONE',  ( 72.61552859537219717, 1.010053820890850051, -61.65938070570059892 ) ) ;
#33447=CARTESIAN_POINT ( 'NONE',  ( 63.64770250141179986, 1.099199775695780090, -69.62734437806821575 ) ) ;
#33460=CARTESIAN_POINT ( 'NONE',  ( 64.93393739769619799, 11.23736444591397543, -61.59644660940672622 ) ) ;
#33480=CARTESIAN_POINT ( 'NONE',  ( 64.93393739769619799, 10.88381105532070059, -61.94999999999999574 ) ) ;
#33491=ORIENTED_EDGE ( 'NONE', *, *, #5449, .F. ) ;
#33522=CARTESIAN_POINT ( 'NONE',  ( 65.09331375576360301, 1.276058558775509999, -60.69120887205459525 ) ) ;
#33548=CARTESIAN_POINT ( 'NONE',  ( 72.97593009921529017, 1.263903724274369811, -62.37965189720969761 ) ) ;
#33549=CARTESIAN_POINT ( 'NONE',  ( 72.78175560864718818, 1.385702546077159925, -68.77407799673838440 ) ) ;
#33552=CARTESIAN_POINT ( 'NONE',  ( 73.06384957064030061, 1.187237555532410171, -62.39609834743819761 ) ) ;
#33560=CARTESIAN_POINT ( 'NONE',  ( 64.94442696602180831, 1.326324093417230232, -70.44093178352311213 ) ) ;
#33572=DIRECTION ( 'NONE',  ( 0.000000000000000000, -1.000000000000000000, 0.000000000000000000 ) ) ;
#33579=ORIENTED_EDGE ( 'NONE', *, *, #17263, .T. ) ;
#33602=CARTESIAN_POINT ( 'NONE',  ( 63.46249669555339779, 1.383767307422969939, -62.59255479634269648 ) ) ;
#33611=CARTESIAN_POINT ( 'NONE',  ( 63.58222404636121183, 1.087299280848000205, -69.55154624241478700 ) ) ;
#33640=CARTESIAN_POINT ( 'NONE',  ( 73.08672326322148649, 0.8966068345641430293, -69.03681046574689617 ) ) ;
#33651=CARTESIAN_POINT ( 'NONE',  ( 73.24758132965830271, 0.8838110553206740549, -62.51131646858519275 ) ) ;
#33655=CARTESIAN_POINT ( 'NONE',  ( 72.84263360082020711, 1.236214136008370046, -69.21416709495440500 ) ) ;
#33666=CARTESIAN_POINT ( 'NONE',  ( 64.37933009232320103, 1.063298638255609996, -60.97768308011880123 ) ) ;
#33693=VECTOR ( 'NONE', #29315, 1000.000000000000000 ) ;
#33703=CARTESIAN_POINT ( 'NONE',  ( 63.64944581154209402, 1.039768281806159989, -69.63739004519409548 ) ) ;
#33715=CARTESIAN_POINT ( 'NONE',  ( 63.18170070234948810, 0.9989215084294049696, -69.02509836011120115 ) ) ;
#33732=CARTESIAN_POINT ( 'NONE',  ( 72.82769086651219936, 1.383811055320669947, -68.52712657046359368 ) ) ;
#33780=CIRCLE ( 'NONE', #31272, 0.5000000000000004441 ) ;
#33789=EDGE_LOOP ( 'NONE', ( #40457, #9840, #47287, #13926 ) ) ;
#33797=CARTESIAN_POINT ( 'NONE',  ( 65.01129443250870565, 1.391252479931859964, -61.03617692120100457 ) ) ;
#33802=CARTESIAN_POINT ( 'NONE',  ( 72.84798422376138660, 1.369544300367010026, -68.78354504031220529 ) ) ;
#33805=CARTESIAN_POINT ( 'NONE',  ( 72.81780655506248934, 1.383161449028140089, -62.62844710992279573 ) ) ;
#33807=CARTESIAN_POINT ( 'NONE',  ( 71.50060750274239751, 1.264689361399219836, -60.86115090893359536 ) ) ;
#33809=CARTESIAN_POINT ( 'NONE',  ( 71.25019707560579718, 0.8838110553206759423, -60.52272727272730179 ) ) ;
#33811=CARTESIAN_POINT ( 'NONE',  ( 64.93084822843239579, 1.265664290790580182, -70.52755531239479581 ) ) ;
#33853=CARTESIAN_POINT ( 'NONE',  ( 63.48611918674540533, 1.385702546077169917, -62.52592200326169092 ) ) ;
#33855=DIRECTION ( 'NONE',  ( 0.8059588108975772602, 0.1342272854595020215, -0.5765530599821120372 ) ) ;
#33865=CARTESIAN_POINT ( 'NONE',  ( 63.25402410758490390, 0.9098571636355720083, -69.14090909090960224 ) ) ;
#33870=CARTESIAN_POINT ( 'NONE',  ( 72.63889986537131449, 1.416242794301129981, -62.22702189776489945 ) ) ;
#33884=CARTESIAN_POINT ( 'NONE',  ( 64.02475525337911222, 1.458407608744489936, -61.60944193589799767 ) ) ;
#33885=VERTEX_POINT ( 'NONE', #18265 ) ;
#33907=CARTESIAN_POINT ( 'NONE',  ( 72.88602187343720118, 1.308647200627810259, -68.98304916495260386 ) ) ;
#33918=ORIENTED_EDGE ( 'NONE', *, *, #14312, .T. ) ;
#33920=CARTESIAN_POINT ( 'NONE',  ( 63.57531447127419710, 1.379674774870449871, -62.12513747322240221 ) ) ;
#33927=DIRECTION ( 'NONE',  ( 1.000000000000000000, -0.000000000000000000, 7.105427357601000281E-15 ) ) ;
#33931=VERTEX_POINT ( 'NONE', #49994 ) ;
#33954=CARTESIAN_POINT ( 'NONE',  ( 64.39533937344960179, 1.328776533453549957, -70.16816298099379878 ) ) ;
#33958=ORIENTED_EDGE ( 'NONE', *, *, #2313, .F. ) ;
#33965=CARTESIAN_POINT ( 'NONE',  ( 63.14953303862429124, 0.9272522097098119254, -68.99005086130968323 ) ) ;
#34028=CARTESIAN_POINT ( 'NONE',  ( 65.02205492013339949, 0.9960089569207349891, -60.52992920782880049 ) ) ;
#34049=CARTESIAN_POINT ( 'NONE',  ( 64.80710063092610085, 1.263823323415670163, -60.83883010097409993 ) ) ;
#34057=CARTESIAN_POINT ( 'NONE',  ( 72.80287646850248962, 1.383922910988889976, -62.58539998085741018 ) ) ;
#34064=CARTESIAN_POINT ( 'NONE',  ( 64.72741779930989026, 0.8986939045430288875, -70.58925035374339529 ) ) ;
#34069=EDGE_CURVE ( 'NONE', #10547, #35448, #19541, .T. ) ;
#34079=AXIS2_PLACEMENT_3D ( 'NONE', #27174, #42665, #22718 ) ;
#34089=CARTESIAN_POINT ( 'NONE',  ( 64.64302830678670375, 0.9098571636355720083, -70.52991329011129551 ) ) ;
#34112=DIRECTION ( 'NONE',  ( -1.000000000000000000, 0.000000000000000000, 0.000000000000000000 ) ) ;
#34118=CARTESIAN_POINT ( 'NONE',  ( 63.49748922100520332, 1.316033847539019863, -69.19960462970651349 ) ) ;
#34124=ADVANCED_FACE ( 'NONE', ( #42011 ), #7181, .T. ) ;
#34146=CARTESIAN_POINT ( 'NONE',  ( 62.13393739769620083, -42.11618894467930119, -65.65000000000000568 ) ) ;
#34160=CARTESIAN_POINT ( 'NONE',  ( 72.92870999253369746, 1.229734285826180162, -69.07389306497110226 ) ) ;
#34175=CARTESIAN_POINT ( 'NONE',  ( 63.90196154687351537, 1.277721627657099956, -61.48328519722549856 ) ) ;
#34183=CIRCLE ( 'NONE', #39219, 0.4999999999999990008 ) ;
#34187=ORIENTED_EDGE ( 'NONE', *, *, #131, .T. ) ;
#34204=DIRECTION ( 'NONE',  ( -0.7071067811865457964, 0.7071067811865492381, 0.000000000000000000 ) ) ;
#34211=CARTESIAN_POINT ( 'NONE',  ( 64.86412778899749298, 1.402436395646509792, -70.21307676274530252 ) ) ;
#34223=CARTESIAN_POINT ( 'NONE',  ( 63.11571638736320011, 0.9242073871622918935, -68.93904330669420233 ) ) ;
#34264=VERTEX_POINT ( 'NONE', #35525 ) ;
#34291=FACE_OUTER_BOUND ( 'NONE', #2705, .T. ) ;
#34319=CARTESIAN_POINT ( 'NONE',  ( 73.12814476249489815, 0.9958340104639701318, -62.33798249239750078 ) ) ;
#34325=CARTESIAN_POINT ( 'NONE',  ( 64.79014552703429786, 0.9971903505820729485, -70.62320069164850622 ) ) ;
#34357=ORIENTED_EDGE ( 'NONE', *, *, #12349, .T. ) ;
#34362=CARTESIAN_POINT ( 'NONE',  ( 63.33805919087440373, 1.375383258925270136, -68.56484433753419694 ) ) ;
#34382=CARTESIAN_POINT ( 'NONE',  ( 63.60417424459109981, 1.405463742252590187, -69.09493810159840166 ) ) ;
#34413=CARTESIAN_POINT ( 'NONE',  ( 73.18782247527531126, 0.8859637708054480809, -68.88406027352149863 ) ) ;
#34416=AXIS2_PLACEMENT_3D ( 'NONE', #38026, #18615, #46162 ) ;
#34428=CARTESIAN_POINT ( 'NONE',  ( 71.52074786344310553, 0.8966068345641450277, -60.69721413447469871 ) ) ;
#34433=CARTESIAN_POINT ( 'NONE',  ( 63.43393739769620510, 1.383811055320669947, -62.79342862858290886 ) ) ;
#34442=VERTEX_POINT ( 'NONE', #44421 ) ;
#34445=CARTESIAN_POINT ( 'NONE',  ( 63.42524119458249743, 1.236214136009519793, -62.08583290503010232 ) ) ;
#34456=ORIENTED_EDGE ( 'NONE', *, *, #3789, .F. ) ;
#34461=CARTESIAN_POINT ( 'NONE',  ( 68.13393739769620083, -42.61618894467930119, -65.65000000000000568 ) ) ;
#34472=EDGE_CURVE ( 'NONE', #11677, #23424, #1178, .T. ) ;
#34481=CARTESIAN_POINT ( 'NONE',  ( 64.39815381769149383, 0.9561815866734409974, -70.34594416269000305 ) ) ;
#34489=CARTESIAN_POINT ( 'NONE',  ( 71.40227520965750330, 1.367045641526529964, -70.32522074196269557 ) ) ;
#34495=CARTESIAN_POINT ( 'NONE',  ( 63.26997363883779713, 1.264791438333819906, -68.87905435786350949 ) ) ;
#34498=CARTESIAN_POINT ( 'NONE',  ( 68.13393739769620083, -42.61618894467930119, -60.14999999999999858 ) ) ;
#34503=CARTESIAN_POINT ( 'NONE',  ( 71.45332619318591583, 1.096305581841150012, -70.60102141519101338 ) ) ;
#34511=CARTESIAN_POINT ( 'NONE',  ( 71.44807725908989937, 0.8904513541338869853, -70.65165619965230803 ) ) ;
#34525=CARTESIAN_POINT ( 'NONE',  ( 71.46698656264879901, 1.308647200627810259, -60.89791552425909771 ) ) ;
#34551=CARTESIAN_POINT ( 'NONE',  ( 64.92397392854900318, 1.188582381068100213, -60.69479001402090290 ) ) ;
#34581=CARTESIAN_POINT ( 'NONE',  ( 72.79675206836721202, 1.372372808637219999, -68.90857576278480678 ) ) ;
#34583=CARTESIAN_POINT ( 'NONE',  ( 73.13235683752471061, 1.096291039689170077, -62.40636042108670267 ) ) ;
#34593=PLANE ( 'NONE',  #34416 ) ;
#34615=DIRECTION ( 'NONE',  ( 0.000000000000000000, 1.000000000000000000, 0.000000000000000000 ) ) ;
#34619=ORIENTED_EDGE ( 'NONE', *, *, #26161, .F. ) ;
#34643=CARTESIAN_POINT ( 'NONE',  ( 71.29455428839979447, 0.9209334348186318797, -60.54988453772739376 ) ) ;
#34645=CARTESIAN_POINT ( 'NONE',  ( 72.75077066479440191, 1.389801772588449946, -62.42722031148289830 ) ) ;
#34658=CARTESIAN_POINT ( 'NONE',  ( 63.52011431889719972, 1.391252479931859964, -68.77264296518760034 ) ) ;
#34670=EDGE_CURVE ( 'NONE', #33885, #19450, #18720, .T. ) ;
#34674=CARTESIAN_POINT ( 'NONE',  ( 63.15096886846599489, 0.8925687589132619282, -62.30780775221810330 ) ) ;
#34688=CARTESIAN_POINT ( 'NONE',  ( 71.33393739769628894, 10.88381105532070059, -69.84999999999999432 ) ) ;
#34705=CARTESIAN_POINT ( 'NONE',  ( 63.71314823352749812, 1.019773975906300034, -61.59278770926529489 ) ) ;
#34709=CARTESIAN_POINT ( 'NONE',  ( 73.19748134167231512, 1.099973129953850215, -68.78515728267289830 ) ) ;
#34719=ORIENTED_EDGE ( 'NONE', *, *, #36465, .F. ) ;
#34734=CARTESIAN_POINT ( 'NONE',  ( 64.73021287799150514, 1.402114179617120149, -70.19765531490459409 ) ) ;
#34742=CARTESIAN_POINT ( 'NONE',  ( 71.56069454884870140, 1.310552739454249993, -70.35422282388560689 ) ) ;
#34750=AXIS2_PLACEMENT_3D ( 'NONE', #18237, #26606, #34204 ) ;
#34761=CARTESIAN_POINT ( 'NONE',  ( 71.48394854028050815, 1.096932441169210071, -70.58143231363629866 ) ) ;
#34782=CARTESIAN_POINT ( 'NONE',  ( 64.93393739769619799, 1.883811055320669947, -60.94999999999999574 ) ) ;
#34808=EDGE_LOOP ( 'NONE', ( #13221, #4222, #10311, #20158, #48045 ) ) ;
#34810=CARTESIAN_POINT ( 'NONE',  ( 64.82636581786128716, 1.096153228089730147, -60.69147900812899366 ) ) ;
#34829=CIRCLE ( 'NONE', #3911, 0.5000000000000004441 ) ;
#34844=CARTESIAN_POINT ( 'NONE',  ( 72.87455824417580175, 1.326134026835569912, -62.35486255807249734 ) ) ;
#34846=CARTESIAN_POINT ( 'NONE',  ( 68.13393739769624347, 1.383811055320669947, -71.15000000000000568 ) ) ;
#34847=CARTESIAN_POINT ( 'NONE',  ( 68.13393739769620083, 1.383811055320669947, -65.65000000000000568 ) ) ;
#34866=DIRECTION ( 'NONE',  ( 0.000000000000000000, 0.000000000000000000, 1.000000000000000000 ) ) ;
#34880=DIRECTION ( 'NONE',  ( 0.000000000000000000, 0.000000000000000000, 1.000000000000000000 ) ) ;
#34889=ORIENTED_EDGE ( 'NONE', *, *, #36465, .T. ) ;
#34907=CARTESIAN_POINT ( 'NONE',  ( 71.01106396815980304, 1.383811055320669947, -60.95624653118409242 ) ) ;
#34910=CIRCLE ( 'NONE', #21516, 0.5000000000000004441 ) ;
#34914=EDGE_LOOP ( 'NONE', ( #20466, #38520, #44881, #25745 ) ) ;
#34960=EDGE_CURVE ( 'NONE', #41914, #4949, #41354, .T. ) ;
#34964=CARTESIAN_POINT ( 'NONE',  ( 63.44472555293038596, 1.153605328059160051, -61.96710904643580164 ) ) ;
#34968=CARTESIAN_POINT ( 'NONE',  ( 73.23379646625190276, 0.8840451408750739093, -68.81103260973570457 ) ) ;
#35001=CARTESIAN_POINT ( 'NONE',  ( 71.71886329086420631, 0.9254890127224509877, -70.46161719983020078 ) ) ;
#35008=CARTESIAN_POINT ( 'NONE',  ( 63.29941945011370308, 1.188860127980280179, -69.06196878611640955 ) ) ;
#35012=EDGE_CURVE ( 'NONE', #38406, #51314, #33780, .T. ) ;
#35017=CARTESIAN_POINT ( 'NONE',  ( 71.27608674571190761, 1.386446979194299933, -70.29126806847389730 ) ) ;
#35024=CARTESIAN_POINT ( 'NONE',  ( 71.52074786344320501, 0.8966068345641470261, -70.60278586552519187 ) ) ;
#35026=ORIENTED_EDGE ( 'NONE', *, *, #45482, .T. ) ;
#35039=DIRECTION ( 'NONE',  ( 0.7071067811865457964, 0.7071067811865492381, 0.000000000000000000 ) ) ;
#35045=CARTESIAN_POINT ( 'NONE',  ( 63.08005232011709751, 0.8859637708054499683, -68.88406027352149863 ) ) ;
#35065=CARTESIAN_POINT ( 'NONE',  ( 64.92362553771700107, 1.265401080857980087, -60.77621068871049204 ) ) ;
#35079=AXIS2_PLACEMENT_3D ( 'NONE', #20408, #12838, #20667 ) ;
#35089=CIRCLE ( 'NONE', #38472, 0.5000000000000000000 ) ;
#35093=EDGE_LOOP ( 'NONE', ( #35998, #9026, #37352, #35251, #2158, #27630, #38730, #6701, #45953, #27086, #44944, #18162, #38826, #31848 ) ) ;
#35099=CARTESIAN_POINT ( 'NONE',  ( 72.78175560864708871, 1.385702546077169917, -62.52592200326169092 ) ) ;
#35104=EDGE_CURVE ( 'NONE', #25175, #8004, #1158, .T. ) ;
#35152=CARTESIAN_POINT ( 'NONE',  ( 65.27736602627911111, 1.383811055320669947, -60.94999999999999574 ) ) ;
#35163=DIRECTION ( 'NONE',  ( -0.000000000000000000, 1.000000000000000000, 0.000000000000000000 ) ) ;
#35165=CARTESIAN_POINT ( 'NONE',  ( 71.12477309692330607, 1.336371993404959824, -60.77157093307350522 ) ) ;
#35167=CARTESIAN_POINT ( 'NONE',  ( 72.42914715746668719, 1.346167254499869959, -61.62073875063699546 ) ) ;
#35173=ORIENTED_EDGE ( 'NONE', *, *, #46268, .T. ) ;
#35227=CARTESIAN_POINT ( 'NONE',  ( 63.27581436415109550, 1.132579237369250036, -62.21177178793440277 ) ) ;
#35231=CARTESIAN_POINT ( 'NONE',  ( 72.80030139158668590, 1.384887413063060180, -68.61455525072810246 ) ) ;
#35251=ORIENTED_EDGE ( 'NONE', *, *, #14250, .T. ) ;
#35256=CARTESIAN_POINT ( 'NONE',  ( 64.93393739769619799, 1.530257664727401767, -69.99644660940670349 ) ) ;
#35270=CARTESIAN_POINT ( 'NONE',  ( 71.49710702210251156, 1.370387345317799932, -70.28519118483690420 ) ) ;
#35280=CARTESIAN_POINT ( 'NONE',  ( 64.60839616882741154, 0.9151442779661310700, -70.50513874227569033 ) ) ;
#35286=CARTESIAN_POINT ( 'NONE',  ( 71.48076113803239195, 1.264121749638649872, -70.45005197993600632 ) ) ;
#35315=CARTESIAN_POINT ( 'NONE',  ( 63.43393739769620510, 1.883811055320669947, -65.65000000000000568 ) ) ;
#35332=CARTESIAN_POINT ( 'NONE',  ( 65.09799605061490979, 1.383357884654609959, -60.97108096920410247 ) ) ;
#35338=CARTESIAN_POINT ( 'NONE',  ( 72.12455669199461283, 1.010053820890669973, -70.13159119767689731 ) ) ;
#35363=CARTESIAN_POINT ( 'NONE',  ( 73.04596072059979406, 1.186701509386330011, -62.36552507365149722 ) ) ;
#35406=CARTESIAN_POINT ( 'NONE',  ( 63.04027743911709791, 0.9947083095259759977, -68.80546575785609775 ) ) ;
#35414=LINE ( 'NONE', #35152, #17302 ) ;
#35428=CARTESIAN_POINT ( 'NONE',  ( 71.04878173523039209, 1.375383258925270136, -60.85412179317820147 ) ) ;
#35432=CARTESIAN_POINT ( 'NONE',  ( 72.51559007951500746, 1.439519383694849886, -61.97453994048029813 ) ) ;
#35434=EDGE_CURVE ( 'NONE', #49378, #6409, #36212, .T. ) ;
#35448=VERTEX_POINT ( 'NONE', #44343 ) ;
#35460=DIRECTION ( 'NONE',  ( -0.7071067811865475727, 0.000000000000000000, 0.7071067811865475727 ) ) ;
#35499=CARTESIAN_POINT ( 'NONE',  ( 72.87639502376930523, 1.370118064600889918, -68.71049874078630637 ) ) ;
#35525=CARTESIAN_POINT ( 'NONE',  ( 64.43393739769619799, 11.38381105532070059, -68.84999999999999432 ) ) ;
#35535=CARTESIAN_POINT ( 'NONE',  ( 71.57077554288350996, 1.229987811083010030, -70.43721585241399907 ) ) ;
#35539=SURFACE_STYLE_USAGE ( .BOTH. , #19805 ) ;
#35541=CARTESIAN_POINT ( 'NONE',  ( 63.22121223625129716, 0.9369374701296400154, -69.09468190869459647 ) ) ;
#35544=DIRECTION ( 'NONE',  ( 0.000000000000000000, 1.000000000000000000, 0.000000000000000000 ) ) ;
#35547=ORIENTED_EDGE ( 'NONE', *, *, #24931, .T. ) ;
#35551=CARTESIAN_POINT ( 'NONE',  ( 71.60000756020500035, 0.9395704634982890990, -70.54765821028050254 ) ) ;
#35580=CARTESIAN_POINT ( 'NONE',  ( 63.15932386229340523, 0.8936201581567920771, -69.00461532610479765 ) ) ;
#35581=CARTESIAN_POINT ( 'NONE',  ( 71.33393739769628894, 1.883811055320669947, -69.84999999999999432 ) ) ;
#35584=LINE ( 'NONE', #43958, #3567 ) ;
#35598=CARTESIAN_POINT ( 'NONE',  ( 65.11238450761909746, 1.383161449028130097, -60.96613084263369586 ) ) ;
#35614=AXIS2_PLACEMENT_3D ( 'NONE', #36907, #1270, #48982 ) ;
#35624=B_SPLINE_CURVE_WITH_KNOTS ( 'NONE', 3,
 ( #51567, #27954, #48672, #39521, #16690, #20602, #12250, #32647, #11748, #36597, #12776, #36087, #32386, #8061, #20347, #24267 ),
 .UNSPECIFIED., .F., .F.,
 ( 4, 2, 2, 2, 2, 2, 2, 4 ),
 ( 0.000000000000000000, 0.07216186899278899392, 0.1546325764131200042, 0.2061767685508260062, 0.2319488646196799786, 0.2731842183298449633, 0.3391607842661090166, 0.4123535371016520124 ),
 .UNSPECIFIED. ) ;
#35631=CARTESIAN_POINT ( 'NONE',  ( 72.73458218292580568, 1.393731187554809958, -62.48946499964799983 ) ) ;
#35635=VECTOR ( 'NONE', #21144, 1000.000000000000000 ) ;
#35637=CARTESIAN_POINT ( 'NONE',  ( 64.83879995576880617, 1.326134026835569912, -70.39062084647959239 ) ) ;
#35658=CIRCLE ( 'NONE', #35614, 0.5000000000000004441 ) ;
#35674=CARTESIAN_POINT ( 'NONE',  ( 63.43729419656740731, 1.382840740411490188, -68.63401718432778864 ) ) ;
#35678=EDGE_LOOP ( 'NONE', ( #42421, #14143, #7278, #42033, #19348, #31485 ) ) ;
#35695=CARTESIAN_POINT ( 'NONE',  ( 71.40678801050209756, 1.186856010528209993, -60.73114026433219692 ) ) ;
#35697=CARTESIAN_POINT ( 'NONE',  ( 72.61552859537209770, 1.010053820890850051, -61.65938070570050655 ) ) ;
#35730=DIRECTION ( 'NONE',  ( 0.000000000000000000, -1.000000000000000000, 0.000000000000000000 ) ) ;
#35740=CARTESIAN_POINT ( 'NONE',  ( 63.31614497232158811, 1.328073773609210084, -62.51929651814780442 ) ) ;
#35744=CARTESIAN_POINT ( 'NONE',  ( 64.14331810339589879, 1.010053820890960186, -61.16840880232479805 ) ) ;
#35756=CARTESIAN_POINT ( 'NONE',  ( 72.78346131865960444, 1.386342629514219826, -68.66646381051069170 ) ) ;
#35788=CARTESIAN_POINT ( 'NONE',  ( 71.83406239764909174, 11.38381102407070067, -62.44999999999999574 ) ) ;
#35792=CARTESIAN_POINT ( 'NONE',  ( 72.16319864705920395, 1.346167254499869959, -69.94520975977049204 ) ) ;
#35796=CARTESIAN_POINT ( 'NONE',  ( 63.27438507250460020, 1.187296498006439993, -69.02170307486190381 ) ) ;
#35804=CARTESIAN_POINT ( 'NONE',  ( 64.60023990589328946, 0.9543424661148549593, -60.80063435388460391 ) ) ;
#35806=CARTESIAN_POINT ( 'NONE',  ( 71.62124566564099837, 0.9425424353906030062, -70.53248918539379986 ) ) ;
#35810=CARTESIAN_POINT ( 'NONE',  ( 64.64302830678670375, 0.9098571636355720083, -60.77008670988870165 ) ) ;
#35832=ORIENTED_EDGE ( 'NONE', *, *, #30989, .F. ) ;
#35878=CARTESIAN_POINT ( 'NONE',  ( 73.11690592692660573, 0.8925687589132640376, -62.30780775221820278 ) ) ;
#35889=ORIENTED_EDGE ( 'NONE', *, *, #48865, .T. ) ;
#35907=EDGE_CURVE ( 'NONE', #23424, #24662, #21325, .T. ) ;
#35910=CARTESIAN_POINT ( 'NONE',  ( 71.15040120820690106, 1.386342629514219826, -61.00047607903670155 ) ) ;
#35919=CARTESIAN_POINT ( 'NONE',  ( 63.20675433611359750, 1.270877794983130027, -68.75550371754310675 ) ) ;
#35938=CARTESIAN_POINT ( 'NONE',  ( 71.50903575780739629, 0.9989215084293960878, -60.69776330465320058 ) ) ;
#35939=CARTESIAN_POINT ( 'NONE',  ( 72.13898961932780196, 1.457833794292699992, -61.50804513633939763 ) ) ;
#35987=CARTESIAN_POINT ( 'NONE',  ( 63.07934790479939835, 0.9219904752505979628, -62.41704322431660046 ) ) ;
#35992=CARTESIAN_POINT ( 'NONE',  ( 68.13393739769620083, 0.8838110553206759423, -60.14999999999999858 ) ) ;
#35998=ORIENTED_EDGE ( 'NONE', *, *, #35104, .F. ) ;
#36013=ORIENTED_EDGE ( 'NONE', *, *, #11532, .F. ) ;
#36039=CARTESIAN_POINT ( 'NONE',  ( 72.55316574448160338, 1.396295651964220008, -69.41420804701510860 ) ) ;
#36056=CARTESIAN_POINT ( 'NONE',  ( 71.50564047255809896, 1.187296498006439993, -70.50955232519169158 ) ) ;
#36066=DIRECTION ( 'NONE',  ( 0.000000000000000000, 1.000000000000000000, 0.000000000000000000 ) ) ;
#36085=CARTESIAN_POINT ( 'NONE',  ( 64.93393739769616957, 11.38381105532080184, -61.44999999999993889 ) ) ;
#36087=CARTESIAN_POINT ( 'NONE',  ( 64.74712693194929614, 0.8966068345641450277, -70.60278586552529134 ) ) ;
#36139=AXIS2_PLACEMENT_3D ( 'NONE', #47073, #27129, #14825 ) ;
#36152=CYLINDRICAL_SURFACE ( 'NONE', #25167, 0.5000000000000049960 ) ;
#36162=CARTESIAN_POINT ( 'NONE',  ( 71.25658036288379549, 1.391252479931859964, -61.03617692120100457 ) ) ;
#36171=CARTESIAN_POINT ( 'NONE',  ( 63.28287142701668699, 1.331842543267529821, -68.70530175958410268 ) ) ;
#36184=CARTESIAN_POINT ( 'NONE',  ( 71.30558087559749936, 1.190292248953970011, -70.62687270921169613 ) ) ;
#36187=CARTESIAN_POINT ( 'NONE',  ( 64.93393739769619799, 1.883811055320669947, -62.44999999999999574 ) ) ;
#36192=CARTESIAN_POINT ( 'NONE',  ( 71.51817256006181367, 0.9307121176571799825, -60.69545425604199806 ) ) ;
#36194=CARTESIAN_POINT ( 'NONE',  ( 72.14208904168791037, 1.345243094457279964, -61.33716833010870317 ) ) ;
#36197=CARTESIAN_POINT ( 'NONE',  ( 65.14310169846920928, 1.336371993404949832, -70.52842906692660563 ) ) ;
#36212=LINE ( 'NONE', #47519, #38040 ) ;
#36222=CARTESIAN_POINT ( 'NONE',  ( 64.75240447675760436, 1.412311545208970065, -70.17188921921470524 ) ) ;
#36230=DIRECTION ( 'NONE',  ( 0.000000000000000000, 0.000000000000000000, 1.000000000000000000 ) ) ;
#36239=CARTESIAN_POINT ( 'NONE',  ( 63.08453170404659716, 0.9940423591679348192, -62.42346963566990325 ) ) ;
#36240=FACE_OUTER_BOUND ( 'NONE', #27381, .T. ) ;
#36246=B_SPLINE_CURVE_WITH_KNOTS ( 'NONE', 3,
 ( #45293, #1268, #49496, #25351, #32953, #29039, #5468, #9646, #13583, #29548, #9134, #45034, #17761, #25089, #33732, #49745 ),
 .UNSPECIFIED., .F., .F.,
 ( 4, 2, 2, 2, 2, 2, 2, 4 ),
 ( -1.165733999999999982E-15, 0.07319275283555999601, 0.1391693187718409941, 0.1804046724820169978, 0.2061767685508770209, 0.2577209606885970117, 0.3401916681089490191, 0.4123535371017569839 ),
 .UNSPECIFIED. ) ;
#36248=CARTESIAN_POINT ( 'NONE',  ( 64.76726729265010363, 1.264689361399219836, -60.86115090893359536 ) ) ;
#36250=CARTESIAN_POINT ( 'NONE',  ( 63.55847417696450208, 1.399433130755639798, -62.41600958228519858 ) ) ;
#36252=CARTESIAN_POINT ( 'NONE',  ( 74.13393739769620083, 0.8838110553206759423, -65.65000000000000568 ) ) ;
#36261=EDGE_CURVE ( 'NONE', #19147, #21117, #20462, .T. ) ;
#36287=ADVANCED_FACE ( 'NONE', ( #1232 ), #32650, .T. ) ;
#36290=CARTESIAN_POINT ( 'NONE',  ( 72.49788296046230585, 1.442158793902679870, -69.35604527063249236 ) ) ;
#36300=CIRCLE ( 'NONE', #30436, 0.5000000000000002220 ) ;
#36391=CARTESIAN_POINT ( 'NONE',  ( 63.49388541862201407, 1.387412027389909985, -62.60488565353588797 ) ) ;
#36402=DIRECTION ( 'NONE',  ( -1.000000000000000000, 0.000000000000000000, 0.000000000000000000 ) ) ;
#36412=CARTESIAN_POINT ( 'NONE',  ( 70.99050876911339003, 1.383811055320669947, -60.94999999999999574 ) ) ;
#36422=CARTESIAN_POINT ( 'NONE',  ( 63.08005232011719698, 0.8859637708054489691, -68.88406027352149863 ) ) ;
#36434=CARTESIAN_POINT ( 'NONE',  ( 71.06936022730370439, 1.374300485541529948, -70.43861994117489189 ) ) ;
#36435=PLANE ( 'NONE',  #12546 ) ;
#36440=B_SPLINE_CURVE_WITH_KNOTS ( 'NONE', 3,
 ( #48206, #12309, #28268, #44269, #8375, #24845, #17019, #1025, #5229, #29053, #40342, #4436, #44529, #12832, #48728, #49252, #45048, #9418, #17276, #24324 ),
 .UNSPECIFIED., .F., .F.,
 ( 4, 2, 2, 2, 2, 2, 2, 2, 2, 4 ),
 ( 0.000000000000000000, 0.08842663232653856509, 0.2261948956664324439, 0.3749999999999999445, 0.5000000000000005551, 0.5625000000000004441, 0.6625000000000004219, 0.7983826544682063320, 0.9363829142882441614, 1.000000000000000000 ),
 .UNSPECIFIED. ) ;
#36445=CARTESIAN_POINT ( 'NONE',  ( 71.19853741683878923, 1.383922910988889976, -60.98106092919370269 ) ) ;
#36447=CARTESIAN_POINT ( 'NONE',  ( 71.60533839042560089, 1.134292167764330062, -60.81357835167419523 ) ) ;
#36449=CARTESIAN_POINT ( 'NONE',  ( 64.96708350509699414, 1.267233196669030004, -70.54626486029009413 ) ) ;
#36465=EDGE_CURVE ( 'NONE', #29849, #11777, #22970, .T. ) ;
#36478=CARTESIAN_POINT ( 'NONE',  ( 63.99083253892909084, 1.458411868502019981, -69.65665569611660146 ) ) ;
#36488=EDGE_LOOP ( 'NONE', ( #18323, #3409, #18430, #6554, #37737, #30322 ) ) ;
#36493=CARTESIAN_POINT ( 'NONE',  ( 63.46757340380580814, 1.384887413063070172, -62.68544474927200127 ) ) ;
#36503=CARTESIAN_POINT ( 'NONE',  ( 64.89503925317040967, 1.371509258145880095, -60.97885864891310348 ) ) ;
#36552=CARTESIAN_POINT ( 'NONE',  ( 72.43587670424329872, 1.060191324942699964, -69.83271228958450649 ) ) ;
#36564=CARTESIAN_POINT ( 'NONE',  ( 64.01157812772038369, 1.056850087111250058, -61.28959142989100428 ) ) ;
#36597=CARTESIAN_POINT ( 'NONE',  ( 64.79174514991440503, 0.8925687589132599298, -70.63296852923029689 ) ) ;
#36600=DIRECTION ( 'NONE',  ( 0.000000000000000000, 0.000000000000000000, -1.000000000000000000 ) ) ;
#36605=CARTESIAN_POINT ( 'NONE',  ( 63.77399527780870869, 1.113947854059440079, -69.76572286218529939 ) ) ;
#36615=DIRECTION ( 'NONE',  ( 0.000000000000000000, 0.000000000000000000, -1.000000000000000000 ) ) ;
#36652=ADVANCED_FACE ( 'NONE', ( #10389 ), #38167, .T. ) ;
#36657=DIRECTION ( 'NONE',  ( -1.000000000000000000, 0.000000000000000000, 0.000000000000000000 ) ) ;
#36664=ORIENTED_EDGE ( 'NONE', *, *, #26021, .F. ) ;
#36671=CARTESIAN_POINT ( 'NONE',  ( 71.17189893730710537, 1.387131204727290124, -61.00757424182599920 ) ) ;
#36680=CARTESIAN_POINT ( 'NONE',  ( 63.13746035244330557, 0.8910129994591549085, -68.97194292341539779 ) ) ;
#36695=CARTESIAN_POINT ( 'NONE',  ( 71.23719564129540061, 1.194703186106690129, -70.66446396659920026 ) ) ;
#36699=CARTESIAN_POINT ( 'NONE',  ( 63.43393739769620510, 1.883811055320669947, -68.84999999999999432 ) ) ;
#36701=CARTESIAN_POINT ( 'NONE',  ( 73.08617409304301304, 0.9989215084294049696, -69.02509836011120115 ) ) ;
#36704=CARTESIAN_POINT ( 'NONE',  ( 73.08275130671789555, 1.274277262446069869, -62.58867475943009850 ) ) ;
#36706=CARTESIAN_POINT ( 'NONE',  ( 71.33702656696020483, 1.265664290790580182, -60.77244468760530083 ) ) ;
#36707=DIRECTION ( 'NONE',  ( 0.000000000000000000, 0.000000000000000000, -1.000000000000000000 ) ) ;
#36708=CARTESIAN_POINT ( 'NONE',  ( 72.23076864380078632, 1.112168069084249922, -61.27267649081910150 ) ) ;
#36709=CARTESIAN_POINT ( 'NONE',  ( 71.33393739769628894, 11.38381105532070059, -61.94999999999999574 ) ) ;
#36710=CARTESIAN_POINT ( 'NONE',  ( 65.00498282733049393, 1.269319268680890067, -70.56549354633131088 ) ) ;
#36712=ORIENTED_EDGE ( 'NONE', *, *, #34069, .T. ) ;
#36713=CARTESIAN_POINT ( 'NONE',  ( 71.33393739769809372, 11.38381103969570063, -61.94987500004359759 ) ) ;
#36716=EDGE_LOOP ( 'NONE', ( #49884, #8758, #51117 ) ) ;
#36722=CARTESIAN_POINT ( 'NONE',  ( 64.93393739763529027, 1.883811055311890081, -62.44999999997569518 ) ) ;
#36752=CARTESIAN_POINT ( 'NONE',  ( 63.11000452699359897, 0.9945465939392541532, -62.38364600848370145 ) ) ;
#36757=CARTESIAN_POINT ( 'NONE',  ( 72.68796522584510456, 1.404650034022369987, -62.35426166056780062 ) ) ;
#36761=CARTESIAN_POINT ( 'NONE',  ( 64.80090148641959047, 1.186614556332910020, -60.76691531849380112 ) ) ;
#36774=VERTEX_POINT ( 'NONE', #51259 ) ;
#36815=CARTESIAN_POINT ( 'NONE',  ( 72.31224245611890922, 1.117804454683279936, -69.95018517907431033 ) ) ;
#36816=CARTESIAN_POINT ( 'NONE',  ( 71.45588032111159293, 0.8910129994591539093, -60.65352295474710331 ) ) ;
#36820=CARTESIAN_POINT ( 'NONE',  ( 72.40605974471309025, 1.033004162168289941, -69.86315739208511388 ) ) ;
#36831=CARTESIAN_POINT ( 'NONE',  ( 64.00784214253330617, 1.443555314919450216, -61.59234650647290010 ) ) ;
#36852=ORIENTED_EDGE ( 'NONE', *, *, #22435, .F. ) ;
#36874=VECTOR ( 'NONE', #41912, 1000.000000000000000 ) ;
#36877=CARTESIAN_POINT ( 'NONE',  ( 64.02817266311009803, 1.026090475080779996, -70.02573918086800120 ) ) ;
#36889=DIRECTION ( 'NONE',  ( 0.000000000000000000, -1.000000000000000000, 0.000000000000000000 ) ) ;
#36890=CARTESIAN_POINT ( 'NONE',  ( 68.13393739769620083, 1.383811055320669947, -65.65000000000000568 ) ) ;
#36899=DIRECTION ( 'NONE',  ( -0.8545454545454580497, -2.306495000000000021E-16, 0.5193766129849289870 ) ) ;
#36907=CARTESIAN_POINT ( 'NONE',  ( 64.93393739769619799, 10.88381105532070059, -69.34999999999999432 ) ) ;
#36949=CARTESIAN_POINT ( 'NONE',  ( 73.17080802144360518, 1.198183261254770038, -68.71131498411249083 ) ) ;
#36952=CARTESIAN_POINT ( 'NONE',  ( 63.22191407479270708, 1.186701509386330011, -68.93447492634859941 ) ) ;
#36968=CARTESIAN_POINT ( 'NONE',  ( 71.20883305211729919, 1.369885150286779929, -70.38694600888931063 ) ) ;
#36974=CARTESIAN_POINT ( 'NONE',  ( 72.91105647262868672, 1.325839985408290067, -68.86912414701170349 ) ) ;
#36977=CARTESIAN_POINT ( 'NONE',  ( 73.09272852564158995, 1.276058558775519991, -62.60937635806730839 ) ) ;
#36979=CARTESIAN_POINT ( 'NONE',  ( 71.60000756020500035, 0.9395704634982890990, -60.75234178971950172 ) ) ;
#36981=CARTESIAN_POINT ( 'NONE',  ( 71.61582913010290952, 1.408710407022130129, -61.13660121446530127 ) ) ;
#36983=CARTESIAN_POINT ( 'NONE',  ( 64.90928650851499526, 1.188042061556800144, -70.59681938162209747 ) ) ;
#36997=CARTESIAN_POINT ( 'NONE',  ( 68.13393739769620083, 0.8838110553206759423, -65.65000000000000568 ) ) ;
#37003=DIRECTION ( 'NONE',  ( 0.000000000000000000, 1.000000000000000000, 0.000000000000000000 ) ) ;
#37026=CARTESIAN_POINT ( 'NONE',  ( 63.22121223625140374, 0.9369374701296400154, -62.20531809130540069 ) ) ;
#37046=ORIENTED_EDGE ( 'NONE', *, *, #34670, .T. ) ;
#37055=CARTESIAN_POINT ( 'NONE',  ( 64.88669131378958355, 1.400446703426900141, -61.07889042780649902 ) ) ;
#37083=CARTESIAN_POINT ( 'NONE',  ( 72.72018323891309421, 1.017423949636760083, -69.51966756621098398 ) ) ;
#37098=CARTESIAN_POINT ( 'NONE',  ( 64.36548184775359971, 0.9973858971043548793, -60.98020530084170332 ) ) ;
#37099=ORIENTED_EDGE ( 'NONE', *, *, #44404, .T. ) ;
#37143=CARTESIAN_POINT ( 'NONE',  ( 63.83267354985680697, 1.033012681683360023, -69.83402047387529876 ) ) ;
#37153=FACE_OUTER_BOUND ( 'NONE', #12175, .T. ) ;
#37188=CARTESIAN_POINT ( 'NONE',  ( 63.43393739769620510, 1.383811055320669947, -62.79342862858290886 ) ) ;
#37195=CARTESIAN_POINT ( 'NONE',  ( 72.83393739769620367, 1.883811055320669947, -65.65000000000000568 ) ) ;
#37209=CARTESIAN_POINT ( 'NONE',  ( 65.17800597998859757, 1.373356196620459935, -60.86873524938349789 ) ) ;
#37233=CARTESIAN_POINT ( 'NONE',  ( 71.17189893730710537, 1.387131204727280132, -70.29242575817399086 ) ) ;
#37238=CARTESIAN_POINT ( 'NONE',  ( 73.04443511092439678, 0.9036513197889520788, -69.09785636402040154 ) ) ;
#37245=CARTESIAN_POINT ( 'NONE',  ( 71.65879992446289748, 1.379674774869709797, -61.09137707357210445 ) ) ;
#37246=CARTESIAN_POINT ( 'NONE',  ( 64.43393739769619799, 10.88381105532070059, -68.84999999999999432 ) ) ;
#37247=CARTESIAN_POINT ( 'NONE',  ( 64.92520290936280958, 0.8850831926798630178, -70.72000234600830026 ) ) ;
#37280=DIRECTION ( 'NONE',  ( 0.000000000000000000, 1.000000000000000000, 0.000000000000000000 ) ) ;
#37287=CARTESIAN_POINT ( 'NONE',  ( 63.41538649190439969, 1.369535599030029971, -62.52785204568030508 ) ) ;
#37297=CARTESIAN_POINT ( 'NONE',  ( 63.66395377270059441, 1.424118951467219896, -69.15359763556290318 ) ) ;
#37314=CARTESIAN_POINT ( 'NONE',  ( 64.12726891144080810, 1.458412159422780130, -61.50690654180700534 ) ) ;
#37326=CARTESIAN_POINT ( 'NONE',  ( 73.13559359734860266, 0.8904513541338849869, -68.96413986139360475 ) ) ;
#37342=CARTESIAN_POINT ( 'NONE',  ( 72.74974170911090710, 1.318402576460560027, -69.23505850801080896 ) ) ;
#37352=ORIENTED_EDGE ( 'NONE', *, *, #44738, .F. ) ;
#37354=CARTESIAN_POINT ( 'NONE',  ( 64.36068579096159681, 0.9644290104359679594, -60.98409269229880181 ) ) ;
#37361=DIRECTION ( 'NONE',  ( 0.000000000000000000, 0.000000000000000000, -1.000000000000000000 ) ) ;
#37394=CARTESIAN_POINT ( 'NONE',  ( 72.43519100933379207, 1.033013263524900083, -61.46596897695270201 ) ) ;
#37396=CARTESIAN_POINT ( 'NONE',  ( 64.31741031388310148, 1.334515466074710055, -70.11420104233359041 ) ) ;
#37446=EDGE_LOOP ( 'NONE', ( #44147, #29345, #4543, #15646 ) ) ;
#37449=ADVANCED_FACE ( 'NONE', ( #34291 ), #1333, .F. ) ;
#37459=LINE ( 'NONE', #25643, #36874 ) ;
#37463=CARTESIAN_POINT ( 'NONE',  ( 64.92520290936280958, 0.8850831926798630178, -60.57999765399179637 ) ) ;
#37470=CARTESIAN_POINT ( 'NONE',  ( 73.26121012496899709, 0.9212109678634080590, -68.76625967790960203 ) ) ;
#37474=DIRECTION ( 'NONE',  ( -0.5765530599821108160, 0.1342272854595029929, -0.8059588108975778153 ) ) ;
#37491=CARTESIAN_POINT ( 'NONE',  ( 72.74776047649530142, 1.391252479931859964, -68.77264296518760034 ) ) ;
#37494=CARTESIAN_POINT ( 'NONE',  ( 72.87639502376930523, 1.370118064600909902, -62.58950125921369789 ) ) ;
#37498=CARTESIAN_POINT ( 'NONE',  ( 71.74419295952090181, 1.145379646617759928, -60.90832955879639599 ) ) ;
#37501=CARTESIAN_POINT ( 'NONE',  ( 64.81394005445639550, 0.9259537755896120048, -70.64777040355440363 ) ) ;
#37513=CARTESIAN_POINT ( 'NONE',  ( 71.33393739769628894, 11.38381105532070059, -68.84999999999999432 ) ) ;
#37538=CARTESIAN_POINT ( 'NONE',  ( 63.43166809737898859, 1.369719003397489976, -62.48691920258249155 ) ) ;
#37539=CARTESIAN_POINT ( 'NONE',  ( 68.13393739769620083, -42.11618894467930119, -65.65000000000000568 ) ) ;
#37548=CARTESIAN_POINT ( 'NONE',  ( 63.73255073857669828, 1.426104593066200188, -69.34551121535889706 ) ) ;
#37560=ORIENTED_EDGE ( 'NONE', *, *, #29160, .F. ) ;
#37566=CARTESIAN_POINT ( 'NONE',  ( 64.93393739769599904, 1.396834109478129804, -61.06337307536569625 ) ) ;
#37586=DIRECTION ( 'NONE',  ( 0.7071067811865475727, 0.000000000000000000, -0.7071067811865475727 ) ) ;
#37589=CARTESIAN_POINT ( 'NONE',  ( 72.79388427887360535, 1.241979851175039951, -69.28847831928310086 ) ) ;
#37593=CARTESIAN_POINT ( 'NONE',  ( 72.33393739769479680, 10.88381105532070059, -68.85000000000388809 ) ) ;
#37608=CARTESIAN_POINT ( 'NONE',  ( 64.45847733817470271, 1.439519383694989996, -61.26834731818230040 ) ) ;
#37610=DIRECTION ( 'NONE',  ( -1.000000000000000000, 0.000000000000000000, 0.000000000000000000 ) ) ;
#37621=EDGE_LOOP ( 'NONE', ( #48327, #8561, #23084 ) ) ;
#37631=AXIS2_PLACEMENT_3D ( 'NONE', #41850, #2020, #30554 ) ;
#37636=VECTOR ( 'NONE', #11226, 1000.000000000000000 ) ;
#37650=CARTESIAN_POINT ( 'NONE',  ( 63.97355303201310051, 1.199411168077020085, -69.93688014721760737 ) ) ;
#37651=FACE_OUTER_BOUND ( 'NONE', #45743, .T. ) ;
#37707=CARTESIAN_POINT ( 'NONE',  ( 63.93393739769619089, 1.883811055320669947, -62.44999999999999574 ) ) ;
#37723=ADVANCED_FACE ( 'NONE', ( #37153 ), #21148, .T. ) ;
#37731=CARTESIAN_POINT ( 'NONE',  ( 73.26121012496899709, 0.8838110553206759423, -68.76625967790960203 ) ) ;
#37737=ORIENTED_EDGE ( 'NONE', *, *, #41996, .F. ) ;
#37748=CARTESIAN_POINT ( 'NONE',  ( 64.95277593799399085, 1.369976237678190101, -60.95504431261769440 ) ) ;
#37753=CARTESIAN_POINT ( 'NONE',  ( 72.92486918121929307, 1.326324093417220240, -68.83951043167449768 ) ) ;
#37756=CARTESIAN_POINT ( 'NONE',  ( 73.06112045927889653, 1.270877794983130027, -62.54449628245689752 ) ) ;
#37760=CARTESIAN_POINT ( 'NONE',  ( 71.42907483962369497, 1.326134026835569912, -60.90937915352040477 ) ) ;
#37766=CARTESIAN_POINT ( 'NONE',  ( 64.90488303983279650, 1.264791438333819906, -70.51396375885850887 ) ) ;
#37780=FACE_OUTER_BOUND ( 'NONE', #33789, .T. ) ;
#37809=CARTESIAN_POINT ( 'NONE',  ( 63.25638208530150308, 1.265664290790580182, -62.44691083073610116 ) ) ;
#37818=CARTESIAN_POINT ( 'NONE',  ( 65.13393739769620083, 1.383811055320669947, -65.65000000000000568 ) ) ;
#37820=CARTESIAN_POINT ( 'NONE',  ( 63.75430343581950154, 1.400155262441499904, -69.47341233291868434 ) ) ;
#37822=CARTESIAN_POINT ( 'NONE',  ( 68.13393739769630031, 1.530257664727401767, -69.99644660940670349 ) ) ;
#37824=CARTESIAN_POINT ( 'NONE',  ( 71.25019707560579718, 0.8838110553206759423, -60.52272727272730179 ) ) ;
#37848=ORIENTED_EDGE ( 'NONE', *, *, #40229, .F. ) ;
#37856=DIRECTION ( 'NONE',  ( -1.000000000000000000, 0.000000000000000000, 0.000000000000000000 ) ) ;
#37864=CARTESIAN_POINT ( 'NONE',  ( 72.69256032412449997, 1.379674774869650067, -69.17486252676589231 ) ) ;
#37865=CARTESIAN_POINT ( 'NONE',  ( 71.47612964547799663, 0.8925687589132609290, -60.66703147076970737 ) ) ;
#37874=CARTESIAN_POINT ( 'NONE',  ( 70.99050876911339003, 1.383811055320669947, -60.94999999999999574 ) ) ;
#37879=VERTEX_POINT ( 'NONE', #23394 ) ;
#37881=CARTESIAN_POINT ( 'NONE',  ( 63.75818144730860126, 1.026088617261689873, -61.54425306709249810 ) ) ;
#37884=DIRECTION ( 'NONE',  ( 0.000000000000000000, 0.7071067811865492381, 0.7071067811865457964 ) ) ;
#37898=ORIENTED_EDGE ( 'NONE', *, *, #15949, .F. ) ;
#37903=VERTEX_POINT ( 'NONE', #34688 ) ;
#37913=CARTESIAN_POINT ( 'NONE',  ( 72.49279582477669237, 1.028300555801499927, -61.52602141601349928 ) ) ;
#37915=CARTESIAN_POINT ( 'NONE',  ( 64.57873039904879420, 0.9579170000946040098, -70.48345851730660172 ) ) ;
#37920=CIRCLE ( 'NONE', #15337, 0.5000000000000004441 ) ;
#37925=CARTESIAN_POINT ( 'NONE',  ( 63.13228119804391270, 0.8904513541338849869, -68.96413986139360475 ) ) ;
#37946=VERTEX_POINT ( 'NONE', #46521 ) ;
#37957=CARTESIAN_POINT ( 'NONE',  ( 64.93393739769749118, 11.38381105532110205, -69.85000000000074749 ) ) ;
#37986=CARTESIAN_POINT ( 'NONE',  ( 65.07262241358380095, 1.198183261254770038, -60.61312937625270081 ) ) ;
#37993=CARTESIAN_POINT ( 'NONE',  ( 64.85894149894409111, 0.8879664753683469414, -60.62259972594610247 ) ) ;
#38007=CARTESIAN_POINT ( 'NONE',  ( 64.67849076041288470, 1.005545696829380109, -60.75297091621269630 ) ) ;
#38010=ORIENTED_EDGE ( 'NONE', *, *, #48280, .F. ) ;
#38015=CARTESIAN_POINT ( 'NONE',  ( 73.15615143370008866, 1.097085799869290224, -62.44531798733959960 ) ) ;
#38023=CARTESIAN_POINT ( 'NONE',  ( 64.81933968820119674, 1.186515949276290227, -70.54416184698391135 ) ) ;
#38026=CARTESIAN_POINT ( 'NONE',  ( 63.93393739769619089, 1.383811055320669947, -62.44999999999999574 ) ) ;
#38040=VECTOR ( 'NONE', #15791, 1000.000000000000000 ) ;
#38067=CARTESIAN_POINT ( 'NONE',  ( 63.19469565515579745, 1.000225705806889964, -62.25573873525459589 ) ) ;
#38076=CARTESIAN_POINT ( 'NONE',  ( 63.47791868668480220, 1.368314977562110180, -68.96521306187010225 ) ) ;
#38081=CARTESIAN_POINT ( 'NONE',  ( 72.76912858252920557, 1.370387345318210048, -62.28683037558460001 ) ) ;
#38117=B_SPLINE_SURFACE_WITH_KNOTS ( 'NONE', 3, 3, ( 
 ( #38866, #34645, #14230, #6895, #45950, #21818, #18157, #18925, #15000 ),
 ( #46738, #18411, #50908, #17897, #26784, #45688, #6370, #38608, #46219 ),
 ( #30456, #1920, #38081, #10565, #10306, #42799, #6627, #22332, #50399 ),
 ( #33870, #18672, #26005, #38338, #2698, #49881, #13976, #2427, #14486 ),
 ( #29933, #30716, #42015, #6117, #26522, #16034, #19447, #31729, #3734 ),
 ( #35432, #31224, #15525, #19705, #30968, #15775, #12109, #51681, #31477 ),
 ( #40137, #15268, #39888, #51174, #47250, #47501, #47755, #11862, #35697 ),
 ( #24117, #28066, #7151, #35167, #43566, #11340, #3215, #27817, #3476 ),
 ( #7667, #46999, #27304, #27051, #11083, #43055, #44070, #11599, #43817 ),
 ( #43312, #7916, #27558, #31990, #39631, #7404, #23351, #23866, #23610 ),
 ( #35939, #3987, #48011, #39375, #23103, #4233, #19186, #51429, #39121 ),
 ( #20207, #19950, #8173, #36194, #60, #305, #36708, #49052, #1078 ),
 ( #44584, #17077, #24640, #49312, #29108, #40653, #20983, #48784, #41426 ),
 ( #32759, #33027, #13407, #8689, #25166, #41173, #553, #20457, #5020 ),
 ( #8955, #40394, #1343, #29366, #17333, #4751, #33296, #45107, #20718 ),
 ( #21235, #36981, #37245, #45371, #13158, #9213, #5284, #9476, #48263 ),
 ( #25423, #5543, #21498, #28322, #16539, #37498, #12624, #810, #16286 ),
 ( #32240, #16810, #12358, #32492, #44850, #44323, #8433, #48519, #12892 ),
 ( #24379, #4489, #28847, #24897, #40910, #36447, #28584, #23486, #18548 ),
 ( #3351, #38474, #19325, #34525, #30590, #42930, #10697, #6771, #39249 ) ),
 .UNSPECIFIED., .F., .F., .F.,
 ( 4, 2, 2, 2, 2, 2, 2, 2, 2, 4 ),
 ( 4, 1, 1, 1, 1, 1, 4 ),
 ( -1.826192301619909975, -1.664708266391559999, -1.413116924483460046, -1.141370188512440098, -0.9130961508099539881, -0.7989591319587090457, -0.6163399017967190474, -0.3681920442862079978, -0.1161770321749559937, 0.000000000000000000 ),
 ( 0.000000000000000000, 0.1666666666666670182, 0.3333333333333329818, 0.5000000000000000000, 0.6666666666666670737, 0.8333333333333330373, 1.000000000000000000 ),
 .UNSPECIFIED. ) ;
#38123=CARTESIAN_POINT ( 'NONE',  ( 72.89119224076110015, 1.045341414532760194, -69.29500968820069318 ) ) ;
#38135=CARTESIAN_POINT ( 'NONE',  ( 63.76776162078119370, 1.195685806282509978, -61.57371279390859797 ) ) ;
#38167=CYLINDRICAL_SURFACE ( 'NONE', #34750, 0.4999999999999994449 ) ;
#38173=CARTESIAN_POINT ( 'NONE',  ( 64.52268999588739007, 1.145495783610749996, -70.39094822078129710 ) ) ;
#38182=DIRECTION ( 'NONE',  ( 0.000000000000000000, -1.000000000000000000, 0.000000000000000000 ) ) ;
#38184=CARTESIAN_POINT ( 'NONE',  ( 63.33772283987339335, 1.326578174762039986, -68.82808305222700085 ) ) ;
#38193=CARTESIAN_POINT ( 'NONE',  ( 71.20900144662560649, 1.388715606738730068, -70.28003120372629553 ) ) ;
#38201=CARTESIAN_POINT ( 'NONE',  ( 71.42462519098069151, 0.8888742037077599356, -70.66714310028369539 ) ) ;
#38236=CARTESIAN_POINT ( 'NONE',  ( 68.13393739769620083, 1.383811055320669947, -60.14999999999999858 ) ) ;
#38242=CARTESIAN_POINT ( 'NONE',  ( 64.97847163984020824, 0.9947083095259759977, -60.55634004142090276 ) ) ;
#38271=CARTESIAN_POINT ( 'NONE',  ( 73.01625195241490474, 1.007912009470880221, -69.12629645913949616 ) ) ;
#38273=CARTESIAN_POINT ( 'NONE',  ( 73.16133767175010405, 0.8879664753683469414, -62.37500410124779648 ) ) ;
#38282=CARTESIAN_POINT ( 'NONE',  ( 64.79174514991450451, 0.8925687589132640376, -70.63296852923039637 ) ) ;
#38294=CIRCLE ( 'NONE', #41644, 0.5000000000000004441 ) ;
#38323=CARTESIAN_POINT ( 'NONE',  ( 63.46279604660929863, 1.371509258145880095, -62.41110185547420031 ) ) ;
#38333=CARTESIAN_POINT ( 'NONE',  ( 63.64098798152370762, 1.412341182043239884, -69.17505041201758331 ) ) ;
#38338=CARTESIAN_POINT ( 'NONE',  ( 72.77037870541830955, 1.316034553466219892, -62.10038360666850110 ) ) ;
#38351=CARTESIAN_POINT ( 'NONE',  ( 63.46757340380580814, 1.384887413063060180, -68.61455525072810246 ) ) ;
#38393=CARTESIAN_POINT ( 'NONE',  ( 63.53675997960419863, 1.374525224581449878, -62.20330014729499624 ) ) ;
#38406=VERTEX_POINT ( 'NONE', #2709 ) ;
#38410=DIRECTION ( 'NONE',  ( 0.000000000000000000, 1.000000000000000000, 0.000000000000000000 ) ) ;
#38427=CARTESIAN_POINT ( 'NONE',  ( 64.69570918563078976, 1.132579237369299996, -70.50812303354531707 ) ) ;
#38436=CARTESIAN_POINT ( 'NONE',  ( 72.00712697859638922, 1.176186365484889862, -70.19198721960910348 ) ) ;
#38441=CARTESIAN_POINT ( 'NONE',  ( 63.21507766202849865, 1.186856010528209993, -68.92285061280580294 ) ) ;
#38449=CARTESIAN_POINT ( 'NONE',  ( 71.17905174416029013, 1.387412027389909985, -70.29005197907430613 ) ) ;
#38470=ORIENTED_EDGE ( 'NONE', *, *, #23615, .T. ) ;
#38472=AXIS2_PLACEMENT_3D ( 'NONE', #44896, #51726, #31785 ) ;
#38474=CARTESIAN_POINT ( 'NONE',  ( 71.35671708621339349, 1.389801772588449946, -61.03316673290180461 ) ) ;
#38500=CARTESIAN_POINT ( 'NONE',  ( 64.81199447428090821, 0.8910129994591549085, -60.65352295474710331 ) ) ;
#38520=ORIENTED_EDGE ( 'NONE', *, *, #29160, .T. ) ;
#38537=CARTESIAN_POINT ( 'NONE',  ( 73.23379646625190276, 0.8840451408750739093, -62.48896739026430680 ) ) ;
#38544=CARTESIAN_POINT ( 'NONE',  ( 64.97448143965360146, 1.327097482837290121, -70.45474866971780159 ) ) ;
#38592=CARTESIAN_POINT ( 'NONE',  ( 63.47112272702528912, 1.372372808637209785, -62.39142423721519748 ) ) ;
#38606=CARTESIAN_POINT ( 'NONE',  ( 71.13364007206789097, 1.371651820402770117, -60.88469507784019896 ) ) ;
#38608=CARTESIAN_POINT ( 'NONE',  ( 72.98330304380999678, 0.9543424661151610477, -62.11630250819479926 ) ) ;
#38613=CARTESIAN_POINT ( 'NONE',  ( 63.25402410758490390, 0.9098571636355720083, -62.15909090909049439 ) ) ;
#38621=ORIENTED_EDGE ( 'NONE', *, *, #44068, .F. ) ;
#38632=CARTESIAN_POINT ( 'NONE',  ( 63.10653712364229762, 0.8879664753683499390, -62.37500410124779648 ) ) ;
#38656=DIRECTION ( 'NONE',  ( 0.000000000000000000, 0.000000000000000000, 1.000000000000000000 ) ) ;
#38668=CARTESIAN_POINT ( 'NONE',  ( 63.43387347518848429, 0.9897451961579500912, -61.91936536276160297 ) ) ;
#38673=CARTESIAN_POINT ( 'NONE',  ( 73.22759735627541033, 0.9947083095259801055, -68.80546575785609775 ) ) ;
#38675=AXIS2_PLACEMENT_3D ( 'NONE', #40700, #24945, #13460 ) ;
#38694=CARTESIAN_POINT ( 'NONE',  ( 71.33393739769628894, 1.883811055320669947, -68.84999999999999432 ) ) ;
#38700=CARTESIAN_POINT ( 'NONE',  ( 64.64722926691230498, 0.9479899806831150189, -70.53291850127419593 ) ) ;
#38708=CARTESIAN_POINT ( 'NONE',  ( 71.82945924946500327, 1.426105412860660060, -70.05138037415009933 ) ) ;
#38712=CARTESIAN_POINT ( 'NONE',  ( 63.25402410758490390, 0.9098571636355680115, -69.14090909090950277 ) ) ;
#38721=CARTESIAN_POINT ( 'NONE',  ( 71.43836573789060651, 0.9955677559369568996, -70.64918477200470193 ) ) ;
#38730=ORIENTED_EDGE ( 'NONE', *, *, #50149, .F. ) ;
#38741=ADVANCED_FACE ( 'NONE', ( #33080 ), #29419, .T. ) ;
#38762=CARTESIAN_POINT ( 'NONE',  ( 71.07527734533519492, 1.384447124000270035, -70.32375107525380997 ) ) ;
#38769=CARTESIAN_POINT ( 'NONE',  ( 65.07649219403889163, 1.383767307422960169, -60.97855929785719553 ) ) ;
#38797=ORIENTED_EDGE ( 'NONE', *, *, #39305, .F. ) ;
#38800=CARTESIAN_POINT ( 'NONE',  ( 72.80507874878320251, 1.371509258145880095, -62.41110185547420031 ) ) ;
#38817=VERTEX_POINT ( 'NONE', #5972 ) ;
#38826=ORIENTED_EDGE ( 'NONE', *, *, #46040, .F. ) ;
#38862=DIRECTION ( 'NONE',  ( 0.000000000000000000, 0.000000000000000000, -1.000000000000000000 ) ) ;
#38864=CARTESIAN_POINT ( 'NONE',  ( 71.00993340901570150, 1.383811055320669947, -60.91804007473620430 ) ) ;
#38866=CARTESIAN_POINT ( 'NONE',  ( 72.72056432233058842, 1.396834109478129804, -62.44999999999999574 ) ) ;
#38887=AXIS2_PLACEMENT_3D ( 'NONE', #23142, #46776, #31260 ) ;
#38914=DIRECTION ( 'NONE',  ( 1.000000000000000000, 0.000000000000000000, 0.000000000000000000 ) ) ;
#38920=CARTESIAN_POINT ( 'NONE',  ( 63.99198253403570646, 1.457833794292699992, -61.64494777836840456 ) ) ;
#38924=CARTESIAN_POINT ( 'NONE',  ( 72.83834671619840151, 1.382830464309369844, -68.61079447352989291 ) ) ;
#38929=ORIENTED_EDGE ( 'NONE', *, *, #26161, .T. ) ;
#38931=EDGE_CURVE ( 'NONE', #46311, #38817, #19047, .T. ) ;
#38939=EDGE_CURVE ( 'NONE', #21117, #17335, #39857, .T. ) ;
#38940=CARTESIAN_POINT ( 'NONE',  ( 64.93393739769619799, 1.883811055320669947, -70.34999999999999432 ) ) ;
#38944=DIRECTION ( 'NONE',  ( 0.000000000000000000, 0.000000000000000000, 1.000000000000000000 ) ) ;
#38962=CARTESIAN_POINT ( 'NONE',  ( 71.60705152684150221, 1.024253516290730026, -70.53167046690928998 ) ) ;
#38969=CARTESIAN_POINT ( 'NONE',  ( 63.22343968446819673, 0.9036513197889520788, -69.09785636402040154 ) ) ;
#38976=ORIENTED_EDGE ( 'NONE', *, *, #50867, .T. ) ;
#38979=CARTESIAN_POINT ( 'NONE',  ( 71.51817256006181367, 0.9307121176571799825, -70.60454574395809857 ) ) ;
#39026=CARTESIAN_POINT ( 'NONE',  ( 64.94442696602180831, 1.326324093417220240, -60.85906821647699871 ) ) ;
#39028=CARTESIAN_POINT ( 'NONE',  ( 64.93393739769599904, 1.396834109478129804, -61.06337307536569625 ) ) ;
#39044=VECTOR ( 'NONE', #38656, 1000.000000000000000 ) ;
#39059=CARTESIAN_POINT ( 'NONE',  ( 72.86479754607628934, 1.326666718054990035, -62.33513496753349870 ) ) ;
#39107=CARTESIAN_POINT ( 'NONE',  ( 63.53329261246669546, 1.393731187554809958, -62.48946499964799983 ) ) ;
#39119=CARTESIAN_POINT ( 'NONE',  ( 71.21626143364200345, 1.196343736543249880, -60.62426770491639871 ) ) ;
#39121=CARTESIAN_POINT ( 'NONE',  ( 72.31745269033768864, 1.031856533264720266, -61.34884692546020091 ) ) ;
#39154=EDGE_CURVE ( 'NONE', #21117, #8299, #43242, .T. ) ;
#39166=CYLINDRICAL_SURFACE ( 'NONE', #20008, 0.5000000000000154321 ) ;
#39167=CARTESIAN_POINT ( 'NONE',  ( 63.75818144730860126, 1.026088617261689873, -61.54425306709249810 ) ) ;
#39174=CARTESIAN_POINT ( 'NONE',  ( 63.38185292195529286, 1.308647200627810259, -62.31695083504749988 ) ) ;
#39178=CARTESIAN_POINT ( 'NONE',  ( 73.20393974370449541, 0.8850831926798630178, -68.85873448833339694 ) ) ;
#39197=CARTESIAN_POINT ( 'NONE',  ( 68.13393739769620083, -42.11618894467930119, -59.64999999999999858 ) ) ;
#39210=CARTESIAN_POINT ( 'NONE',  ( 71.51343005691549592, 1.309114013480880079, -70.37891650423269141 ) ) ;
#39219=AXIS2_PLACEMENT_3D ( 'NONE', #48197, #12562, #16479 ) ;
#39220=CARTESIAN_POINT ( 'NONE',  ( 63.25409997666370288, 1.100585178972010025, -69.07860007646949896 ) ) ;
#39224=CARTESIAN_POINT ( 'NONE',  ( 63.41196002899329898, 0.9486721756287899154, -69.35284629089680664 ) ) ;
#39229=CARTESIAN_POINT ( 'NONE',  ( 71.58293006479010501, 1.102139304147779830, -70.51608385812031088 ) ) ;
#39238=ORIENTED_EDGE ( 'NONE', *, *, #3918, .T. ) ;
#39243=DIRECTION ( 'NONE',  ( 0.000000000000000000, 1.000000000000000000, 0.000000000000000000 ) ) ;
#39249=CARTESIAN_POINT ( 'NONE',  ( 71.62484648860579739, 0.9098571636355720083, -60.77008670988870165 ) ) ;
#39257=CARTESIAN_POINT ( 'NONE',  ( 63.93393739769591377, 11.38381105532030801, -61.44999999999966178 ) ) ;
#39273=CARTESIAN_POINT ( 'NONE',  ( 64.89987712417480736, 0.8859637708054489691, -60.59611492242089525 ) ) ;
#39296=AXIS2_PLACEMENT_3D ( 'NONE', #3015, #46278, #37884 ) ;
#39305=EDGE_CURVE ( 'NONE', #8243, #29849, #12139, .T. ) ;
#39309=CARTESIAN_POINT ( 'NONE',  ( 72.75396425272869294, 1.390208944942419755, -62.54542373973200142 ) ) ;
#39313=ORIENTED_EDGE ( 'NONE', *, *, #21227, .F. ) ;
#39334=AXIS2_PLACEMENT_3D ( 'NONE', #30470, #18941, #12062 ) ;
#39354=CARTESIAN_POINT ( 'NONE',  ( 63.45006824032990522, 1.383161449028130097, -68.67155289007729380 ) ) ;
#39355=CYLINDRICAL_SURFACE ( 'NONE', #24735, 0.5000000000000049960 ) ;
#39361=DIRECTION ( 'NONE',  ( 1.000000000000000000, 0.000000000000000000, 0.000000000000000000 ) ) ;
#39373=CARTESIAN_POINT ( 'NONE',  ( 71.24781132387310834, 1.101170701158060039, -60.57405794295090118 ) ) ;
#39375=CARTESIAN_POINT ( 'NONE',  ( 72.23215937178071044, 1.347758125946160179, -61.41854848478109830 ) ) ;
#39425=CARTESIAN_POINT ( 'NONE',  ( 63.83278432315639606, 1.031856533264730258, -61.46648470735859604 ) ) ;
#39430=B_SPLINE_CURVE_WITH_KNOTS ( 'NONE', 3,
 ( #49490, #12542, #13577, #4931, #28509, #41345, #20903, #41095, #1518, #1262, #17503, #44506, #5462, #8609, #4667, #20641 ),
 .UNSPECIFIED., .F., .F.,
 ( 4, 2, 2, 2, 2, 2, 2, 4 ),
 ( -4.528785000000000087E-15, 0.07216186899280399580, 0.1546325764131560032, 0.2061767685508759940, 0.2319488646197360171, 0.2731842183299119653, 0.3391607842661930050, 0.4123535371017559847 ),
 .UNSPECIFIED. ) ;
#39435=CARTESIAN_POINT ( 'NONE',  ( 63.45871665573360332, 1.367045641526529964, -62.38166218803879559 ) ) ;
#39439=CARTESIAN_POINT ( 'NONE',  ( 72.95172982307090592, 1.328073773609210084, -68.78070348185231353 ) ) ;
#39449=( BOUNDED_SURFACE ( )  B_SPLINE_SURFACE ( 2, 2, ( 
 ( #8440, #48524, #36713 ),
 ( #24122, #16292, #31995 ),
 ( #816, #28072, #44077 ) ),
 .UNSPECIFIED., .F., .F., .T. ) 
 B_SPLINE_SURFACE_WITH_KNOTS ( ( 3, 3 ),
 ( 3, 3 ),
 ( -1.570546326878010213, -1.285150385668689982E-13 ),
 ( 1.570796326791910058, 3.141592653593380025 ),
 .UNSPECIFIED. ) 
 GEOMETRIC_REPRESENTATION_ITEM ( )  RATIONAL_B_SPLINE_SURFACE ( (
 ( 1.000000000000000000, 0.7071067811842219886, 1.000000000000000000),
 ( 0.7071951639803649714, 0.5000624960712040101, 0.7071951639803649714),
 ( 1.000000000000000000, 0.7071067811842219886, 1.000000000000000000) ) ) 
 REPRESENTATION_ITEM ( '' )  SURFACE ( )  );
#39475=CARTESIAN_POINT ( 'NONE',  ( 71.90718900442469419, 0.9644290104345999426, -70.31590730770628284 ) ) ;
#39508=VERTEX_POINT ( 'NONE', #34089 ) ;
#39521=CARTESIAN_POINT ( 'NONE',  ( 64.92520290936280958, 0.8850831926798620186, -70.72000234600830026 ) ) ;
#39534=CARTESIAN_POINT ( 'NONE',  ( 65.07343865691001383, 1.370118064600909902, -60.90754237392700077 ) ) ;
#39563=CARTESIAN_POINT ( 'NONE',  ( 73.08848314165430793, 0.9307121176571839793, -62.26576483763439995 ) ) ;
#39568=CARTESIAN_POINT ( 'NONE',  ( 64.69948915615030671, 1.003508719579999875, -70.56164792957929421 ) ) ;
#39582=EDGE_CURVE ( 'NONE', #51003, #16762, #42412, .T. ) ;
#39605=CARTESIAN_POINT ( 'NONE',  ( 63.44018392888030178, 1.383811055320669947, -68.52712657046359368 ) ) ;
#39628=CARTESIAN_POINT ( 'NONE',  ( 71.40029138921259744, 0.9945465939392541532, -60.62606712929739672 ) ) ;
#39631=CARTESIAN_POINT ( 'NONE',  ( 72.30065220047070795, 1.277721627657099956, -61.41802414917730601 ) ) ;
#39644=DIRECTION ( 'NONE',  ( 1.000000000000000000, 0.000000000000000000, 0.000000000000000000 ) ) ;
#39673=CARTESIAN_POINT ( 'NONE',  ( 63.47971227208819300, 1.385888765344519991, -62.64792042614390510 ) ) ;
#39677=CARTESIAN_POINT ( 'NONE',  ( 64.54901150452380421, 0.9254890127232520136, -60.83838280017310041 ) ) ;
#39691=CARTESIAN_POINT ( 'NONE',  ( 73.00373354607030763, 1.334812829108570131, -68.66140445374750811 ) ) ;
#39692=FACE_OUTER_BOUND ( 'NONE', #4408, .T. ) ;
#39725=CARTESIAN_POINT ( 'NONE',  ( 72.43398376235579406, 1.116860450401449878, -69.82773512215300116 ) ) ;
#39743=CARTESIAN_POINT ( 'NONE',  ( 71.39251316048110141, 1.372372808637209785, -70.31281467067098845 ) ) ;
#39771=CARTESIAN_POINT ( 'NONE',  ( 64.93393739769628326, 10.88381105532060111, -61.44999999999999574 ) ) ;
#39812=ORIENTED_EDGE ( 'NONE', *, *, #31618, .F. ) ;
#39817=CARTESIAN_POINT ( 'NONE',  ( 72.93015195551900831, 1.326578174762039986, -62.47191694777300341 ) ) ;
#39824=CARTESIAN_POINT ( 'NONE',  ( 64.78711365736019445, 1.264121749638649872, -70.45005197993610579 ) ) ;
#39851=CARTESIAN_POINT ( 'NONE',  ( 71.23851365796429036, 1.390208944942409985, -61.02997314496759884 ) ) ;
#39852=PRODUCT_DEFINITION_SHAPE ( 'NONE', 'NONE',  #48485 ) ;
#39857=CIRCLE ( 'NONE', #17272, 6.000000000000005329 ) ;
#39862=CARTESIAN_POINT ( 'NONE',  ( 63.00666467042349694, 0.8838110553206759423, -68.76625967790960203 ) ) ;
#39866=ORIENTED_EDGE ( 'NONE', *, *, #2519, .F. ) ;
#39886=CARTESIAN_POINT ( 'NONE',  ( 71.48629080024771554, 0.9281439705311279598, -60.67386159597580075 ) ) ;
#39888=CARTESIAN_POINT ( 'NONE',  ( 72.51356393101009701, 1.400155911913269824, -61.82657703151539863 ) ) ;
#39920=CARTESIAN_POINT ( 'NONE',  ( 64.86412778899749298, 1.402436395646509792, -70.21307676274530252 ) ) ;
#39933=CARTESIAN_POINT ( 'NONE',  ( 63.46018632244250313, 1.384447124000270035, -62.70866005236110396 ) ) ;
#39939=CARTESIAN_POINT ( 'NONE',  ( 63.00666467042349694, 0.8838110553206759423, -68.76625967790960203 ) ) ;
#39984=CARTESIAN_POINT ( 'NONE',  ( 72.37391086482439562, 1.440335647928530083, -69.57825580936660970 ) ) ;
#40003=AXIS2_PLACEMENT_3D ( 'NONE', #46946, #2130, #10516 ) ;
#40007=CARTESIAN_POINT ( 'NONE',  ( 71.29497000743199919, 0.8840451408750739093, -70.74985906855570761 ) ) ;
#40009=EDGE_LOOP ( 'NONE', ( #32842, #26285 ) ) ;
#40010=FACE_OUTER_BOUND ( 'NONE', #32145, .T. ) ;
#40018=ORIENTED_EDGE ( 'NONE', *, *, #50882, .F. ) ;
#40027=CARTESIAN_POINT ( 'NONE',  ( 63.02029346573409185, 0.8838110553206740549, -68.78868353141480441 ) ) ;
#40053=CARTESIAN_POINT ( 'NONE',  ( 72.43509047223599850, 1.031856533264720266, -69.83351529264139401 ) ) ;
#40107=FACE_OUTER_BOUND ( 'NONE', #34914, .T. ) ;
#40115=CARTESIAN_POINT ( 'NONE',  ( 63.23767253740619765, 1.267233196669050210, -68.81685389259939711 ) ) ;
#40127=CARTESIAN_POINT ( 'NONE',  ( 71.27262092911099955, 0.8838110553206759423, -70.76364393196210756 ) ) ;
#40129=ORIENTED_EDGE ( 'NONE', *, *, #41996, .T. ) ;
#40133=DIRECTION ( 'NONE',  ( 1.000000000000000000, 0.000000000000000000, 0.000000000000000000 ) ) ;
#40135=CARTESIAN_POINT ( 'NONE',  ( 71.16987874477759135, 1.383357884654609959, -60.97108096920410247 ) ) ;
#40137=CARTESIAN_POINT ( 'NONE',  ( 72.46078431608199821, 1.446932438105759999, -61.88285690311300158 ) ) ;
#40139=CARTESIAN_POINT ( 'NONE',  ( 64.96229391979498757, 1.190292248953970011, -70.62687270921169613 ) ) ;
#40180=AXIS2_PLACEMENT_3D ( 'NONE', #7813, #18818, #30860 ) ;
#40186=CARTESIAN_POINT ( 'NONE',  ( 63.39147977162330960, 1.370118064600909902, -62.58950125921379737 ) ) ;
#40199=CARTESIAN_POINT ( 'NONE',  ( 63.52910586918969216, 1.391735898526599957, -62.39330133199160144 ) ) ;
#40207=ORIENTED_EDGE ( 'NONE', *, *, #41775, .T. ) ;
#40221=CIRCLE ( 'NONE', #41044, 0.4999999999999962252 ) ;
#40229=EDGE_CURVE ( 'NONE', #17827, #29784, #29528, .T. ) ;
#40240=CARTESIAN_POINT ( 'NONE',  ( 72.08436319736711084, 1.441354674475110009, -69.87293635634929956 ) ) ;
#40253=CARTESIAN_POINT ( 'NONE',  ( 64.64959960286040541, 1.134960180547699871, -60.82204151093920075 ) ) ;
#40255=CARTESIAN_POINT ( 'NONE',  ( 71.60339545440879760, 0.9065823421260970072, -70.54525856488079683 ) ) ;
#40342=CARTESIAN_POINT ( 'NONE',  ( 72.27589226135678757, 1.457833794292699992, -69.65505222163159260 ) ) ;
#40343=CARTESIAN_POINT ( 'NONE',  ( 63.46018632244250313, 1.384447124000270035, -62.70866005236110396 ) ) ;
#40359=CARTESIAN_POINT ( 'NONE',  ( 71.31427394968270050, 1.395196698723390138, -61.05633982442969909 ) ) ;
#40368=CARTESIAN_POINT ( 'NONE',  ( 63.29300171101180439, 1.330484379554840002, -68.72860478453370092 ) ) ;
#40381=CARTESIAN_POINT ( 'NONE',  ( 71.15687762518609816, 1.370937308141420230, -70.40667188452539449 ) ) ;
#40392=CARTESIAN_POINT ( 'NONE',  ( 71.47398825900590680, 0.9272522097098119254, -60.66559564092809609 ) ) ;
#40394=CARTESIAN_POINT ( 'NONE',  ( 71.77737262410839492, 1.421976796946140098, -61.21910751912620441 ) ) ;
#40396=CARTESIAN_POINT ( 'NONE',  ( 65.07261215712630076, 1.274277262446069869, -70.59881390902160092 ) ) ;
#40406=CIRCLE ( 'NONE', #263, 0.4999999999999982236 ) ;
#40436=CARTESIAN_POINT ( 'NONE',  ( 63.42952807919409253, 1.382830464309369844, -62.68920552647019662 ) ) ;
#40446=CARTESIAN_POINT ( 'NONE',  ( 64.72741779930979078, 0.8986939045430379913, -60.71074964625670134 ) ) ;
#40457=ORIENTED_EDGE ( 'NONE', *, *, #1370, .F. ) ;
#40491=CARTESIAN_POINT ( 'NONE',  ( 72.22985692015490145, 1.197080272271600077, -69.99851329395420407 ) ) ;
#40498=CARTESIAN_POINT ( 'NONE',  ( 64.93393739769619799, 1.883811055320669947, -61.44999999999999574 ) ) ;
#40508=CARTESIAN_POINT ( 'NONE',  ( 64.88669131378958355, 1.400446703426900141, -61.07889042780649902 ) ) ;
#40546=AXIS2_PLACEMENT_3D ( 'NONE', #41726, #37280, #21020 ) ;
#40552=CARTESIAN_POINT ( 'NONE',  ( 64.12576500581000971, 1.345243900246989810, -69.96281373730460018 ) ) ;
#40586=CARTESIAN_POINT ( 'NONE',  ( 68.13393739769620083, -42.61618894467930119, -65.65000000000000568 ) ) ;
#40587=ORIENTED_EDGE ( 'NONE', *, *, #11230, .T. ) ;
#40593=CARTESIAN_POINT ( 'NONE',  ( 63.47971227208819300, 1.385888765344519991, -62.64792042614390510 ) ) ;
#40599=DIRECTION ( 'NONE',  ( 0.000000000000000000, -0.7071067811865292541, 0.7071067811865656694 ) ) ;
#40625=CARTESIAN_POINT ( 'NONE',  ( 63.13616699414190236, 0.9259537755896120048, -68.96999734323989628 ) ) ;
#40639=CARTESIAN_POINT ( 'NONE',  ( 71.24581987525910165, 0.9960089569207349891, -70.77007079217121088 ) ) ;
#40645=CARTESIAN_POINT ( 'NONE',  ( 73.13170780125059878, 0.9259537755896120048, -68.96999734323989628 ) ) ;
#40651=CARTESIAN_POINT ( 'NONE',  ( 71.53768886009270034, 0.9325382164350239922, -60.70884169071130287 ) ) ;
#40653=CARTESIAN_POINT ( 'NONE',  ( 72.15767745866649818, 1.191618978581419963, -61.23657242805779788 ) ) ;
#40655=CARTESIAN_POINT ( 'NONE',  ( 64.84489409100208945, 0.9242073871622918935, -70.66822101033309877 ) ) ;
#40674=CARTESIAN_POINT ( 'NONE',  ( 64.93393739769619799, 4.883811055320659733, -61.44999999999999574 ) ) ;
#40697=CARTESIAN_POINT ( 'NONE',  ( 63.21844385136499511, 1.269319268680890067, -62.52104542963419931 ) ) ;
#40700=CARTESIAN_POINT ( 'NONE',  ( 68.13393739769620083, 0.8838110553206759423, -65.65000000000000568 ) ) ;
#40707=CARTESIAN_POINT ( 'NONE',  ( 64.87536163491139973, 1.372372808637209785, -60.98718532932910819 ) ) ;
#40738=CARTESIAN_POINT ( 'NONE',  ( 72.72759757326660690, 1.395196698723390138, -62.46966344801350601 ) ) ;
#40752=CARTESIAN_POINT ( 'NONE',  ( 72.55698300813111246, 1.048861872235970161, -69.70476459732599039 ) ) ;
#40765=CARTESIAN_POINT ( 'NONE',  ( 63.95069823516159602, 1.061277144319840104, -61.34795443974510221 ) ) ;
#40803=CARTESIAN_POINT ( 'NONE',  ( 71.79848734841171165, 0.9405967369903629471, -60.89823624368929700 ) ) ;
#40808=CARTESIAN_POINT ( 'NONE',  ( 64.17132984853199673, 1.406832289998090069, -69.92220598882080651 ) ) ;
#40819=CIRCLE ( 'NONE', #20719, 0.5000000000000000000 ) ;
#40839=DIRECTION ( 'NONE',  ( 0.000000000000000000, 0.000000000000000000, 1.000000000000000000 ) ) ;
#40883=CARTESIAN_POINT ( 'NONE',  ( 63.30180592418038543, 1.263738073398970041, -68.93858679394679712 ) ) ;
#40897=CARTESIAN_POINT ( 'NONE',  ( 71.40743923234819590, 0.9234936569010840923, -70.67837287176459427 ) ) ;
#40903=CARTESIAN_POINT ( 'NONE',  ( 73.13041444294920268, 0.8910129994591549085, -68.97194292341539779 ) ) ;
#40906=CARTESIAN_POINT ( 'NONE',  ( 73.14840136429539541, 1.194703186106690129, -62.54674175640080591 ) ) ;
#40908=CARTESIAN_POINT ( 'NONE',  ( 71.23750802749680133, 1.369613126987639928, -60.92417343964400089 ) ) ;
#40910=CARTESIAN_POINT ( 'NONE',  ( 71.55783046266638792, 1.229734285826160178, -60.85522740516210405 ) ) ;
#40913=CARTESIAN_POINT ( 'NONE',  ( 64.85231939490250852, 0.9948723650351710690, -70.66407068423170301 ) ) ;
#40918=CARTESIAN_POINT ( 'NONE',  ( 68.13393739769620083, -42.11618894467930119, -65.65000000000000568 ) ) ;
#40930=ORIENTED_EDGE ( 'NONE', *, *, #15601, .F. ) ;
#40953=CARTESIAN_POINT ( 'NONE',  ( 63.18170070234948810, 0.9989215084294049696, -62.27490163988890259 ) ) ;
#40958=CARTESIAN_POINT ( 'NONE',  ( 71.36792781540339092, 1.399433130755050048, -61.07453677926569924 ) ) ;
#41015=CARTESIAN_POINT ( 'NONE',  ( 72.79374086912940811, 1.313759828078489900, -69.15881847709009378 ) ) ;
#41025=CARTESIAN_POINT ( 'NONE',  ( 64.58432100436870371, 1.316034553465939894, -61.01355869227559481 ) ) ;
#41030=DIRECTION ( 'NONE',  ( 0.8545454545454508333, 0.000000000000000000, 0.5193766129849408664 ) ) ;
#41044=AXIS2_PLACEMENT_3D ( 'NONE', #43224, #47665, #8085 ) ;
#41066=DIRECTION ( 'NONE',  ( -0.000000000000000000, 1.000000000000000000, 0.000000000000000000 ) ) ;
#41072=CARTESIAN_POINT ( 'NONE',  ( 64.11017304249050142, 1.191621070196819954, -70.06340612986369365 ) ) ;
#41095=CARTESIAN_POINT ( 'NONE',  ( 65.09597585808539577, 1.387131204727280132, -61.00757424182599920 ) ) ;
#41108=LINE ( 'NONE', #5218, #23997 ) ;
#41111=VERTEX_POINT ( 'NONE', #40498 ) ;
#41115=LINE ( 'NONE', #29307, #42601 ) ;
#41116=CARTESIAN_POINT ( 'NONE',  ( 63.44650199127489998, 1.383928098097870096, -62.75238677440889035 ) ) ;
#41122=FACE_OUTER_BOUND ( 'NONE', #2935, .T. ) ;
#41137=CARTESIAN_POINT ( 'NONE',  ( 65.23737843152770211, 1.383411777981069957, -60.92458877361669778 ) ) ;
#41142=CARTESIAN_POINT ( 'NONE',  ( 64.77932207159139466, 0.8936201581567920771, -60.67538646459720297 ) ) ;
#41149=AXIS2_PLACEMENT_3D ( 'NONE', #30198, #38862, #2174 ) ;
#41157=CARTESIAN_POINT ( 'NONE',  ( 71.26764986431300031, 0.9952464559119579279, -70.75693755662150863 ) ) ;
#41163=VERTEX_POINT ( 'NONE', #28433 ) ;
#41165=CARTESIAN_POINT ( 'NONE',  ( 73.08672326322148649, 0.8966068345641440285, -69.03681046574699565 ) ) ;
#41168=CARTESIAN_POINT ( 'NONE',  ( 73.15966969277990017, 1.196343736543249880, -62.56767596405429543 ) ) ;
#41170=CARTESIAN_POINT ( 'NONE',  ( 71.62484648860569791, 0.9098571636355680115, -60.77008670988870165 ) ) ;
#41173=CARTESIAN_POINT ( 'NONE',  ( 72.03321845393109868, 1.179532368575649803, -61.12950465565599956 ) ) ;
#41177=CARTESIAN_POINT ( 'NONE',  ( 65.17800597998869705, 1.373356196620459935, -70.43126475061649217 ) ) ;
#41188=FACE_OUTER_BOUND ( 'NONE', #26542, .T. ) ;
#41216=CARTESIAN_POINT ( 'NONE',  ( 63.30180592418049912, 1.263738073398960049, -62.36141320605320004 ) ) ;
#41226=CARTESIAN_POINT ( 'NONE',  ( 63.27581436415109550, 1.132579237369250036, -69.08822821206570097 ) ) ;
#41228=VERTEX_POINT ( 'NONE', #16925 ) ;
#41231=AXIS2_PLACEMENT_3D ( 'NONE', #11812, #28276, #20410 ) ;
#41272=EDGE_CURVE ( 'NONE', #37879, #28243, #22251, .T. ) ;
#41275=CARTESIAN_POINT ( 'NONE',  ( 65.05887334876689465, 1.388715606738730068, -70.28003120372629553 ) ) ;
#41277=DIRECTION ( 'NONE',  ( 0.000000000000000000, 0.000000000000000000, -1.000000000000000000 ) ) ;
#41284=CARTESIAN_POINT ( 'NONE',  ( 64.22068262707080066, 1.025918948572249745, -61.10071074863649443 ) ) ;
#41286=CYLINDRICAL_SURFACE ( 'NONE', #10876, 1.000000000000000888 ) ;
#41291=CARTESIAN_POINT ( 'NONE',  ( 68.13393739769624347, 0.8838110553206759423, -71.15000000000000568 ) ) ;
#41323=CARTESIAN_POINT ( 'NONE',  ( 64.22355794744891000, 1.454950765200730078, -69.87277598216670071 ) ) ;
#41345=CARTESIAN_POINT ( 'NONE',  ( 65.13185782384009315, 1.385888765344509999, -60.99577487439199786 ) ) ;
#41354=CIRCLE ( 'NONE', #51392, 0.5000000000000034417 ) ;
#41369=CARTESIAN_POINT ( 'NONE',  ( 63.50007682179899149, 1.388189907116970101, -62.58632377286669879 ) ) ;
#41391=CARTESIAN_POINT ( 'NONE',  ( 64.93204900141920177, 0.9940695285616559795, -60.58508503553749591 ) ) ;
#41397=CARTESIAN_POINT ( 'NONE',  ( 64.84324960441180963, 0.8888742037077599356, -60.63285689971630177 ) ) ;
#41418=CARTESIAN_POINT ( 'NONE',  ( 72.77398937677050128, 1.387412027389909985, -68.69511434646409498 ) ) ;
#41421=CARTESIAN_POINT ( 'NONE',  ( 72.80768847294999091, 1.384447124000270035, -62.70866005236110396 ) ) ;
#41426=CARTESIAN_POINT ( 'NONE',  ( 72.19114968843099689, 1.019773975906300034, -61.22921083583120350 ) ) ;
#41428=CARTESIAN_POINT ( 'NONE',  ( 65.09597585808549525, 1.387131204727280132, -70.29242575817399086 ) ) ;
#41464=CARTESIAN_POINT ( 'NONE',  ( 71.33393739769628894, 1.883811055320669947, -62.44999999999999574 ) ) ;
#41472=CARTESIAN_POINT ( 'NONE',  ( 63.50659274611129490, 1.388313565858570131, -62.46994910431339321 ) ) ;
#41483=CARTESIAN_POINT ( 'NONE',  ( 63.55206628625449383, 1.395841248662849976, -68.96826120918760239 ) ) ;
#41484=DIRECTION ( 'NONE',  ( -1.000000000000000000, 0.000000000000000000, 0.000000000000000000 ) ) ;
#41502=CARTESIAN_POINT ( 'NONE',  ( 63.64445560419389381, 1.419970371293449940, -62.18985507218640407 ) ) ;
#41526=CARTESIAN_POINT ( 'NONE',  ( 73.23379646625190276, 0.8840451408750739093, -62.48896739026430680 ) ) ;
#41528=CARTESIAN_POINT ( 'NONE',  ( 72.96828430334601023, 1.031491003830610209, -69.18984148332670259 ) ) ;
#41541=CARTESIAN_POINT ( 'NONE',  ( 64.01820444265550236, 1.113948672550079788, -61.29006734358329567 ) ) ;
#41578=CARTESIAN_POINT ( 'NONE',  ( 72.19114968843099689, 1.019773975906310026, -61.22921083583130297 ) ) ;
#41581=CARTESIAN_POINT ( 'NONE',  ( 63.80720226989929245, 1.275251724699800082, -69.71680052808839889 ) ) ;
#41585=EDGE_LOOP ( 'NONE', ( #48669, #8712, #19062, #37560, #28341, #43213 ) ) ;
#41644=AXIS2_PLACEMENT_3D ( 'NONE', #96, #12927, #1115 ) ;
#41647=EDGE_CURVE ( 'NONE', #309, #20803, #16199, .T. ) ;
#41661=CARTESIAN_POINT ( 'NONE',  ( 63.66068354842759192, 0.9098571636355720083, -62.44999999999999574 ) ) ;
#41672=CARTESIAN_POINT ( 'NONE',  ( 65.00985940095789317, 1.385702546077159925, -61.00218178904909649 ) ) ;
#41677=CARTESIAN_POINT ( 'NONE',  ( 72.93868606741401095, 1.327097482837290121, -68.80945595804269033 ) ) ;
#41680=CARTESIAN_POINT ( 'NONE',  ( 73.14800808192789816, 0.9948723650351710690, -62.36838199720629916 ) ) ;
#41682=CARTESIAN_POINT ( 'NONE',  ( 71.52584472686049821, 1.187931651339009909, -60.80292108597650014 ) ) ;
#41687=CARTESIAN_POINT ( 'NONE',  ( 64.74970223533068747, 0.9307121176571799825, -70.60454574395809857 ) ) ;
#41726=CARTESIAN_POINT ( 'NONE',  ( 68.13393739769620083, -20.61618894467929763, -65.65000000000000568 ) ) ;
#41732=CARTESIAN_POINT ( 'NONE',  ( 71.25019707560589666, 0.8838110553206759423, -70.77727272727270247 ) ) ;
#41733=CARTESIAN_POINT ( 'NONE',  ( 63.13616699414190236, 0.9259537755896120048, -62.33000265676009377 ) ) ;
#41742=CARTESIAN_POINT ( 'NONE',  ( 63.50128955454680124, 1.245298479525740021, -69.32855572113911080 ) ) ;
#41743=DIRECTION ( 'NONE',  ( 0.000000000000000000, -1.000000000000000000, 0.000000000000000000 ) ) ;
#41760=LINE ( 'NONE', #13229, #49403 ) ;
#41768=CARTESIAN_POINT ( 'NONE',  ( 74.13393739769620083, -20.61618894467929763, -65.65000000000000568 ) ) ;
#41775=EDGE_CURVE ( 'NONE', #11777, #37946, #6677, .T. ) ;
#41786=CARTESIAN_POINT ( 'NONE',  ( 72.71255372047811250, 1.170697810385189941, -69.47735791416680229 ) ) ;
#41795=CARTESIAN_POINT ( 'NONE',  ( 71.33393739769628894, 1.883811055320669947, -60.94999999999999574 ) ) ;
#41800=CARTESIAN_POINT ( 'NONE',  ( 64.70718024653930911, 1.310552739454400095, -60.94577717611679901 ) ) ;
#41820=VERTEX_POINT ( 'NONE', #22378 ) ;
#41841=CARTESIAN_POINT ( 'NONE',  ( 72.34709478978140851, 1.033004162168289941, -61.37787765298320153 ) ) ;
#41843=CARTESIAN_POINT ( 'NONE',  ( 64.19630443091290317, 1.030838547160819907, -70.17805703969949604 ) ) ;
#41850=CARTESIAN_POINT ( 'NONE',  ( 72.83393739769620367, 0.8838110553206759423, -62.79342862858290886 ) ) ;
#41853=CARTESIAN_POINT ( 'NONE',  ( 63.19469565515579745, 1.000225705806889964, -69.04426126474540126 ) ) ;
#41912=DIRECTION ( 'NONE',  ( 1.000000000000000000, 0.000000000000000000, 0.000000000000000000 ) ) ;
#41914=VERTEX_POINT ( 'NONE', #50694 ) ;
#41916=CARTESIAN_POINT ( 'NONE',  ( 65.21909306016200958, 1.375383258925270136, -60.85412179317820147 ) ) ;
#41940=CARTESIAN_POINT ( 'NONE',  ( 64.77932207159139466, 0.8936201581567889685, -60.67538646459720297 ) ) ;
#41948=CARTESIAN_POINT ( 'NONE',  ( 73.08914738367541020, 1.188582381068110205, -62.44003653085270145 ) ) ;
#41955=CIRCLE ( 'NONE', #10148, 0.5000000000000000000 ) ;
#41958=CARTESIAN_POINT ( 'NONE',  ( 65.01178944337659971, 1.369535599030039963, -70.36855090579189209 ) ) ;
#41961=CARTESIAN_POINT ( 'NONE',  ( 72.72056432233058842, 1.396834109478129804, -68.84999999999999432 ) ) ;
#41965=CYLINDRICAL_SURFACE ( 'NONE', #20290, 0.4999999999999994449 ) ;
#41968=CARTESIAN_POINT ( 'NONE',  ( 68.13393739769620083, -42.11618894467930119, -65.65000000000000568 ) ) ;
#41996=EDGE_CURVE ( 'NONE', #14211, #46311, #34829, .T. ) ;
#42001=CARTESIAN_POINT ( 'NONE',  ( 63.34300561417320807, 1.326324093417230232, -62.46048956832549948 ) ) ;
#42011=FACE_OUTER_BOUND ( 'NONE', #47675, .T. ) ;
#42015=CARTESIAN_POINT ( 'NONE',  ( 72.67019432586680239, 1.382578538659579914, -62.08265642326169598 ) ) ;
#42033=ORIENTED_EDGE ( 'NONE', *, *, #8742, .T. ) ;
#42051=CARTESIAN_POINT ( 'NONE',  ( 73.15108049797990475, 0.8888742037077599356, -62.35931220671550790 ) ) ;
#42053=CARTESIAN_POINT ( 'NONE',  ( 72.72276342993330900, 1.080095028449130190, -69.50719766003020084 ) ) ;
#42067=CARTESIAN_POINT ( 'NONE',  ( 63.84704430308629952, 1.199410787637519960, -61.48962906069409939 ) ) ;
#42080=VERTEX_POINT ( 'NONE', #20248 ) ;
#42102=CARTESIAN_POINT ( 'NONE',  ( 64.20744331450271147, 1.091543525800269920, -70.18026150519258977 ) ) ;
#42108=ADVANCED_FACE ( 'NONE', ( #36240 ), #348, .T. ) ;
#42114=EDGE_CURVE ( 'NONE', #28243, #51085, #51603, .T. ) ;
#42115=CARTESIAN_POINT ( 'NONE',  ( 63.25638208530150308, 1.265664290790570190, -68.85308916926389600 ) ) ;
#42122=ORIENTED_EDGE ( 'NONE', *, *, #47847, .F. ) ;
#42127=CARTESIAN_POINT ( 'NONE',  ( 71.26464087954850868, 1.328073773609210084, -70.46779242537471077 ) ) ;
#42136=CARTESIAN_POINT ( 'NONE',  ( 71.60339545440879760, 0.9065823421260940096, -70.54525856488069735 ) ) ;
#42177=CARTESIAN_POINT ( 'NONE',  ( 65.02843368015311398, 1.270877794983130027, -60.72281693841739525 ) ) ;
#42202=CARTESIAN_POINT ( 'NONE',  ( 64.97085660027880749, 1.369719003397489976, -60.94773069968270107 ) ) ;
#42207=CARTESIAN_POINT ( 'NONE',  ( 72.87455824417588701, 1.326134026835569912, -68.94513744192749982 ) ) ;
#42209=CARTESIAN_POINT ( 'NONE',  ( 72.89060928222170332, 1.370937308141420230, -62.62705977251020784 ) ) ;
#42215=CARTESIAN_POINT ( 'NONE',  ( 64.88003574513449223, 1.187237555532410171, -70.57991217294409125 ) ) ;
#42232=EDGE_CURVE ( 'NONE', #45766, #1196, #10611, .T. ) ;
#42252=CARTESIAN_POINT ( 'NONE',  ( 63.43393739769620510, 1.383811055320669947, -68.50657137141709541 ) ) ;
#42258=CARTESIAN_POINT ( 'NONE',  ( 63.33388541776029257, 1.264121749638649872, -62.30317625966389983 ) ) ;
#42301=LINE ( 'NONE', #22359, #27497 ) ;
#42309=EDGE_CURVE ( 'NONE', #35448, #11637, #35414, .T. ) ;
#42310=B_SPLINE_SURFACE_WITH_KNOTS ( 'NONE', 3, 3, ( 
 ( #42252, #6351, #34362, #22568, #15752, #19426, #28295, #31707, #12334, #39862 ),
 ( #39605, #16009, #8659, #44300, #3709, #19926, #32216, #3453, #31456, #43792 ),
 ( #11836, #7893, #20181, #20435, #15503, #23839, #279, #35406, #16263, #47481 ),
 ( #3964, #27536, #19677, #36171, #35919, #48240, #47731, #8407, #43542, #8149 ),
 ( #24354, #35674, #51404, #40368, #4465, #27796, #47988, #31966, #32464, #36422 ),
 ( #529, #39354, #16515, #34, #40115, #12087, #23587, #28041, #51659, #44046 ),
 ( #11574, #24093, #48494, #4209, #12597, #28558, #44560, #7642, #34223, #44822 ),
 ( #9884, #26106, #10149, #14075, #42115, #18522, #22432, #784, #28820, #37925 ),
 ( #48760, #30036, #49729, #18001, #2023, #24614, #4993, #20690, #40625, #36680 ),
 ( #6217, #22173, #46059, #38184, #34495, #38441, #16783, #8929, #33965, #20956 ),
 ( #2278, #13817, #49982, #18254, #4725, #36952, #32730, #12865, #24874, #6475 ),
 ( #2541, #1764, #50242, #25840, #10411, #14332, #17745, #33715, #30301, #5958 ),
 ( #46318, #26360, #42378, #29777, #40883, #50499, #45796, #41853, #21917, #14589 ),
 ( #30559, #46579, #3834, #26625, #22696, #35796, #50757, #27664, #35541, #38969 ),
 ( #51531, #3060, #15629, #11187, #11448, #10927, #39220, #31837, #31580, #26895 ),
 ( #3580, #42641, #2804, #15111, #51013, #35008, #31070, #43408, #43666, #38712 ) ),
 .UNSPECIFIED., .F., .F., .F.,
 ( 4, 2, 2, 2, 2, 2, 2, 4 ),
 ( 4, 1, 1, 1, 1, 1, 1, 4 ),
 ( -8.880243999999999390E-15, 0.07216186899280199740, 0.1546325764131560032, 0.2061767685508779924, 0.2319488646197390147, 0.2731842183299159621, 0.3391607842661999994, 0.4123535371017649775 ),
 ( 0.000000000000000000, 0.1428571428571430157, 0.2857142857142860315, 0.4285714285714289917, 0.5714285714285709528, 0.7142857142857139685, 0.8571428571428569843, 1.000000000000000000 ),
 .UNSPECIFIED. ) ;
#42320=CARTESIAN_POINT ( 'NONE',  ( 71.33393739769628894, 1.530257664727401767, -69.99644660940670349 ) ) ;
#42331=CARTESIAN_POINT ( 'NONE',  ( 63.94317349953750096, 1.409272994606969975, -61.59476957024820365 ) ) ;
#42363=CARTESIAN_POINT ( 'NONE',  ( 64.66082326855108420, 1.024253516290760002, -70.53167046690938946 ) ) ;
#42378=CARTESIAN_POINT ( 'NONE',  ( 63.43898171031389666, 1.369976237678190101, -68.83116145970220146 ) ) ;
#42386=ORIENTED_EDGE ( 'NONE', *, *, #38939, .T. ) ;
#42387=CARTESIAN_POINT ( 'NONE',  ( 71.47398825900590680, 0.9272522097098119254, -70.63440435907199344 ) ) ;
#42408=AXIS2_PLACEMENT_3D ( 'NONE', #14470, #33855, #22576 ) ;
#42412=CIRCLE ( 'NONE', #31495, 0.5000000000000004441 ) ;
#42421=ORIENTED_EDGE ( 'NONE', *, *, #3918, .F. ) ;
#42436=AXIS2_PLACEMENT_3D ( 'NONE', #2865, #18830, #7829 ) ;
#42441=CARTESIAN_POINT ( 'NONE',  ( 64.97448143965360146, 1.327097482837290121, -60.84525133028229504 ) ) ;
#42471=CARTESIAN_POINT ( 'NONE',  ( 72.89924231985609993, 1.371651820402789879, -62.65029732562830844 ) ) ;
#42478=CARTESIAN_POINT ( 'NONE',  ( 65.05077035654551310, 1.384378348444520013, -70.31241234944640439 ) ) ;
#42489=EDGE_CURVE ( 'NONE', #5288, #49378, #6457, .T. ) ;
#42499=ORIENTED_EDGE ( 'NONE', *, *, #21241, .T. ) ;
#42535=FACE_OUTER_BOUND ( 'NONE', #40009, .T. ) ;
#42537=CARTESIAN_POINT ( 'NONE',  ( 71.36689417337970553, 0.9219904752505979628, -60.59541050710320320 ) ) ;
#42576=CYLINDRICAL_SURFACE ( 'NONE', #38887, 0.5000000000000154321 ) ;
#42594=CARTESIAN_POINT ( 'NONE',  ( 63.90248588247730765, 1.347758125946160179, -61.55177802591560265 ) ) ;
#42601=VECTOR ( 'NONE', #45309, 1000.000000000000000 ) ;
#42625=TOROIDAL_SURFACE ( 'NONE', #20002, 1.499999999983230081, 0.4999999999993299804 ) ;
#42627=CARTESIAN_POINT ( 'NONE',  ( 64.61284426162950467, 0.9526384849486110307, -70.50836581366849032 ) ) ;
#42637=CARTESIAN_POINT ( 'NONE',  ( 71.62064552848029564, 0.9479899806831150189, -70.53291850127411067 ) ) ;
#42641=CARTESIAN_POINT ( 'NONE',  ( 63.52141932237860544, 1.390806392144110060, -68.86952544730040415 ) ) ;
#42650=CARTESIAN_POINT ( 'NONE',  ( 71.23851365796429036, 1.390208944942409985, -70.27002685503239832 ) ) ;
#42661=ORIENTED_EDGE ( 'NONE', *, *, #11436, .T. ) ;
#42665=DIRECTION ( 'NONE',  ( -1.080939296543039954E-11, -1.000000000000000000, 2.435884827299240233E-11 ) ) ;
#42700=CARTESIAN_POINT ( 'NONE',  ( 64.90488303983269702, 1.264791438333819906, -60.78603624114159487 ) ) ;
#42701=VECTOR ( 'NONE', #49130, 1000.000000000000000 ) ;
#42704=VECTOR ( 'NONE', #15413, 1000.000000000000000 ) ;
#42707=DIRECTION ( 'NONE',  ( -4.537176718267040445E-11, -1.000000000000000000, 6.290312716002009228E-11 ) ) ;
#42715=EDGE_LOOP ( 'NONE', ( #12113, #25093, #38010, #13936, #28747, #46959 ) ) ;
#42723=CARTESIAN_POINT ( 'NONE',  ( 64.77076777328539947, 1.370387345317999994, -61.01480881516509669 ) ) ;
#42731=CARTESIAN_POINT ( 'NONE',  ( 72.93398937763220147, 1.264121749638659864, -68.99682374033621102 ) ) ;
#42733=CARTESIAN_POINT ( 'NONE',  ( 73.02743803608620965, 1.099344084866040072, -62.24193811877859162 ) ) ;
#42740=CARTESIAN_POINT ( 'NONE',  ( 64.95388650200969494, 1.388313565858560139, -70.27734465158509636 ) ) ;
#42760=ORIENTED_EDGE ( 'NONE', *, *, #43713, .F. ) ;
#42783=CARTESIAN_POINT ( 'NONE',  ( 63.25402410758490390, 0.9098571636355680115, -62.15909090909049439 ) ) ;
#42797=CARTESIAN_POINT ( 'NONE',  ( 71.40743923234819590, 0.9234936569010840923, -60.62162712823539579 ) ) ;
#42799=CARTESIAN_POINT ( 'NONE',  ( 72.93063970810558772, 1.138495779908299754, -62.11940254112219861 ) ) ;
#42856=CARTESIAN_POINT ( 'NONE',  ( 63.57924418363759855, 1.254613999360089993, -61.86253808879629901 ) ) ;
#42861=CARTESIAN_POINT ( 'NONE',  ( 73.09272852564158995, 1.276058558775509999, -68.69062364193268877 ) ) ;
#42881=ADVANCED_FACE ( 'NONE', ( #39692 ), #14004, .T. ) ;
#42889=CARTESIAN_POINT ( 'NONE',  ( 64.66196796819860992, 1.134321519919950116, -70.48604978123970000 ) ) ;
#42896=CARTESIAN_POINT ( 'NONE',  ( 71.96892370708050635, 1.258806274518780022, -70.16925935983108786 ) ) ;
#42910=CARTESIAN_POINT ( 'NONE',  ( 71.25658036288379549, 1.391252479931859964, -70.26382307879899258 ) ) ;
#42913=CARTESIAN_POINT ( 'NONE',  ( 63.93393739769619089, 10.88381105532070059, -62.44999999999999574 ) ) ;
#42930=CARTESIAN_POINT ( 'NONE',  ( 71.57216560976189612, 1.132579237369250036, -60.79187696645490036 ) ) ;
#42956=CARTESIAN_POINT ( 'NONE',  ( 65.05887334876679517, 1.388715606738730068, -61.01996879627380110 ) ) ;
#42989=CARTESIAN_POINT ( 'NONE',  ( 72.80507874878320251, 1.371509258145890087, -68.88889814452579685 ) ) ;
#42991=CARTESIAN_POINT ( 'NONE',  ( 72.74645547301390991, 1.390806392144110060, -62.43047455269960011 ) ) ;
#42997=CARTESIAN_POINT ( 'NONE',  ( 64.64302830678690270, 0.9098571636355550218, -70.52991329011150867 ) ) ;
#43013=EDGE_CURVE ( 'NONE', #9287, #14211, #34910, .T. ) ;
#43053=CARTESIAN_POINT ( 'NONE',  ( 71.26764986431300031, 0.9952464559119579279, -60.54306244337850273 ) ) ;
#43055=CARTESIAN_POINT ( 'NONE',  ( 72.42107927723590421, 1.200163167270710041, -61.48893495576489698 ) ) ;
#43057=CARTESIAN_POINT ( 'NONE',  ( 65.01767771978660448, 0.8838110553206759423, -70.77727272727270247 ) ) ;
#43079=AXIS2_PLACEMENT_3D ( 'NONE', #36699, #24631, #48256 ) ;
#43084=EDGE_CURVE ( 'NONE', #43577, #26724, #41108, .T. ) ;
#43111=CARTESIAN_POINT ( 'NONE',  ( 63.54731047306190561, 1.396834109478129804, -62.44999999999999574 ) ) ;
#43114=FACE_OUTER_BOUND ( 'NONE', #13236, .T. ) ;
#43115=CARTESIAN_POINT ( 'NONE',  ( 73.18334309134590399, 0.9940423591679348192, -68.87653036433009390 ) ) ;
#43151=CARTESIAN_POINT ( 'NONE',  ( 72.00766661773259614, 1.338417587229379979, -70.07245980288250564 ) ) ;
#43161=CARTESIAN_POINT ( 'NONE',  ( 63.58805182154581104, 0.9952259095800390920, -69.56719234871339097 ) ) ;
#43166=CARTESIAN_POINT ( 'NONE',  ( 71.35306154470789863, 1.325839985408290067, -70.42711907493250578 ) ) ;
#43179=ORIENTED_EDGE ( 'NONE', *, *, #21241, .F. ) ;
#43213=ORIENTED_EDGE ( 'NONE', *, *, #1370, .T. ) ;
#43215=CARTESIAN_POINT ( 'NONE',  ( 64.84946247134770658, 1.186701509386330011, -60.73797667709650483 ) ) ;
#43224=CARTESIAN_POINT ( 'NONE',  ( 63.66068354842749244, 0.9098571636355720083, -68.84999999999999432 ) ) ;
#43242=CIRCLE ( 'NONE', #28999, 0.5000000000000004441 ) ;
#43246=B_SPLINE_CURVE_WITH_KNOTS ( 'NONE', 3,
 ( #7578, #48896, #3390, #27730, #43980, #19097, #44951, #24031, #11249, #40053, #36820, #4856, #47418, #35338, #12997, #9051, #27211, #3643, #15438, #51078 ),
 .UNSPECIFIED., .F., .F.,
 ( 4, 2, 2, 2, 2, 2, 2, 2, 2, 4 ),
 ( -1.826192301619919967, -1.710015269441619967, -1.458000257336709904, -1.209852399823200031, -1.027233169661200041, -0.9130961508099589841, -0.6848221131074689882, -0.4130753771317612344, -0.1614840352128998902, 0.000000000000000000 ),
 .UNSPECIFIED. ) ;
#43251=CARTESIAN_POINT ( 'NONE',  ( 73.09245838956729813, 1.096153228089730147, -62.34242842016499964 ) ) ;
#43308=CARTESIAN_POINT ( 'NONE',  ( 71.33393739769628894, 1.383811055320669947, -61.44999999999999574 ) ) ;
#43310=CARTESIAN_POINT ( 'NONE',  ( 71.13601697155240799, 1.385888765344509999, -60.99577487439199786 ) ) ;
#43312=CARTESIAN_POINT ( 'NONE',  ( 72.17449546179830122, 1.458407608744489936, -61.54081785568290286 ) ) ;
#43339=B_SPLINE_CURVE_WITH_KNOTS ( 'NONE', 3,
 ( #13380, #29340, #13634, #45597, #46128, #41142, #45342, #50312, #9447, #41397, #37993, #49542, #5515, #49283, #50045, #14138 ),
 .UNSPECIFIED., .F., .F.,
 ( 4, 2, 2, 2, 2, 2, 2, 4 ),
 ( -4.551914000000000309E-15, 0.07319275283555799760, 0.1391693187718399949, 0.1804046724820149994, 0.2061767685508749948, 0.2577209606885960125, 0.3401916681089480199, 0.4123535371017559847 ),
 .UNSPECIFIED. ) ;
#43359=CARTESIAN_POINT ( 'NONE',  ( 63.86181505067941089, 1.033004162168289941, -61.43684260791479801 ) ) ;
#43368=CARTESIAN_POINT ( 'NONE',  ( 63.35923387292240250, 1.230946250268760034, -62.19265059571660004 ) ) ;
#43369=ORIENTED_EDGE ( 'NONE', *, *, #39154, .F. ) ;
#43372=CARTESIAN_POINT ( 'NONE',  ( 72.82137280411760116, 1.383928098097870096, -68.54761322559109260 ) ) ;
#43375=ORIENTED_EDGE ( 'NONE', *, *, #35434, .T. ) ;
#43390=CARTESIAN_POINT ( 'NONE',  ( 72.80768847294999091, 1.384447124000270035, -62.70866005236110396 ) ) ;
#43402=CARTESIAN_POINT ( 'NONE',  ( 71.76028641513160267, 1.321111291667659948, -70.24077000692989259 ) ) ;
#43408=CARTESIAN_POINT ( 'NONE',  ( 63.25162284297759641, 1.007912009470870229, -69.12629645913949616 ) ) ;
#43411=ADVANCED_FACE ( 'NONE', ( #11211 ), #24028, .F. ) ;
#43420=CARTESIAN_POINT ( 'NONE',  ( 71.42907483962369497, 1.326134026835569912, -70.39062084647959239 ) ) ;
#43448=CARTESIAN_POINT ( 'NONE',  ( 63.18115153217100755, 0.8966068345641480253, -69.03681046574699565 ) ) ;
#43464=CARTESIAN_POINT ( 'NONE',  ( 64.86758340617990370, 0.9945465939392541532, -60.62606712929739672 ) ) ;
#43499=CARTESIAN_POINT ( 'NONE',  ( 73.11007580172049813, 0.9281439705311369526, -62.29764659744859756 ) ) ;
#43502=DIRECTION ( 'NONE',  ( 0.000000000000000000, 0.000000000000000000, -1.000000000000000000 ) ) ;
#43542=CARTESIAN_POINT ( 'NONE',  ( 63.06339012708429692, 0.9214125008369580261, -68.85787081529349507 ) ) ;
#43564=CARTESIAN_POINT ( 'NONE',  ( 71.15549028777350316, 1.383161449028130097, -60.96613084263369586 ) ) ;
#43566=CARTESIAN_POINT ( 'NONE',  ( 72.46066273947089087, 1.275252243133929930, -61.58318855245290280 ) ) ;
#43567=CIRCLE ( 'NONE', #30971, 0.5000000000000004441 ) ;
#43577=VERTEX_POINT ( 'NONE', #17204 ) ;
#43611=CARTESIAN_POINT ( 'NONE',  ( 63.23767253740619765, 1.267233196669030004, -62.48314610740069242 ) ) ;
#43617=DIRECTION ( 'NONE',  ( 0.000000000000000000, 0.000000000000000000, 1.000000000000000000 ) ) ;
#43624=CARTESIAN_POINT ( 'NONE',  ( 63.31978226060338955, 1.136600705754869933, -62.14534926897810152 ) ) ;
#43628=CARTESIAN_POINT ( 'NONE',  ( 73.08075677931830683, 1.188042061556800144, -68.87465088918141021 ) ) ;
#43640=AXIS2_PLACEMENT_3D ( 'NONE', #3996, #8699, #15784 ) ;
#43659=CARTESIAN_POINT ( 'NONE',  ( 71.90239294763270550, 0.9973858971030851173, -70.31979469916329606 ) ) ;
#43665=VECTOR ( 'NONE', #13796, 1000.000000000000000 ) ;
#43666=CARTESIAN_POINT ( 'NONE',  ( 63.25144821230251324, 0.9425424353906030062, -69.13730826794480322 ) ) ;
#43669=CARTESIAN_POINT ( 'NONE',  ( 63.32231416895070453, 0.9254875393589929722, -69.23491771966379815 ) ) ;
#43675=CARTESIAN_POINT ( 'NONE',  ( 64.74323834027561020, 1.229084191802120030, -60.83585027030739667 ) ) ;
#43701=CARTESIAN_POINT ( 'NONE',  ( 64.43393739769608430, 11.38381105532050519, -61.94999999999998863 ) ) ;
#43713=EDGE_CURVE ( 'NONE', #41820, #29784, #2290, .T. ) ;
#43714=EDGE_CURVE ( 'NONE', #17827, #9229, #38294, .T. ) ;
#43729=DIRECTION ( 'NONE',  ( 1.000000000000000000, 0.000000000000000000, 0.000000000000000000 ) ) ;
#43751=CARTESIAN_POINT ( 'NONE',  ( 73.08495881288720852, 1.096305581841160004, -62.33061120451039727 ) ) ;
#43757=CARTESIAN_POINT ( 'NONE',  ( 64.66447934098378880, 0.9065823421260920112, -70.54525856488079683 ) ) ;
#43792=CARTESIAN_POINT ( 'NONE',  ( 63.02029346573409185, 0.8838110553206759423, -68.78868353141480441 ) ) ;
#43815=CARTESIAN_POINT ( 'NONE',  ( 71.34424925767550008, 1.265401080857980087, -60.77621068871049204 ) ) ;
#43817=CARTESIAN_POINT ( 'NONE',  ( 72.43519100933379207, 1.033013263524900083, -61.46596897695270201 ) ) ;
#43841=CARTESIAN_POINT ( 'NONE',  ( 63.08005232011709751, 0.8859637708054499683, -62.41593972647849853 ) ) ;
#43849=CARTESIAN_POINT ( 'NONE',  ( 63.62896973943209389, 1.416241615474740145, -69.07296579632759403 ) ) ;
#43861=CARTESIAN_POINT ( 'NONE',  ( 63.06902243323368396, 0.9940695285616559795, -62.44811160372290004 ) ) ;
#43865=CARTESIAN_POINT ( 'NONE',  ( 64.00995881370980101, 1.028300555801489935, -61.29114157291949994 ) ) ;
#43875=CARTESIAN_POINT ( 'NONE',  ( 63.29959049205589849, 1.031491003832160080, -62.11015851666019927 ) ) ;
#43914=CARTESIAN_POINT ( 'NONE',  ( 72.63216195444580592, 1.261444690199509999, -69.51221393975839646 ) ) ;
#43925=ORIENTED_EDGE ( 'NONE', *, *, #5846, .F. ) ;
#43929=CARTESIAN_POINT ( 'NONE',  ( 71.54199927891758648, 1.099344084866040072, -70.54350063839000029 ) ) ;
#43935=DIRECTION ( 'NONE',  ( 0.000000000000000000, 0.000000000000000000, 1.000000000000000000 ) ) ;
#43940=EDGE_CURVE ( 'NONE', #37903, #38406, #4990, .T. ) ;
#43942=DIRECTION ( 'NONE',  ( 0.000000000000000000, 0.000000000000000000, 1.000000000000000000 ) ) ;
#43955=DIRECTION ( 'NONE',  ( 0.000000000000000000, 0.000000000000000000, 1.000000000000000000 ) ) ;
#43958=CARTESIAN_POINT ( 'NONE',  ( 69.73393739769620936, 11.23736444591397543, -61.59644660940672622 ) ) ;
#43980=CARTESIAN_POINT ( 'NONE',  ( 72.83009333885360093, 0.9561296872639739597, -69.38553930450309792 ) ) ;
#44030=EDGE_CURVE ( 'NONE', #23138, #8243, #4795, .T. ) ;
#44037=CARTESIAN_POINT ( 'NONE',  ( 71.33393739769650210, 1.396834109478129804, -61.06337307536569625 ) ) ;
#44046=CARTESIAN_POINT ( 'NONE',  ( 63.10653712364238999, 0.8879664753683469414, -68.92499589875220067 ) ) ;
#44048=CARTESIAN_POINT ( 'NONE',  ( 64.08038400710292137, 11.23736444591397543, -64.04999999999999716 ) ) ;
#44049=VERTEX_POINT ( 'NONE', #24352 ) ;
#44057=CARTESIAN_POINT ( 'NONE',  ( 71.21254218222989607, 1.330484379554840002, -70.49093568668439502 ) ) ;
#44065=PLANE ( 'NONE',  #22731 ) ;
#44067=CARTESIAN_POINT ( 'NONE',  ( 71.47612964547808190, 0.8925687589132640376, -60.66703147076970737 ) ) ;
#44068=EDGE_CURVE ( 'NONE', #16929, #51296, #43339, .T. ) ;
#44070=CARTESIAN_POINT ( 'NONE',  ( 72.43412257677050547, 1.117804454683279936, -61.47169494157739678 ) ) ;
#44074=CARTESIAN_POINT ( 'NONE',  ( 65.02006347151939281, 1.101170701158060039, -70.72594205704909598 ) ) ;
#44077=CARTESIAN_POINT ( 'NONE',  ( 71.33393739769799424, 10.88381105532070059, -61.45000000000079865 ) ) ;
#44103=CARTESIAN_POINT ( 'NONE',  ( 63.54731047306190561, 1.396834109478129804, -68.84999999999999432 ) ) ;
#44118=CARTESIAN_POINT ( 'NONE',  ( 63.30967889250540992, 1.328674444234399843, -62.53373279716100086 ) ) ;
#44122=CARTESIAN_POINT ( 'NONE',  ( 72.51559007951500746, 1.439519383694849886, -61.97453994048029813 ) ) ;
#44138=ORIENTED_EDGE ( 'NONE', *, *, #27836, .T. ) ;
#44144=CARTESIAN_POINT ( 'NONE',  ( 71.33393739769628894, 10.88381105532070059, -61.44999999999999574 ) ) ;
#44147=ORIENTED_EDGE ( 'NONE', *, *, #11741, .F. ) ;
#44168=CARTESIAN_POINT ( 'NONE',  ( 72.29280397036849592, 1.443019669817199979, -69.67232717175519952 ) ) ;
#44180=CARTESIAN_POINT ( 'NONE',  ( 64.81872023251169423, 1.368315088675869928, -60.99398296987489942 ) ) ;
#44181=ORIENTED_EDGE ( 'NONE', *, *, #45187, .T. ) ;
#44182=CARTESIAN_POINT ( 'NONE',  ( 71.57861930639089110, 0.9369374701296400154, -70.56272516144490226 ) ) ;
#44269=CARTESIAN_POINT ( 'NONE',  ( 71.55691549992010891, 1.416242794300029972, -70.15496246767990840 ) ) ;
#44276=DIRECTION ( 'NONE',  ( 0.000000000000000000, 0.000000000000000000, 1.000000000000000000 ) ) ;
#44280=SHAPE_DEFINITION_REPRESENTATION ( #39852, #50919 ) ;
#44300=CARTESIAN_POINT ( 'NONE',  ( 63.25550833076970747, 1.336371993404959824, -68.64083569922701145 ) ) ;
#44311=CARTESIAN_POINT ( 'NONE',  ( 71.11795458202399800, 1.382840740411490188, -70.34664320112889868 ) ) ;
#44315=DIRECTION ( 'NONE',  ( 0.000000000000000000, -1.000000000000000000, 0.000000000000000000 ) ) ;
#44321=CARTESIAN_POINT ( 'NONE',  ( 71.37118938927949330, 1.325715844996850024, -60.88145737504000010 ) ) ;
#44323=CARTESIAN_POINT ( 'NONE',  ( 71.63858812870320492, 1.136600705753829876, -60.83584486289709758 ) ) ;
#44325=CARTESIAN_POINT ( 'NONE',  ( 65.11099717020638877, 1.370937308141410238, -70.40667188452549397 ) ) ;
#44329=AXIS2_PLACEMENT_3D ( 'NONE', #6473, #38182, #50496 ) ;
#44343=CARTESIAN_POINT ( 'NONE',  ( 65.27736602627911111, 1.383811055320669947, -60.94999999999999574 ) ) ;
#44374=CARTESIAN_POINT ( 'NONE',  ( 63.03382193542370260, 0.9209334348186318797, -62.48938310929649731 ) ) ;
#44380=CARTESIAN_POINT ( 'NONE',  ( 71.59408232549860429, 1.419970371292400113, -61.16051820649249748 ) ) ;
#44386=DIRECTION ( 'NONE',  ( 0.000000000000000000, 0.000000000000000000, 1.000000000000000000 ) ) ;
#44404=EDGE_CURVE ( 'NONE', #45770, #8243, #40819, .T. ) ;
#44414=CARTESIAN_POINT ( 'NONE',  ( 64.93393739769619799, 1.883811055320669947, -60.94999999999999574 ) ) ;
#44421=CARTESIAN_POINT ( 'NONE',  ( 64.08038400710292137, 11.23736444591397543, -68.84999999999999432 ) ) ;
#44429=CARTESIAN_POINT ( 'NONE',  ( 72.24967035273689930, 1.113948672550079788, -70.00993265641670860 ) ) ;
#44462=ORIENTED_EDGE ( 'NONE', *, *, #44068, .T. ) ;
#44484=AXIS2_PLACEMENT_3D ( 'NONE', #48233, #16510, #12329 ) ;
#44506=CARTESIAN_POINT ( 'NONE',  ( 65.02936113742819657, 1.390208944942409985, -61.02997314496759884 ) ) ;
#44529=CARTESIAN_POINT ( 'NONE',  ( 72.40210087067039524, 1.451792515613489876, -69.49977495595670973 ) ) ;
#44550=CARTESIAN_POINT ( 'NONE',  ( 71.09849264842429761, 1.384887413063060180, -60.98363600610959878 ) ) ;
#44560=CARTESIAN_POINT ( 'NONE',  ( 63.14473109323350286, 1.096110717717199812, -68.90857121967530929 ) ) ;
#44563=ORIENTED_EDGE ( 'NONE', *, *, #34960, .F. ) ;
#44571=CARTESIAN_POINT ( 'NONE',  ( 70.99050876911339003, 1.383811055320669947, -70.34999999999999432 ) ) ;
#44576=CARTESIAN_POINT ( 'NONE',  ( 72.98500336837570046, 1.331842543267529821, -68.70530175958410268 ) ) ;
#44579=CARTESIAN_POINT ( 'NONE',  ( 72.92981560451809742, 1.375383258925270136, -62.73515566246579311 ) ) ;
#44582=CARTESIAN_POINT ( 'NONE',  ( 71.19761362482960010, 1.388189907116970101, -61.01613942410280345 ) ) ;
#44584=CARTESIAN_POINT ( 'NONE',  ( 71.98371235365300436, 1.451792515613489876, -61.38183652702590365 ) ) ;
#44586=CARTESIAN_POINT ( 'NONE',  ( 65.11238450761909746, 1.383161449028130097, -70.33386915736640788 ) ) ;
#44614=CARTESIAN_POINT ( 'NONE',  ( 63.92800470363879839, 1.456055302763120007, -69.58268673945899252 ) ) ;
#44628=CARTESIAN_POINT ( 'NONE',  ( 63.02016742692980245, 0.9209567800143640959, -62.51152384389749272 ) ) ;
#44633=CARTESIAN_POINT ( 'NONE',  ( 71.51437757259260763, 1.412203896155519889, -61.12765129660999719 ) ) ;
#44639=CARTESIAN_POINT ( 'NONE',  ( 71.33393739769628894, 1.883811055320669947, -70.34999999999999432 ) ) ;
#44657=ADVANCED_FACE ( 'NONE', ( #6324 ), #30783, .F. ) ;
#44685=CARTESIAN_POINT ( 'NONE',  ( 72.51142765151010394, 1.054781932184780002, -69.75391249758430945 ) ) ;
#44698=CARTESIAN_POINT ( 'NONE',  ( 64.54901150452390368, 0.9254890127232510144, -60.83838280017310041 ) ) ;
#44706=DIRECTION ( 'NONE',  ( 0.000000000000000000, 0.000000000000000000, 1.000000000000000000 ) ) ;
#44738=EDGE_CURVE ( 'NONE', #1196, #12484, #13267, .T. ) ;
#44743=CARTESIAN_POINT ( 'NONE',  ( 64.03570111260079045, 1.347758383967160078, -69.88143807632219762 ) ) ;
#44784=AXIS2_PLACEMENT_3D ( 'NONE', #5901, #30249, #21601 ) ;
#44822=CARTESIAN_POINT ( 'NONE',  ( 63.11679429741250402, 0.8888742037077569380, -68.94068779328439689 ) ) ;
#44826=ORIENTED_EDGE ( 'NONE', *, *, #921, .T. ) ;
#44837=CARTESIAN_POINT ( 'NONE',  ( 71.29497000743199919, 0.8840451408750739093, -70.74985906855570761 ) ) ;
#44843=CARTESIAN_POINT ( 'NONE',  ( 72.75396425272869294, 1.390208944942409985, -68.75457626026799574 ) ) ;
#44848=CARTESIAN_POINT ( 'NONE',  ( 71.43836573789050703, 0.9955677559369568996, -60.65081522799539471 ) ) ;
#44850=CARTESIAN_POINT ( 'NONE',  ( 71.59128680196450034, 1.230946250268210029, -60.87529647521710530 ) ) ;
#44853=CARTESIAN_POINT ( 'NONE',  ( 64.92925538503580185, 1.097085799869280009, -70.67221403600389351 ) ) ;
#44864=DIRECTION ( 'NONE',  ( 9.209768215203483886E-28, -6.141198660767589922E-12, -1.000000000000000000 ) ) ;
#44865=VECTOR ( 'NONE', #40839, 1000.000000000000000 ) ;
#44876=VECTOR ( 'NONE', #51026, 1000.000000000000000 ) ;
#44881=ORIENTED_EDGE ( 'NONE', *, *, #41647, .T. ) ;
#44893=CARTESIAN_POINT ( 'NONE',  ( 63.20402522475220053, 1.187237555532410171, -62.39609834743819761 ) ) ;
#44896=CARTESIAN_POINT ( 'NONE',  ( 63.43393739769620510, 0.8838110553206759423, -68.50657137141709541 ) ) ;
#44897=CARTESIAN_POINT ( 'NONE',  ( 72.27703085588929355, 1.458412159422780130, -61.64333151374460584 ) ) ;
#44923=CARTESIAN_POINT ( 'NONE',  ( 64.36679430080839381, 1.446932438105809737, -61.32315308161489753 ) ) ;
#44934=CARTESIAN_POINT ( 'NONE',  ( 72.77636315587029969, 1.387131204727290124, -62.61203846038919352 ) ) ;
#44944=ORIENTED_EDGE ( 'NONE', *, *, #47966, .F. ) ;
#44949=CARTESIAN_POINT ( 'NONE',  ( 72.26003265285929444, 1.443555314919450216, -69.70765349352710416 ) ) ;
#44951=CARTESIAN_POINT ( 'NONE',  ( 72.65863549626330098, 1.000506532484680022, -69.59146369456030357 ) ) ;
#44960=CARTESIAN_POINT ( 'NONE',  ( 64.26074781679190551, 1.176186365485389906, -61.10801278039449613 ) ) ;
#45004=CARTESIAN_POINT ( 'NONE',  ( 63.83374159272360515, 1.117803980320120072, -69.82829407303259472 ) ) ;
#45034=CARTESIAN_POINT ( 'NONE',  ( 72.80030139158668590, 1.384887413063060180, -68.61455525072810246 ) ) ;
#45047=CARTESIAN_POINT ( 'NONE',  ( 64.93393739769619799, 1.883811055320669947, -70.34999999999999432 ) ) ;
#45048=CARTESIAN_POINT ( 'NONE',  ( 72.65628610108569774, 1.412203896155640015, -69.03044017489760620 ) ) ;
#45074=ADVANCED_FACE ( 'NONE', ( #7037 ), #23494, .F. ) ;
#45076=CARTESIAN_POINT ( 'NONE',  ( 72.92981560451809742, 1.375383258925270136, -68.56484433753419694 ) ) ;
#45093=CARTESIAN_POINT ( 'NONE',  ( 71.10413293483961183, 1.338092079250050137, -70.53694914618849054 ) ) ;
#45099=CARTESIAN_POINT ( 'NONE',  ( 72.80287646850260330, 1.383922910988889976, -68.71460001914260829 ) ) ;
#45107=CARTESIAN_POINT ( 'NONE',  ( 72.00360496390891285, 1.017423949637090042, -61.06375415878460444 ) ) ;
#45110=CARTESIAN_POINT ( 'NONE',  ( 65.02205492013339949, 0.9960089569207349891, -70.77007079217121088 ) ) ;
#45151=CARTESIAN_POINT ( 'NONE',  ( 63.17939165373819321, 0.9307121176571839793, -62.26576483763439995 ) ) ;
#45186=B_SPLINE_CURVE_WITH_KNOTS ( 'NONE', 3,
 ( #51256, #15350, #27388, #43390, #7485, #23436, #15608, #44934, #21321, #49141, #9034, #9305, #13237, #8248, #40738, #20283 ),
 .UNSPECIFIED., .F., .F.,
 ( 4, 2, 2, 2, 2, 2, 2, 4 ),
 ( 6.613222000000000237E-15, 0.07216186899281500089, 0.1546325764131659952, 0.2061767685508859860, 0.2319488646197460091, 0.2731842183299219573, 0.3391607842662039962, 0.4123535371017659767 ),
 .UNSPECIFIED. ) ;
#45187=EDGE_CURVE ( 'NONE', #44049, #11677, #50745, .T. ) ;
#45210=CARTESIAN_POINT ( 'NONE',  ( 73.11690592692650625, 0.8925687589132609290, -62.30780775221820278 ) ) ;
#45212=ADVANCED_FACE ( 'NONE', ( #28210 ), #31445, .F. ) ;
#45225=CARTESIAN_POINT ( 'NONE',  ( 64.56814038767528530, 1.034647430440490234, -60.83434081278629435 ) ) ;
#45227=CARTESIAN_POINT ( 'NONE',  ( 71.33393739769628894, 1.383811055320669947, -62.44999999999999574 ) ) ;
#45252=ADVANCED_FACE ( 'NONE', ( #47392 ), #23252, .T. ) ;
#45264=CARTESIAN_POINT ( 'NONE',  ( 64.04379473442959636, 1.409763143870969904, -69.80805258500740251 ) ) ;
#45280=ADVANCED_FACE ( 'NONE', ( #17471 ), #33437, .F. ) ;
#45286=CARTESIAN_POINT ( 'NONE',  ( 70.99050876911339003, 0.8838110553206759423, -60.94999999999999574 ) ) ;
#45293=CARTESIAN_POINT ( 'NONE',  ( 72.72056432233058842, 1.396834109478129804, -68.84999999999999432 ) ) ;
#45309=DIRECTION ( 'NONE',  ( -1.000000000000000000, 0.000000000000000000, 0.000000000000000000 ) ) ;
#45321=CIRCLE ( 'NONE', #3505, 5.500000000000005329 ) ;
#45335=CARTESIAN_POINT ( 'NONE',  ( 64.99525386628140211, 0.8838110553206759423, -60.53635606803790381 ) ) ;
#45338=CARTESIAN_POINT ( 'NONE',  ( 66.53393739769619231, 10.88381105532070059, -69.34999999999999432 ) ) ;
#45342=CARTESIAN_POINT ( 'NONE',  ( 64.79174514991440503, 0.8925687589132609290, -60.66703147076970737 ) ) ;
#45359=CARTESIAN_POINT ( 'NONE',  ( 71.21710443884710173, 1.384378348444520013, -70.31241234944640439 ) ) ;
#45364=CARTESIAN_POINT ( 'NONE',  ( 73.00772670898579975, 1.265401080857980087, -68.86031185997930493 ) ) ;
#45367=CARTESIAN_POINT ( 'NONE',  ( 73.20987945474540481, 1.101170701158060039, -62.53612607382319766 ) ) ;
#45371=CARTESIAN_POINT ( 'NONE',  ( 71.71899590570779992, 1.318402576460610209, -61.03419568858579680 ) ) ;
#45372=CARTESIAN_POINT ( 'NONE',  ( 73.01385068780759013, 0.9098571636355720083, -69.14090909090960224 ) ) ;
#45373=CARTESIAN_POINT ( 'NONE',  ( 65.03752560835739871, 1.369664981662529923, -70.37861443921559612 ) ) ;
#45416=CARTESIAN_POINT ( 'NONE',  ( 63.38363568028500339, 1.325841671674429900, -62.37472934403619718 ) ) ;
#45426=CARTESIAN_POINT ( 'NONE',  ( 63.55717560081600226, 1.377109494087380037, -69.13845142168129598 ) ) ;
#45430=CARTESIAN_POINT ( 'NONE',  ( 71.24581987525910165, 0.9960089569207349891, -60.52992920782880049 ) ) ;
#45432=AXIS2_PLACEMENT_3D ( 'NONE', #2133, #13931, #9738 ) ;
#45470=CARTESIAN_POINT ( 'NONE',  ( 72.71656993463111007, 0.9860880133275220505, -69.52393415259200538 ) ) ;
#45472=CARTESIAN_POINT ( 'NONE',  ( 71.83393739769628894, 11.38381105532070059, -68.85000000000408704 ) ) ;
#45482=EDGE_CURVE ( 'NONE', #46160, #9287, #30013, .T. ) ;
#45485=CARTESIAN_POINT ( 'NONE',  ( 64.23238216415199986, 1.087300712305290018, -61.09829428330199619 ) ) ;
#45524=CARTESIAN_POINT ( 'NONE',  ( 63.77351956156250878, 1.056849143885769893, -69.77234944045780196 ) ) ;
#45589=AXIS2_PLACEMENT_3D ( 'NONE', #5177, #41066, #703 ) ;
#45591=CARTESIAN_POINT ( 'NONE',  ( 65.01767771978660448, 0.9212109678634080590, -60.52272727272730179 ) ) ;
#45597=CARTESIAN_POINT ( 'NONE',  ( 64.72741779930979078, 0.8986939045430368811, -60.71074964625670134 ) ) ;
#45616=CARTESIAN_POINT ( 'NONE',  ( 72.94195630468689728, 1.327322800621349996, -68.80227784490020326 ) ) ;
#45619=CARTESIAN_POINT ( 'NONE',  ( 73.03020225798630349, 1.267233196669050210, -62.48314610740069242 ) ) ;
#45621=CARTESIAN_POINT ( 'NONE',  ( 71.40920805366010882, 1.325841671674429900, -60.89969828258869455 ) ) ;
#45625=CARTESIAN_POINT ( 'NONE',  ( 65.02936113742829605, 1.390208944942409985, -70.27002685503249779 ) ) ;
#45644=AXIS2_PLACEMENT_3D ( 'NONE', #26826, #35730, #51713 ) ;
#45671=CARTESIAN_POINT ( 'NONE',  ( 63.32918872797849019, 1.327097482837290121, -62.49054404195729973 ) ) ;
#45682=CARTESIAN_POINT ( 'NONE',  ( 63.58805182154581104, 0.9952259095800459754, -69.56719234871339097 ) ) ;
#45688=CARTESIAN_POINT ( 'NONE',  ( 72.96189588675559889, 1.134960180547819997, -62.16566220516190100 ) ) ;
#45712=CARTESIAN_POINT ( 'NONE',  ( 73.10855093309899644, 0.8936201581567910779, -69.00461532610479765 ) ) ;
#45732=CARTESIAN_POINT ( 'NONE',  ( 72.33393739769486785, 11.38381105531920845, -68.85000000000410125 ) ) ;
#45735=CARTESIAN_POINT ( 'NONE',  ( 64.93393739769619799, 1.396834109478129804, -70.23662692463440749 ) ) ;
#45743=EDGE_LOOP ( 'NONE', ( #32927, #15936, #27821, #24124, #15958, #26404, #21988, #15192, #38621, #34456, #12751, #20885, #22791, #2619 ) ) ;
#45745=CARTESIAN_POINT ( 'NONE',  ( 64.43604309779919959, 0.9828917932950889114, -60.92414392080449659 ) ) ;
#45766=VERTEX_POINT ( 'NONE', #39197 ) ;
#45770=VERTEX_POINT ( 'NONE', #35256 ) ;
#45775=EDGE_CURVE ( 'NONE', #14121, #4949, #45186, .T. ) ;
#45784=CARTESIAN_POINT ( 'NONE',  ( 64.00162532095220058, 1.348264980582170036, -69.84906706027560119 ) ) ;
#45796=CARTESIAN_POINT ( 'NONE',  ( 63.21464875163319874, 1.097545367735389910, -69.01875481685129898 ) ) ;
#45831=ORIENTED_EDGE ( 'NONE', *, *, #14445, .F. ) ;
#45884=DIRECTION ( 'NONE',  ( -1.000000000000000000, 0.000000000000000000, 0.000000000000000000 ) ) ;
#45885=CARTESIAN_POINT ( 'NONE',  ( 72.97487308438059017, 1.330484379554840002, -62.57139521546629624 ) ) ;
#45889=CARTESIAN_POINT ( 'NONE',  ( 71.29497000743199919, 0.8840451408750739093, -60.55014093144440324 ) ) ;
#45892=CARTESIAN_POINT ( 'NONE',  ( 65.03036676789579928, 1.369613126987639928, -70.37582656035600337 ) ) ;
#45899=CARTESIAN_POINT ( 'NONE',  ( 71.83393739769618946, 10.88381105532070059, -67.25000000000000000 ) ) ;
#45935=CARTESIAN_POINT ( 'NONE',  ( 63.15096886846599489, 0.8925687589132640376, -62.30780775221820278 ) ) ;
#45944=CARTESIAN_POINT ( 'NONE',  ( 63.42971025143901187, 1.310552486429319874, -69.07674887557429599 ) ) ;
#45950=CARTESIAN_POINT ( 'NONE',  ( 72.94808712738880274, 1.229084191802120030, -62.25930094257930136 ) ) ;
#45953=ORIENTED_EDGE ( 'NONE', *, *, #38939, .F. ) ;
#45991=CARTESIAN_POINT ( 'NONE',  ( 72.86935405752659278, 1.308983041454300000, -69.01646217275099104 ) ) ;
#46001=CARTESIAN_POINT ( 'NONE',  ( 65.13185782384009315, 1.385888765344500007, -70.30422512560809878 ) ) ;
#46009=CARTESIAN_POINT ( 'NONE',  ( 63.76999183493178691, 1.442158793902849956, -61.94395472936509606 ) ) ;
#46023=ORIENTED_EDGE ( 'NONE', *, *, #49288, .F. ) ;
#46040=EDGE_CURVE ( 'NONE', #33885, #48970, #32606, .T. ) ;
#46042=DIRECTION ( 'NONE',  ( 0.000000000000000000, -1.000000000000000000, 0.000000000000000000 ) ) ;
#46047=DIRECTION ( 'NONE',  ( 0.000000000000000000, 1.000000000000000000, 0.000000000000000000 ) ) ;
#46049=CARTESIAN_POINT ( 'NONE',  ( 64.67348939754930370, 1.419996320997050088, -70.13930819973541020 ) ) ;
#46059=CARTESIAN_POINT ( 'NONE',  ( 63.41538649190439969, 1.369535599030039963, -68.77214795431979155 ) ) ;
#46122=CARTESIAN_POINT ( 'NONE',  ( 64.97290478796050195, 0.8840451408750739093, -60.55014093144429665 ) ) ;
#46128=CARTESIAN_POINT ( 'NONE',  ( 64.74712693194929614, 0.8966068345641480253, -60.69721413447479819 ) ) ;
#46142=CARTESIAN_POINT ( 'NONE',  ( 64.74712693194929614, 0.8966068345641440285, -60.69721413447479819 ) ) ;
#46151=CARTESIAN_POINT ( 'NONE',  ( 73.00772670898579975, 1.265401080857980087, -62.43968814002079881 ) ) ;
#46159=CARTESIAN_POINT ( 'NONE',  ( 64.84562941585738827, 1.096044978595170027, -70.62064874955129312 ) ) ;
#46160=VERTEX_POINT ( 'NONE', #10331 ) ;
#46162=DIRECTION ( 'NONE',  ( 0.000000000000000000, 0.000000000000000000, 1.000000000000000000 ) ) ;
#46173=EDGE_CURVE ( 'NONE', #23933, #16762, #42301, .T. ) ;
#46188=CIRCLE ( 'NONE', #36139, 0.5000000000000004441 ) ;
#46214=CARTESIAN_POINT ( 'NONE',  ( 63.40602163964879878, 1.051323308921499944, -69.33345902934181026 ) ) ;
#46219=CARTESIAN_POINT ( 'NONE',  ( 72.97999464611700660, 0.9170823515334800557, -62.11176382508629956 ) ) ;
#46223=ORIENTED_EDGE ( 'NONE', *, *, #23634, .T. ) ;
#46230=CARTESIAN_POINT ( 'NONE',  ( 63.44018392888030178, 1.383811055320669947, -68.52712657046359368 ) ) ;
#46247=DIRECTION ( 'NONE',  ( 0.000000000000000000, 0.000000000000000000, -1.000000000000000000 ) ) ;
#46268=EDGE_CURVE ( 'NONE', #24662, #23989, #13179, .T. ) ;
#46275=CARTESIAN_POINT ( 'NONE',  ( 63.54769155648281043, 1.017423949637539904, -61.78033243378509809 ) ) ;
#46278=DIRECTION ( 'NONE',  ( -1.000000000000000000, 0.000000000000000000, 0.000000000000000000 ) ) ;
#46307=CARTESIAN_POINT ( 'NONE',  ( 64.19260248505071331, 1.000485720979669813, -70.17481423849029909 ) ) ;
#46311=VERTEX_POINT ( 'NONE', #31245 ) ;
#46318=CARTESIAN_POINT ( 'NONE',  ( 63.52011431889719972, 1.391252479931859964, -68.77264296518760034 ) ) ;
#46321=LINE ( 'NONE', #50760, #17550 ) ;
#46325=EDGE_CURVE ( 'NONE', #41111, #6409, #28089, .T. ) ;
#46326=AXIS2_PLACEMENT_3D ( 'NONE', #33148, #32617, #939 ) ;
#46331=CARTESIAN_POINT ( 'NONE',  ( 71.34424925767550008, 1.265401080857980087, -70.52378931128949091 ) ) ;
#46354=CARTESIAN_POINT ( 'NONE',  ( 64.93393739769740591, 11.38381105532059934, -69.34999999999999432 ) ) ;
#46374=AXIS2_PLACEMENT_3D ( 'NONE', #8661, #37474, #24616 ) ;
#46410=CARTESIAN_POINT ( 'NONE',  ( 72.72759757326660690, 1.395196698723390138, -68.83033655198650536 ) ) ;
#46412=CARTESIAN_POINT ( 'NONE',  ( 72.78816252330430814, 1.385888765344509999, -62.64792042614379852 ) ) ;
#46419=CARTESIAN_POINT ( 'NONE',  ( 65.00323391584400667, 1.328073773609210084, -70.46779242537471077 ) ) ;
#46477=CARTESIAN_POINT ( 'NONE',  ( 71.09473187122610227, 1.382830464309369844, -60.94559068149789738 ) ) ;
#46503=CARTESIAN_POINT ( 'NONE',  ( 73.07318775143950518, 0.8986939045430389905, -69.05651959838648679 ) ) ;
#46521=CARTESIAN_POINT ( 'NONE',  ( 72.33393739769618946, 1.883811055320669947, -62.44999999999999574 ) ) ;
#46536=CARTESIAN_POINT ( 'NONE',  ( 63.86141673131270835, 1.061268603384970088, -61.43724097146670005 ) ) ;
#46567=CARTESIAN_POINT ( 'NONE',  ( 64.26458081267169575, 1.017362664354699797, -70.23651179247990228 ) ) ;
#46570=CARTESIAN_POINT ( 'NONE',  ( 63.93393739769619089, 10.88381105532070059, -68.84999999999999432 ) ) ;
#46575=CARTESIAN_POINT ( 'NONE',  ( 71.83679462228410273, 0.9486745332793860008, -70.37196876996070216 ) ) ;
#46579=CARTESIAN_POINT ( 'NONE',  ( 63.50659274611129490, 1.388313565858570131, -68.83005089568669632 ) ) ;
#46589=CARTESIAN_POINT ( 'NONE',  ( 71.23750802749680133, 1.369613126987639928, -70.37582656035600337 ) ) ;
#46590=CIRCLE ( 'NONE', #13159, 0.5000000000000004441 ) ;
#46632=CARTESIAN_POINT ( 'NONE',  ( 71.01106396815980304, 1.383811055320669947, -70.34375346881599000 ) ) ;
#46639=CARTESIAN_POINT ( 'NONE',  ( 64.82191989009379540, 0.9958340104639701318, -60.65579263520140074 ) ) ;
#46662=CARTESIAN_POINT ( 'NONE',  ( 64.69570918563060502, 1.132579237369250036, -60.79187696645490036 ) ) ;
#46668=CARTESIAN_POINT ( 'NONE',  ( 72.81333620972418430, 1.370853092582090094, -68.86908206983169123 ) ) ;
#46670=CARTESIAN_POINT ( 'NONE',  ( 72.77636315587029969, 1.387131204727290124, -62.61203846038919352 ) ) ;
#46678=CARTESIAN_POINT ( 'NONE',  ( 64.87536163491149921, 1.372372808637209785, -70.31281467067098845 ) ) ;
#46686=ORIENTED_EDGE ( 'NONE', *, *, #20561, .F. ) ;
#46698=ORIENTED_EDGE ( 'NONE', *, *, #46173, .F. ) ;
#46736=CARTESIAN_POINT ( 'NONE',  ( 71.36799767121769378, 0.8859637708054489691, -60.59611492242089525 ) ) ;
#46738=CARTESIAN_POINT ( 'NONE',  ( 72.70504696988909643, 1.400446703427080219, -62.40275391609110756 ) ) ;
#46743=ADVANCED_FACE ( 'NONE', ( #23951 ), #27528, .T. ) ;
#46771=EDGE_LOOP ( 'NONE', ( #47787, #2333, #40129, #20651 ) ) ;
#46776=DIRECTION ( 'NONE',  ( -1.000000000000000000, 0.000000000000000000, 0.000000000000000000 ) ) ;
#46791=CARTESIAN_POINT ( 'NONE',  ( 63.86404120422080410, 1.117797034538490220, -61.44141157926519980 ) ) ;
#46795=CARTESIAN_POINT ( 'NONE',  ( 73.20987945474540481, 1.101170701158060039, -68.76387392617688477 ) ) ;
#46801=ORIENTED_EDGE ( 'NONE', *, *, #22211, .F. ) ;
#46828=CARTESIAN_POINT ( 'NONE',  ( 64.89936453248850512, 1.399477666643410112, -70.22527192354300496 ) ) ;
#46836=CARTESIAN_POINT ( 'NONE',  ( 71.55691549992010891, 1.416242794300029972, -70.15496246767990840 ) ) ;
#46850=CARTESIAN_POINT ( 'NONE',  ( 71.44595490529880522, 0.9958340104639701318, -70.64420736479868879 ) ) ;
#46858=ORIENTED_EDGE ( 'NONE', *, *, #21292, .F. ) ;
#46896=CARTESIAN_POINT ( 'NONE',  ( 65.01178944337650023, 1.369535599030039963, -60.93144909420819744 ) ) ;
#46929=CARTESIAN_POINT ( 'NONE',  ( 73.06536971133249381, 1.096932441169210071, -62.29998885741579784 ) ) ;
#46946=CARTESIAN_POINT ( 'NONE',  ( 71.33393739775299025, 1.883811055181200178, -62.44999999988809236 ) ) ;
#46948=AXIS2_PLACEMENT_3D ( 'NONE', #7319, #11253, #51081 ) ;
#46959=ORIENTED_EDGE ( 'NONE', *, *, #26755, .T. ) ;
#46976=CARTESIAN_POINT ( 'NONE',  ( 65.13393739769620083, 1.383811055320669947, -65.65000000000000568 ) ) ;
#46996=CARTESIAN_POINT ( 'NONE',  ( 71.42298070439039748, 0.9242073871622918935, -60.63177898966700496 ) ) ;
#46999=CARTESIAN_POINT ( 'NONE',  ( 72.29385319554739908, 1.443559558797639975, -61.62614672395329762 ) ) ;
#47010=CARTESIAN_POINT ( 'NONE',  ( 63.53329261246669546, 1.393731187554809958, -62.48946499964799983 ) ) ;
#47014=CARTESIAN_POINT ( 'NONE',  ( 68.13393739769620083, 0.8838110553206759423, -65.65000000000000568 ) ) ;
#47024=AXIS2_PLACEMENT_3D ( 'NONE', #19182, #35163, #40133 ) ;
#47053=CARTESIAN_POINT ( 'NONE',  ( 63.86577392472210590, 1.451792515613489876, -61.80022504404329453 ) ) ;
#47056=AXIS2_PLACEMENT_3D ( 'NONE', #16532, #16027, #15768 ) ;
#47058=CARTESIAN_POINT ( 'NONE',  ( 73.11081010690790549, 1.190292248953970011, -68.82164347790129000 ) ) ;
#47073=CARTESIAN_POINT ( 'NONE',  ( 64.93393739769619799, 10.88381105532070059, -61.94999999999999574 ) ) ;
#47092=CARTESIAN_POINT ( 'NONE',  ( 71.95736036617928733, 1.400155911913200102, -70.02962653331499610 ) ) ;
#47108=CARTESIAN_POINT ( 'NONE',  ( 71.31509885739851029, 1.369976237678190101, -70.34495568738229565 ) ) ;
#47127=VECTOR ( 'NONE', #46047, 1000.000000000000000 ) ;
#47138=CARTESIAN_POINT ( 'NONE',  ( 72.18749078828946608, 11.23736444591397543, -62.44999999999999574 ) ) ;
#47152=EDGE_CURVE ( 'NONE', #41163, #37879, #29250, .T. ) ;
#47153=CARTESIAN_POINT ( 'NONE',  ( 64.90098062201279561, 0.9219904752505979628, -60.59541050710320320 ) ) ;
#47186=CARTESIAN_POINT ( 'NONE',  ( 73.10855093309899644, 0.8936201581567889685, -62.29538467389520662 ) ) ;
#47227=FACE_OUTER_BOUND ( 'NONE', #18545, .T. ) ;
#47234=CARTESIAN_POINT ( 'NONE',  ( 63.23867883281550206, 0.9065823421260970072, -62.18054194328749418 ) ) ;
#47248=CARTESIAN_POINT ( 'NONE',  ( 71.03155062328740144, 1.383928098097870096, -60.96256459357869772 ) ) ;
#47250=CARTESIAN_POINT ( 'NONE',  ( 72.58908507643239716, 1.266076987107020102, -61.73296247052759611 ) ) ;
#47273=( NAMED_UNIT ( * ) SI_UNIT ( $, .STERADIAN. ) SOLID_ANGLE_UNIT ( ) );
#47287=ORIENTED_EDGE ( 'NONE', *, *, #44030, .F. ) ;
#47301=CARTESIAN_POINT ( 'NONE',  ( 64.21673630462969129, 0.9952277120692989421, -61.10412195540050107 ) ) ;
#47311=CARTESIAN_POINT ( 'NONE',  ( 63.39852073786919817, 1.308983041454369944, -62.28353782724239807 ) ) ;
#47315=CARTESIAN_POINT ( 'NONE',  ( 72.82769086651219936, 1.383811055320669947, -68.52712657046359368 ) ) ;
#47361=CARTESIAN_POINT ( 'NONE',  ( 71.46697330897291067, 1.186614556332910020, -70.53308468150621025 ) ) ;
#47372=ORIENTED_EDGE ( 'NONE', *, *, #12349, .F. ) ;
#47383=CARTESIAN_POINT ( 'NONE',  ( 63.00666467042349694, 0.8838110553206759423, -62.53374032209040223 ) ) ;
#47392=FACE_OUTER_BOUND ( 'NONE', #11654, .T. ) ;
#47409=CARTESIAN_POINT ( 'NONE',  ( 65.03036676789569981, 1.369613126987639928, -60.92417343964400089 ) ) ;
#47418=CARTESIAN_POINT ( 'NONE',  ( 72.25791598168270014, 1.028300555801489935, -70.00885842708049722 ) ) ;
#47423=ORIENTED_EDGE ( 'NONE', *, *, #34960, .T. ) ;
#47440=CARTESIAN_POINT ( 'NONE',  ( 72.96845534527879806, 1.188860127980290171, -62.23803121388370130 ) ) ;
#47444=ORIENTED_EDGE ( 'NONE', *, *, #11486, .F. ) ;
#47481=CARTESIAN_POINT ( 'NONE',  ( 63.03407832914061260, 0.8840451408750739093, -68.81103260973570457 ) ) ;
#47494=CARTESIAN_POINT ( 'NONE',  ( 68.13393739769624347, 0.8838110553206759423, -71.65000000000000568 ) ) ;
#47499=CARTESIAN_POINT ( 'NONE',  ( 71.34267188602969156, 0.8850831926798630178, -60.57999765399179637 ) ) ;
#47501=CARTESIAN_POINT ( 'NONE',  ( 72.61057233489319174, 1.185470598955660204, -61.69804660143999797 ) ) ;
#47519=CARTESIAN_POINT ( 'NONE',  ( 71.33393739769628894, 10.88381105532070059, -61.44999999999999574 ) ) ;
#47545=CARTESIAN_POINT ( 'NONE',  ( 63.17872741171709805, 1.188582381068110205, -62.44003653085279382 ) ) ;
#47562=CARTESIAN_POINT ( 'NONE',  ( 72.91520214831270152, 1.373356196620449943, -68.60593141770759473 ) ) ;
#47581=CARTESIAN_POINT ( 'NONE',  ( 64.93393739769619799, 11.23736444591397543, -69.70355339059327093 ) ) ;
#47596=CARTESIAN_POINT ( 'NONE',  ( 71.71411752565128950, 0.9618757110835569613, -70.46515124295960675 ) ) ;
#47611=CARTESIAN_POINT ( 'NONE',  ( 71.52584472686049821, 1.187931651339009909, -70.49707891402350413 ) ) ;
#47635=CARTESIAN_POINT ( 'NONE',  ( 64.93393739769619799, 10.88381105532070059, -69.34999999999999432 ) ) ;
#47636=ORIENTED_EDGE ( 'NONE', *, *, #6862, .F. ) ;
#47665=DIRECTION ( 'NONE',  ( 0.5765530599821108160, 0.1342272854595029929, -0.8059588108975778153 ) ) ;
#47675=EDGE_LOOP ( 'NONE', ( #2890, #16352, #23937, #8025 ) ) ;
#47685=EDGE_LOOP ( 'NONE', ( #20148, #20004, #40207, #2436 ) ) ;
#47690=CARTESIAN_POINT ( 'NONE',  ( 73.04558532727548936, 1.003508719580009867, -62.21555175845400498 ) ) ;
#47696=EDGE_CURVE ( 'NONE', #28243, #11637, #24344, .T. ) ;
#47697=CARTESIAN_POINT ( 'NONE',  ( 64.91441195039600132, 1.390806392144110060, -70.26251807531768634 ) ) ;
#47731=CARTESIAN_POINT ( 'NONE',  ( 63.09723768121719445, 1.097895768572089814, -68.83057487531520735 ) ) ;
#47753=CARTESIAN_POINT ( 'NONE',  ( 71.46697330897291067, 1.186614556332910020, -60.76691531849380112 ) ) ;
#47755=CARTESIAN_POINT ( 'NONE',  ( 72.62016429705300880, 1.099201050715839845, -61.67264653093729976 ) ) ;
#47763=ADVANCED_FACE ( 'NONE', ( #25133 ), #10257, .T. ) ;
#47777=CARTESIAN_POINT ( 'NONE',  ( 63.00666467042349694, 0.8838110553206759423, -62.53374032209040223 ) ) ;
#47784=CARTESIAN_POINT ( 'NONE',  ( 64.89936453248850512, 1.399477666643410112, -70.22527192354300496 ) ) ;
#47787=ORIENTED_EDGE ( 'NONE', *, *, #48280, .T. ) ;
#47799=CARTESIAN_POINT ( 'NONE',  ( 63.48441347673288959, 1.386342629514219826, -62.63353618948930546 ) ) ;
#47816=CARTESIAN_POINT ( 'NONE',  ( 73.14840136429539541, 1.194703186106690129, -68.75325824359919125 ) ) ;
#47847=EDGE_CURVE ( 'NONE', #49612, #11422, #26746, .T. ) ;
#47850=CARTESIAN_POINT ( 'NONE',  ( 72.40383359117168993, 1.117797034538490220, -69.85858842073480446 ) ) ;
#47852=EDGE_CURVE ( 'NONE', #2182, #19450, #36246, .T. ) ;
#47856=( NAMED_UNIT ( * ) SI_UNIT ( $, .STERADIAN. ) SOLID_ANGLE_UNIT ( ) );
#47869=CARTESIAN_POINT ( 'NONE',  ( 71.33379467969419352, 1.389468113695450091, -70.26995969721829738 ) ) ;
#47882=CARTESIAN_POINT ( 'NONE',  ( 68.13393739769620083, 0.8838110553206759423, -65.65000000000000568 ) ) ;
#47927=DIRECTION ( 'NONE',  ( -0.2267461507313160984, 0.9739538916850897232, -3.885780586188046377E-13 ) ) ;
#47947=CARTESIAN_POINT ( 'NONE',  ( 72.77520546617009245, 1.386446979194299933, -62.50785065198430601 ) ) ;
#47966=EDGE_CURVE ( 'NONE', #32793, #19147, #29386, .T. ) ;
#47982=EDGE_CURVE ( 'NONE', #25965, #4949, #8392, .T. ) ;
#47988=CARTESIAN_POINT ( 'NONE',  ( 63.11172336169240538, 1.097085799869280009, -68.85468201266050414 ) ) ;
#47990=LINE ( 'NONE', #44048, #6373 ) ;
#47999=CARTESIAN_POINT ( 'NONE',  ( 71.28186865452410359, 1.191644800533229853, -70.64005307315129301 ) ) ;
#48006=FACE_OUTER_BOUND ( 'NONE', #3723, .T. ) ;
#48008=CARTESIAN_POINT ( 'NONE',  ( 71.58179376171669617, 0.9036513197889520788, -60.73950228677190211 ) ) ;
#48011=CARTESIAN_POINT ( 'NONE',  ( 72.18916782744800287, 1.409272994606969975, -61.45923610184129871 ) ) ;
#48045=ORIENTED_EDGE ( 'NONE', *, *, #25486, .T. ) ;
#48056=CARTESIAN_POINT ( 'NONE',  ( 63.20675433611359750, 1.270877794983130027, -62.54449628245689752 ) ) ;
#48080=CIRCLE ( 'NONE', #47056, 0.5000000000000045519 ) ;
#48093=VECTOR ( 'NONE', #17667, 1000.000000000000000 ) ;
#48102=CIRCLE ( 'NONE', #25492, 0.9999999999999964473 ) ;
#48106=CARTESIAN_POINT ( 'NONE',  ( 72.45273174173409814, 1.404167647216130188, -69.55372334320209404 ) ) ;
#48112=CARTESIAN_POINT ( 'NONE',  ( 63.83267354985670750, 1.033012681683380007, -69.83402047387519929 ) ) ;
#48114=CARTESIAN_POINT ( 'NONE',  ( 71.33393739769650210, 1.396834109478129804, -61.06337307536569625 ) ) ;
#48117=CARTESIAN_POINT ( 'NONE',  ( 64.64722926691220550, 0.9479899806831150189, -60.76708149872590070 ) ) ;
#48136=ORIENTED_EDGE ( 'NONE', *, *, #50771, .T. ) ;
#48172=CARTESIAN_POINT ( 'NONE',  ( 64.93393739769619799, 11.38381105532070059, -69.34999999999999432 ) ) ;
#48197=CARTESIAN_POINT ( 'NONE',  ( 64.93393739769578588, 0.9098571636355720083, -70.12325384926869276 ) ) ;
#48206=CARTESIAN_POINT ( 'NONE',  ( 71.33393739769650210, 1.396834109478129804, -70.23662692463440749 ) ) ;
#48233=CARTESIAN_POINT ( 'NONE',  ( 69.73393739769620936, 10.88381105532070059, -61.94999999999999574 ) ) ;
#48234=AXIS2_PLACEMENT_3D ( 'NONE', #37539, #14216, #10025 ) ;
#48240=CARTESIAN_POINT ( 'NONE',  ( 63.14388432454488509, 1.191644800533210091, -68.79793125682789423 ) ) ;
#48252=CARTESIAN_POINT ( 'NONE',  ( 71.24781132387310834, 1.101170701158060039, -70.72594205704909598 ) ) ;
#48256=DIRECTION ( 'NONE',  ( 0.000000000000000000, -1.000000000000000000, 0.000000000000000000 ) ) ;
#48261=CARTESIAN_POINT ( 'NONE',  ( 71.40428550048659417, 1.263903724274369811, -60.80800729848100161 ) ) ;
#48263=CARTESIAN_POINT ( 'NONE',  ( 71.86947670220010309, 0.9561296872641509292, -60.95384405884309587 ) ) ;
#48266=CARTESIAN_POINT ( 'NONE',  ( 64.90098062201279561, 0.9219904752505849732, -70.70458949289690054 ) ) ;
#48280=EDGE_CURVE ( 'NONE', #38817, #36774, #50221, .T. ) ;
#48308=CARTESIAN_POINT ( 'NONE',  ( 63.07039345372018602, 1.099973129953850215, -62.51484271732719833 ) ) ;
#48313=DIRECTION ( 'NONE',  ( 0.000000000000000000, -1.000000000000000000, 0.000000000000000000 ) ) ;
#48316=EDGE_CURVE ( 'NONE', #16787, #9287, #18412, .T. ) ;
#48317=CARTESIAN_POINT ( 'NONE',  ( 64.74203006853200293, 1.187931651339009909, -60.80292108597650014 ) ) ;
#48320=CARTESIAN_POINT ( 'NONE',  ( 68.13393739769620083, 1.383811055320669947, -65.65000000000000568 ) ) ;
#48327=ORIENTED_EDGE ( 'NONE', *, *, #11436, .F. ) ;
#48347=DIRECTION ( 'NONE',  ( -1.000000000000000000, 0.000000000000000000, 0.000000000000000000 ) ) ;
#48361=CARTESIAN_POINT ( 'NONE',  ( 72.36591324851900708, 1.277721627657099956, -69.81671480277449859 ) ) ;
#48368=CARTESIAN_POINT ( 'NONE',  ( 64.39815381769149383, 0.9561815866734399982, -70.34594416269000305 ) ) ;
#48420=AXIS2_PLACEMENT_3D ( 'NONE', #34847, #11017, #43502 ) ;
#48458=AXIS2_PLACEMENT_3D ( 'NONE', #50447, #14534, #26571 ) ;
#48466=CARTESIAN_POINT ( 'NONE',  ( 63.46757340380580814, 1.384887413063070172, -62.68544474927200127 ) ) ;
#48485=PRODUCT_DEFINITION ( 'UNKNOWN', '', #13492, #16384 ) ;
#48494=CARTESIAN_POINT ( 'NONE',  ( 63.39699138880700247, 1.369885150286779929, -68.72489565442110404 ) ) ;
#48508=CARTESIAN_POINT ( 'NONE',  ( 71.37757697660960332, 1.096291039689149871, -70.64841943982850125 ) ) ;
#48509=FACE_OUTER_BOUND ( 'NONE', #30173, .T. ) ;
#48517=CARTESIAN_POINT ( 'NONE',  ( 71.44853510719140388, 1.186515949276290227, -60.75583815301620660 ) ) ;
#48519=CARTESIAN_POINT ( 'NONE',  ( 71.68799458498580179, 0.9577391936072879863, -60.81570214284359821 ) ) ;
#48521=CARTESIAN_POINT ( 'NONE',  ( 64.89987712417480736, 0.8859637708054489691, -70.70388507757908769 ) ) ;
#48524=CARTESIAN_POINT ( 'NONE',  ( 71.83406239765474766, 11.38381103969560471, -61.94987500004191361 ) ) ;
#48570=CARTESIAN_POINT ( 'NONE',  ( 63.02699984107479025, 0.9952464559119579279, -62.51628753338329858 ) ) ;
#48577=CARTESIAN_POINT ( 'NONE',  ( 72.72056432233058842, 1.396834109478129804, -62.44999999999999574 ) ) ;
#48585=VERTEX_POINT ( 'NONE', #30457 ) ;
#48602=ORIENTED_EDGE ( 'NONE', *, *, #42489, .F. ) ;
#48627=CARTESIAN_POINT ( 'NONE',  ( 72.43509047223609798, 1.031856533264720266, -69.83351529264139401 ) ) ;
#48634=B_SPLINE_CURVE_WITH_KNOTS ( 'NONE', 3,
 ( #4340, #35280, #31841, #23459, #48368, #51535, #15632, #20056, #11705, #27667, #31330, #48112, #12211, #27153, #43161, #23204, #39224, #43669, #3319, #23721 ),
 .UNSPECIFIED., .F., .F.,
 ( 4, 2, 2, 2, 2, 2, 2, 2, 2, 4 ),
 ( -1.826162956740689847, -1.707995156971769957, -1.458514671262659990, -1.209832958840709960, -1.027216663166639954, -0.9130814783703469217, -0.6848111087777599693, -0.4130647882495273038, -0.1614699006445539098, 0.000000000000000000 ),
 .UNSPECIFIED. ) ;
#48640=CARTESIAN_POINT ( 'NONE',  ( 63.95563233927359192, 1.117804454683279936, -61.34981482092570104 ) ) ;
#48652=ORIENTED_EDGE ( 'NONE', *, *, #2718, .F. ) ;
#48669=ORIENTED_EDGE ( 'NONE', *, *, #48869, .T. ) ;
#48672=CARTESIAN_POINT ( 'NONE',  ( 64.97290478796050195, 0.8840451408750739093, -70.74985906855570761 ) ) ;
#48685=CARTESIAN_POINT ( 'NONE',  ( 64.03708764054000824, 1.112169578473010123, -70.02730617886231812 ) ) ;
#48701=CARTESIAN_POINT ( 'NONE',  ( 64.93393739769619799, 10.88381105532070059, -62.44999999999999574 ) ) ;
#48703=ORIENTED_EDGE ( 'NONE', *, *, #23634, .F. ) ;
#48728=CARTESIAN_POINT ( 'NONE',  ( 72.54418616719020463, 1.434949534324099885, -69.27291511353429598 ) ) ;
#48730=DIRECTION ( 'NONE',  ( 0.8545454545454611583, 0.000000000000000000, -0.5193766129849238800 ) ) ;
#48760=CARTESIAN_POINT ( 'NONE',  ( 63.49388541862201407, 1.387412027389909985, -68.69511434646409498 ) ) ;
#48772=CARTESIAN_POINT ( 'NONE',  ( 71.36799767121769378, 0.8859637708054489691, -70.70388507757908769 ) ) ;
#48778=CARTESIAN_POINT ( 'NONE',  ( 73.05322604375929529, 1.097545367735389910, -69.01875481685119951 ) ) ;
#48780=CARTESIAN_POINT ( 'NONE',  ( 72.91520214831270152, 1.373356196620459935, -62.69406858229250901 ) ) ;
#48782=CARTESIAN_POINT ( 'NONE',  ( 71.15040120820690106, 1.386342629514219826, -61.00047607903670155 ) ) ;
#48784=CARTESIAN_POINT ( 'NONE',  ( 72.18870199502219975, 1.048861872235970161, -61.22695438956509406 ) ) ;
#48785=DIRECTION ( 'NONE',  ( -1.000000000000000000, 0.000000000000000000, 0.000000000000000000 ) ) ;
#48786=CARTESIAN_POINT ( 'NONE',  ( 64.89029781878299730, 1.096291039689149871, -70.64841943982850125 ) ) ;
#48788=EDGE_LOOP ( 'NONE', ( #28334, #8729, #17850, #9076 ) ) ;
#48796=AXIS2_PLACEMENT_3D ( 'NONE', #23087, #10288, #22829 ) ;
#48831=CARTESIAN_POINT ( 'NONE',  ( 63.15932386229340523, 0.8936201581567979613, -62.29538467389520662 ) ) ;
#48836=CARTESIAN_POINT ( 'NONE',  ( 71.33393739769650210, 1.396834109478129804, -61.06337307536569625 ) ) ;
#48861=ORIENTED_EDGE ( 'NONE', *, *, #26587, .F. ) ;
#48865=EDGE_CURVE ( 'NONE', #16787, #49612, #33298, .T. ) ;
#48869=EDGE_CURVE ( 'NONE', #50553, #34442, #25125, .T. ) ;
#48891=CARTESIAN_POINT ( 'NONE',  ( 72.25791598168270014, 1.028300555801489935, -70.00885842708049722 ) ) ;
#48896=CARTESIAN_POINT ( 'NONE',  ( 72.98949351566130872, 0.9150552061895679268, -69.17495778280330399 ) ) ;
#48901=CIRCLE ( 'NONE', #32968, 0.9999999999999964473 ) ;
#48909=CARTESIAN_POINT ( 'NONE',  ( 64.18198399913551100, 1.185470598955730148, -61.17336506280369690 ) ) ;
#48910=EDGE_LOOP ( 'NONE', ( #50572, #20539, #22197, #15649 ) ) ;
#48952=CARTESIAN_POINT ( 'NONE',  ( 64.14219431282829476, 1.270921660756489935, -70.04197312588519253 ) ) ;
#48970=VERTEX_POINT ( 'NONE', #45372 ) ;
#48981=B_SPLINE_SURFACE_WITH_KNOTS ( 'NONE', 3, 3, ( 
 ( #22943, #51269, #34489, #15366, #14585, #26620, #38962, #42637, #2798 ),
 ( #30808, #31321, #51523, #39210, #35535, #18515, #11181, #11443, #3575 ),
 ( #50494, #22689, #35270, #34742, #15624, #3055, #19025, #47596, #35001 ),
 ( #46836, #18770, #2536, #30551, #51009, #7502, #31575, #11696, #46575 ),
 ( #10922, #27401, #27658, #43402, #26886, #19289, #23450, #43659, #39475 ),
 ( #31066, #38708, #10664, #7764, #42896, #38436, #50749, #27147, #14845 ),
 ( #6991, #15105, #47092, #43151, #7246, #23194, #3311, #20047, #32860 ),
 ( #11956, #40240, #147, #35792, #4853, #40491, #44429, #8532, #48891 ),
 ( #32342, #16639, #8263, #24478, #656, #28164, #36815, #23963, #3828 ),
 ( #12994, #44949, #920, #24741, #48361, #16915, #47850, #20819, #28944 ),
 ( #32600, #44168, #4584, #20555, #31833, #23712, #39725, #36552, #48627 ),
 ( #12727, #39984, #400, #19802, #28682, #4076, #4332, #44685, #51774 ),
 ( #24216, #12205, #48106, #20300, #8789, #16125, #15879, #40752, #32086 ),
 ( #36290, #27913, #36039, #16386, #43914, #8009, #12456, #28426, #1961 ),
 ( #1181, #13511, #49414, #33395, #29465, #41786, #42053, #37083, #45470 ),
 ( #17429, #26042, #37864, #37342, #37589, #14013, #13760, #21338, #1443 ),
 ( #22112, #9828, #6155, #41015, #33655, #17937, #38123, #29973, #21080 ),
 ( #5893, #5381, #2218, #9570, #25524, #18196, #41528, #21857, #5645 ),
 ( #24997, #17176, #21591, #45991, #34160, #50175, #33128, #30239, #1702 ),
 ( #14273, #49922, #17684, #33907, #10084, #9049, #5127, #49671, #29718 ) ),
 .UNSPECIFIED., .F., .F., .F.,
 ( 4, 2, 2, 2, 2, 2, 2, 2, 2, 4 ),
 ( 4, 1, 1, 1, 1, 1, 4 ),
 ( -1.826192301619919967, -1.664708266407020076, -1.413116924488160064, -1.141370188512450090, -0.9130961508099589841, -0.7989591319587140417, -0.6163399017967220450, -0.3681920442832050111, -0.1161770321783029969, 0.000000000000000000 ),
 ( 0.000000000000000000, 0.1666666666666670182, 0.3333333333333329818, 0.5000000000000000000, 0.6666666666666670737, 0.8333333333333330373, 1.000000000000000000 ),
 .UNSPECIFIED. ) ;
#48982=DIRECTION ( 'NONE',  ( 0.000000000000000000, 0.000000000000000000, -1.000000000000000000 ) ) ;
#49013=CIRCLE ( 'NONE', #3813, 0.9999999999999964473 ) ;
#49037=CARTESIAN_POINT ( 'NONE',  ( 71.36689417337970553, 0.9219904752505979628, -70.70458949289690054 ) ) ;
#49045=CARTESIAN_POINT ( 'NONE',  ( 72.86255183691179127, 1.369664981662529923, -68.74641178933899255 ) ) ;
#49048=CARTESIAN_POINT ( 'NONE',  ( 72.82769086651219936, 1.383811055320669947, -62.77287342953649585 ) ) ;
#49050=CARTESIAN_POINT ( 'NONE',  ( 71.35346284499661351, 1.390806392144110060, -61.03748192468230371 ) ) ;
#49052=CARTESIAN_POINT ( 'NONE',  ( 72.23784989528050460, 1.054781932184780002, -61.27250974618609547 ) ) ;
#49054=CARTESIAN_POINT ( 'NONE',  ( 65.04142308672740569, 1.102581332775290024, -70.73820378408520071 ) ) ;
#49083=DIRECTION ( 'NONE',  ( 1.000000000000000000, 0.000000000000000000, 0.000000000000000000 ) ) ;
#49100=CARTESIAN_POINT ( 'NONE',  ( 63.47152504824990160, 1.384378348444510243, -62.56683295884919715 ) ) ;
#49130=DIRECTION ( 'NONE',  ( 0.000000000000000000, 1.000000000000000000, 0.000000000000000000 ) ) ;
#49141=CARTESIAN_POINT ( 'NONE',  ( 72.76779797359338886, 1.388189907116970101, -62.58632377286669879 ) ) ;
#49171=CARTESIAN_POINT ( 'NONE',  ( 64.21673630462969129, 0.9952277120692980539, -61.10412195540050107 ) ) ;
#49206=CARTESIAN_POINT ( 'NONE',  ( 72.79984470539690733, 0.9644290104360989657, -61.87674839326469822 ) ) ;
#49209=CARTESIAN_POINT ( 'NONE',  ( 63.87903507333619757, 1.407740274733980002, -69.63435796713869763 ) ) ;
#49252=CARTESIAN_POINT ( 'NONE',  ( 72.62341919120400746, 1.419970371292329947, -69.11014492780159912 ) ) ;
#49259=ORIENTED_EDGE ( 'NONE', *, *, #50754, .F. ) ;
#49261=AXIS2_PLACEMENT_3D ( 'NONE', #15922, #31878, #43955 ) ;
#49267=ORIENTED_EDGE ( 'NONE', *, *, #47847, .T. ) ;
#49277=CARTESIAN_POINT ( 'NONE',  ( 65.19851456808879675, 1.374300485541529948, -60.86138005882520474 ) ) ;
#49283=CARTESIAN_POINT ( 'NONE',  ( 64.97290478796060142, 0.8840451408750739093, -60.55014093144429665 ) ) ;
#49288=EDGE_CURVE ( 'NONE', #41228, #49949, #31001, .T. ) ;
#49299=CARTESIAN_POINT ( 'NONE',  ( 71.23034918703520191, 1.369664981662519931, -70.37861443921559612 ) ) ;
#49305=CARTESIAN_POINT ( 'NONE',  ( 73.10458614724748827, 1.096044978595170027, -68.93830798183888930 ) ) ;
#49308=CARTESIAN_POINT ( 'NONE',  ( 73.25400818986750551, 0.9960089569207349891, -62.53811752243721145 ) ) ;
#49310=CARTESIAN_POINT ( 'NONE',  ( 71.31398829338289147, 1.388313565858570131, -61.02265534841509975 ) ) ;
#49312=CARTESIAN_POINT ( 'NONE',  ( 72.08523627823790036, 1.342503070345590022, -61.28987608900740014 ) ) ;
#49315=CARTESIAN_POINT ( 'NONE',  ( 64.78158399514489929, 0.9281439705311369526, -70.62613840402418930 ) ) ;
#49324=ORIENTED_EDGE ( 'NONE', *, *, #26587, .T. ) ;
#49355=CARTESIAN_POINT ( 'NONE',  ( 63.22191407479270708, 1.186701509386340003, -62.36552507365149722 ) ) ;
#49366=CARTESIAN_POINT ( 'NONE',  ( 63.46802213033249274, 0.9644268476137619617, -69.42324179401759920 ) ) ;
#49378=VERTEX_POINT ( 'NONE', #44144 ) ;
#49387=CARTESIAN_POINT ( 'NONE',  ( 64.71095929546520154, 1.416242794300709873, -61.14503753232310146 ) ) ;
#49403=VECTOR ( 'NONE', #25241, 1000.000000000000000 ) ;
#49414=CARTESIAN_POINT ( 'NONE',  ( 72.60355388137550392, 1.390572245144360064, -69.33358376010779978 ) ) ;
#49426=CARTESIAN_POINT ( 'NONE',  ( 64.21689986822309493, 1.266076987107070062, -61.19485232126449858 ) ) ;
#49440=CIRCLE ( 'NONE', #1730, 0.5000000000000004441 ) ;
#49467=CARTESIAN_POINT ( 'NONE',  ( 63.65233837787889826, 1.010052234904240009, -69.64061050479490689 ) ) ;
#49490=CARTESIAN_POINT ( 'NONE',  ( 65.27736602627911111, 1.383811055320669947, -60.94999999999999574 ) ) ;
#49496=CARTESIAN_POINT ( 'NONE',  ( 72.73458218292580568, 1.393731187554809958, -68.81053500035210391 ) ) ;
#49534=CARTESIAN_POINT ( 'NONE',  ( 65.11099717020638877, 1.370937308141420230, -60.89332811547459556 ) ) ;
#49542=CARTESIAN_POINT ( 'NONE',  ( 64.89987712417470789, 0.8859637708054509675, -60.59611492242100184 ) ) ;
#49566=CARTESIAN_POINT ( 'NONE',  ( 72.94510729672219895, 1.263823323415670163, -68.97683676677020514 ) ) ;
#49569=CARTESIAN_POINT ( 'NONE',  ( 73.15787026839889506, 0.9945465939392541532, -62.38364600848370145 ) ) ;
#49575=ADVANCED_FACE ( 'NONE', ( #21210 ), #29329, .T. ) ;
#49577=CARTESIAN_POINT ( 'NONE',  ( 65.03937945068039994, 1.384708701328909886, -70.30837376962780638 ) ) ;
#49612=VERTEX_POINT ( 'NONE', #14141 ) ;
#49616=CARTESIAN_POINT ( 'NONE',  ( 63.21507766202849865, 1.186856010528209993, -62.37714938719420132 ) ) ;
#49625=CARTESIAN_POINT ( 'NONE',  ( 63.28787718588009881, 0.9170817191178719519, -69.18823203240749820 ) ) ;
#49640=ORIENTED_EDGE ( 'NONE', *, *, #7315, .T. ) ;
#49669=CARTESIAN_POINT ( 'NONE',  ( 73.13041444294920268, 0.8910129994591539093, -62.32805707658469885 ) ) ;
#49671=CARTESIAN_POINT ( 'NONE',  ( 73.01685589897030582, 0.9479899806831150189, -69.13670813078400101 ) ) ;
#49682=CARTESIAN_POINT ( 'NONE',  ( 64.65045080987439974, 1.231980527807049919, -60.89105423166650866 ) ) ;
#49720=CARTESIAN_POINT ( 'NONE',  ( 63.92533662763849378, 1.117797273082159926, -69.91988402493059596 ) ) ;
#49729=CARTESIAN_POINT ( 'NONE',  ( 63.40811083734029552, 1.369613126987639928, -68.75357062980060618 ) ) ;
#49732=DIRECTION ( 'NONE',  ( -0.7071067811865441310, 0.000000000000000000, 0.7071067811865510144 ) ) ;
#49745=CARTESIAN_POINT ( 'NONE',  ( 72.83393739769620367, 1.383811055320669947, -68.50657137141709541 ) ) ;
#49784=CARTESIAN_POINT ( 'NONE',  ( 65.27736602627911111, 1.383811055320669947, -60.94999999999999574 ) ) ;
#49806=CARTESIAN_POINT ( 'NONE',  ( 64.68608103367580497, 0.9036513197889520788, -60.73950228677190211 ) ) ;
#49813=CARTESIAN_POINT ( 'NONE',  ( 72.79231116732400153, 1.384708701328909886, -68.74455794701600553 ) ) ;
#49815=CARTESIAN_POINT ( 'NONE',  ( 68.13393739769620083, 1.530257664727400879, -61.30355339059330078 ) ) ;
#49816=CARTESIAN_POINT ( 'NONE',  ( 72.98500336837570046, 1.331842543267529821, -62.59469824041600816 ) ) ;
#49824=CARTESIAN_POINT ( 'NONE',  ( 64.81199447428100768, 0.8910129994591459157, -70.64647704525299332 ) ) ;
#49840=CIRCLE ( 'NONE', #45644, 5.499999999999998224 ) ;
#49862=CYLINDRICAL_SURFACE ( 'NONE', #40546, 5.999999999999998224 ) ;
#49868=CARTESIAN_POINT ( 'NONE',  ( 63.13973003289760300, 0.9958340104639651358, -62.33798249239750078 ) ) ;
#49876=CARTESIAN_POINT ( 'NONE',  ( 63.28485546126960770, 1.028860417577979858, -69.16957158642991033 ) ) ;
#49881=CARTESIAN_POINT ( 'NONE',  ( 72.84761368145599647, 1.149538111077639924, -62.00072402692669726 ) ) ;
#49884=ORIENTED_EDGE ( 'NONE', *, *, #9818, .F. ) ;
#49895=CARTESIAN_POINT ( 'NONE',  ( 63.99198253403570646, 1.457833794292699992, -61.64494777836840456 ) ) ;
#49903=EDGE_CURVE ( 'NONE', #16762, #6409, #21713, .T. ) ;
#49905=CARTESIAN_POINT ( 'NONE',  ( 73.15108049797990475, 0.8888742037077599356, -68.94068779328439689 ) ) ;
#49922=CARTESIAN_POINT ( 'NONE',  ( 72.75077066479440191, 1.389801772588449946, -68.87277968851719834 ) ) ;
#49926=CARTESIAN_POINT ( 'NONE',  ( 71.33393739770056641, 11.38381105531911075, -69.84999999999840270 ) ) ;
#49928=CARTESIAN_POINT ( 'NONE',  ( 65.09597585808549525, 1.387131204727280132, -70.29242575817399086 ) ) ;
#49937=CARTESIAN_POINT ( 'NONE',  ( 63.60379491233669569, 1.091560265417989894, -61.72337259268859810 ) ) ;
#49949=VERTEX_POINT ( 'NONE', #34498 ) ;
#49959=CARTESIAN_POINT ( 'NONE',  ( 72.83393739769620367, 1.383811055320669947, -62.79342862858290886 ) ) ;
#49972=CARTESIAN_POINT ( 'NONE',  ( 64.76690267173279381, 1.308988796301270074, -70.38513104616750127 ) ) ;
#49976=EDGE_CURVE ( 'NONE', #41163, #41111, #46321, .T. ) ;
#49982=CARTESIAN_POINT ( 'NONE',  ( 63.41989057163110743, 1.369544300367010026, -68.78354504031220529 ) ) ;
#49994=CARTESIAN_POINT ( 'NONE',  ( 64.43393739769619799, 11.38381105532070059, -62.44999999999999574 ) ) ;
#50013=CARTESIAN_POINT ( 'NONE',  ( 63.93393739769613404, 11.38381105532129922, -68.84999999999941167 ) ) ;
#50038=CARTESIAN_POINT ( 'NONE',  ( 65.05161336175049769, 1.196343736543249880, -60.62426770491639871 ) ) ;
#50045=CARTESIAN_POINT ( 'NONE',  ( 64.99525386628140211, 0.8838110553206740549, -60.53635606803790381 ) ) ;
#50059=CARTESIAN_POINT ( 'NONE',  ( 64.68925548900161004, 0.9369374701296400154, -60.73727483855509490 ) ) ;
#50067=CARTESIAN_POINT ( 'NONE',  ( 72.93868606741401095, 1.327097482837290121, -62.49054404195729973 ) ) ;
#50071=CARTESIAN_POINT ( 'NONE',  ( 71.34267188602959209, 0.8850831926798620186, -60.57999765399169689 ) ) ;
#50074=CARTESIAN_POINT ( 'NONE',  ( 64.95255690645950608, 1.266538207494809942, -70.53881316596870477 ) ) ;
#50128=EDGE_CURVE ( 'NONE', #8243, #38406, #15887, .T. ) ;
#50129=CARTESIAN_POINT ( 'NONE',  ( 63.40807272917960091, 0.9828896327562162138, -69.34788335338460286 ) ) ;
#50137=ORIENTED_EDGE ( 'NONE', *, *, #7315, .F. ) ;
#50145=CARTESIAN_POINT ( 'NONE',  ( 63.54027722212589424, 1.395196698723379924, -62.46966344801359838 ) ) ;
#50149=EDGE_CURVE ( 'NONE', #39508, #44049, #48634, .T. ) ;
#50159=( BOUNDED_SURFACE ( )  B_SPLINE_SURFACE ( 2, 2, ( 
 ( #21947, #2311, #26925 ),
 ( #37957, #18034, #50013 ),
 ( #46354, #6507, #26140 ) ),
 .UNSPECIFIED., .F., .F., .T. ) 
 B_SPLINE_SURFACE_WITH_KNOTS ( ( 3, 3 ),
 ( 3, 3 ),
 ( -7.280321556379879384E-13, 1.570796326795560027 ),
 ( -3.141592653588870299, -1.570796326795379949 ),
 .UNSPECIFIED. ) 
 GEOMETRIC_REPRESENTATION_ITEM ( )  RATIONAL_B_SPLINE_SURFACE ( (
 ( 1.000000000000000000, 0.7071067811870440645, 1.000000000000000000),
 ( 0.7071067811860539676, 0.5000000000000000000, 0.7071067811860539676),
 ( 1.000000000000000000, 0.7071067811870440645, 1.000000000000000000) ) ) 
 REPRESENTATION_ITEM ( '' )  SURFACE ( )  );
#50160=CARTESIAN_POINT ( 'NONE',  ( 73.13041444294910320, 0.8910129994591539093, -68.97194292341539779 ) ) ;
#50175=CARTESIAN_POINT ( 'NONE',  ( 72.97035904602149969, 1.134292167764390014, -69.12140099273041471 ) ) ;
#50194=CARTESIAN_POINT ( 'NONE',  ( 63.54511136546258854, 1.080095028449789885, -61.79280233996579597 ) ) ;
#50199=CARTESIAN_POINT ( 'NONE',  ( 65.01767771978660448, 0.8838110553206759423, -70.77727272727270247 ) ) ;
#50221=CIRCLE ( 'NONE', #3384, 0.5000000000000004441 ) ;
#50232=CARTESIAN_POINT ( 'NONE',  ( 64.86559958573539575, 1.367045641526589916, -70.32522074196269557 ) ) ;
#50242=CARTESIAN_POINT ( 'NONE',  ( 63.43166809737898859, 1.369719003397489976, -68.81308079741751271 ) ) ;
#50253=CARTESIAN_POINT ( 'NONE',  ( 71.19138260135351004, 1.383767307422960169, -70.32144070214289400 ) ) ;
#50268=ORIENTED_EDGE ( 'NONE', *, *, #5449, .T. ) ;
#50305=CARTESIAN_POINT ( 'NONE',  ( 65.17314292416639887, 1.382830464309369844, -60.94559068149789738 ) ) ;
#50312=CARTESIAN_POINT ( 'NONE',  ( 64.81199447428090821, 0.8910129994591539093, -60.65352295474699673 ) ) ;
#50332=CARTESIAN_POINT ( 'NONE',  ( 72.80537809983910336, 1.383767307422969939, -62.59255479634269648 ) ) ;
#50341=CARTESIAN_POINT ( 'NONE',  ( 64.82636581786128716, 1.096153228089730147, -70.60852099187108877 ) ) ;
#50372=TOROIDAL_SURFACE ( 'NONE', #38675, 5.500000000000000000, 0.5000000000000000000 ) ;
#50394=CARTESIAN_POINT ( 'NONE',  ( 63.59194260610701122, 1.176185264361309990, -69.52318026956261576 ) ) ;
#50397=CARTESIAN_POINT ( 'NONE',  ( 71.10413293483961183, 1.338092079250050137, -60.76305085381149951 ) ) ;
#50399=CARTESIAN_POINT ( 'NONE',  ( 72.94555459751978788, 0.9254890127240680275, -62.06507410682309711 ) ) ;
#50424=CARTESIAN_POINT ( 'NONE',  ( 73.16133767175020353, 0.8879664753683469414, -68.92499589875210120 ) ) ;
#50440=TOROIDAL_SURFACE ( 'NONE', #24438, 5.500000000000000000, 0.5000000000000000000 ) ;
#50442=CARTESIAN_POINT ( 'NONE',  ( 63.02029346573409185, 0.8838110553206759423, -62.51131646858519275 ) ) ;
#50447=CARTESIAN_POINT ( 'NONE',  ( 64.93393739769578588, 0.9098571636355720083, -61.17674615073129729 ) ) ;
#50454=CARTESIAN_POINT ( 'NONE',  ( 63.87812827450808584, 1.200157260841299811, -61.45760966837089967 ) ) ;
#50487=CARTESIAN_POINT ( 'NONE',  ( 64.64302830678678902, 0.9098571636355680115, -70.52991329011140920 ) ) ;
#50494=CARTESIAN_POINT ( 'NONE',  ( 71.42967573711919727, 1.404650034021559968, -70.20402782815220633 ) ) ;
#50496=DIRECTION ( 'NONE',  ( -0.7071067811865475727, 0.000000000000000000, -0.7071067811865475727 ) ) ;
#50499=CARTESIAN_POINT ( 'NONE',  ( 63.25085271618998917, 1.186614556332910020, -68.98303591127670131 ) ) ;
#50505=ORIENTED_EDGE ( 'NONE', *, *, #6862, .T. ) ;
#50510=CARTESIAN_POINT ( 'NONE',  ( 71.31531788893299506, 1.266538207494809942, -70.53881316596870477 ) ) ;
#50553=VERTEX_POINT ( 'NONE', #46570 ) ;
#50555=CARTESIAN_POINT ( 'NONE',  ( 64.95585434546930514, 1.326578174762039986, -60.85378544217730479 ) ) ;
#50572=ORIENTED_EDGE ( 'NONE', *, *, #36261, .T. ) ;
#50578=CARTESIAN_POINT ( 'NONE',  ( 64.81566772303590085, 1.395841836299290151, -61.06813208783949420 ) ) ;
#50587=CARTESIAN_POINT ( 'NONE',  ( 73.12399047084761605, 1.191644800533229853, -62.50206874317210293 ) ) ;
#50589=CARTESIAN_POINT ( 'NONE',  ( 64.93393739769619799, 1.883811055320669947, -69.84999999999999432 ) ) ;
#50630=EDGE_CURVE ( 'NONE', #23138, #50553, #2192, .T. ) ;
#50634=FACE_OUTER_BOUND ( 'NONE', #47685, .T. ) ;
#50643=AXIS2_PLACEMENT_3D ( 'NONE', #13551, #20607, #36600 ) ;
#50648=CARTESIAN_POINT ( 'NONE',  ( 71.23719564129540061, 1.194703186106690129, -60.63553603340079690 ) ) ;
#50657=AXIS2_PLACEMENT_3D ( 'NONE', #14270, #23647, #27087 ) ;
#50658=EDGE_CURVE ( 'NONE', #33090, #25965, #41760, .T. ) ;
#50664=CARTESIAN_POINT ( 'NONE',  ( 63.53329261246669546, 1.393731187554809958, -68.81053500035210391 ) ) ;
#50674=CARTESIAN_POINT ( 'NONE',  ( 63.19468704395289649, 0.8986939045430389905, -62.24348040161360274 ) ) ;
#50693=FACE_OUTER_BOUND ( 'NONE', #11215, .T. ) ;
#50694=CARTESIAN_POINT ( 'NONE',  ( 73.01385068780759013, 0.9098571636355720083, -62.15909090909049439 ) ) ;
#50696=FACE_OUTER_BOUND ( 'NONE', #21314, .T. ) ;
#50705=CARTESIAN_POINT ( 'NONE',  ( 63.74194282759800245, 1.270920007605170099, -61.65828220330239873 ) ) ;
#50709=CARTESIAN_POINT ( 'NONE',  ( 72.83058059882510804, 1.382840740411490188, -68.63401718432778864 ) ) ;
#50715=AXIS2_PLACEMENT_3D ( 'NONE', #17806, #42707, #2866 ) ;
#50719=CARTESIAN_POINT ( 'NONE',  ( 74.13393739769620083, -42.11618894467930119, -65.65000000000000568 ) ) ;
#50725=EDGE_LOOP ( 'NONE', ( #13721, #44138, #29598, #50777 ) ) ;
#50738=CARTESIAN_POINT ( 'NONE',  ( 64.34681638194778941, 1.254582981797469854, -70.20495024723810218 ) ) ;
#50745=B_SPLINE_CURVE_WITH_KNOTS ( 'NONE', 3,
 ( #15412, #31111, #3618, #19072, #43448, #35580, #32128, #7550, #51565, #15667, #27952, #35045, #23241, #51054, #40027, #51818 ),
 .UNSPECIFIED., .F., .F.,
 ( 4, 2, 2, 2, 2, 2, 2, 4 ),
 ( -8.881783999999999806E-15, 0.07319275283555599920, 0.1391693187718399949, 0.1804046724820169978, 0.2061767685508779924, 0.2577209606886000093, 0.3401916681089540151, 0.4123535371017650331 ),
 .UNSPECIFIED. ) ;
#50749=CARTESIAN_POINT ( 'NONE',  ( 72.03549263123640856, 1.087300712304640093, -70.20170571670161053 ) ) ;
#50754=EDGE_CURVE ( 'NONE', #31343, #9229, #6722, .T. ) ;
#50757=CARTESIAN_POINT ( 'NONE',  ( 63.24043675930629860, 1.099344084866040072, -69.05806188122140554 ) ) ;
#50760=CARTESIAN_POINT ( 'NONE',  ( 71.33393739769628894, 1.883811055320669947, -61.44999999999999574 ) ) ;
#50764=( BOUNDED_SURFACE ( )  B_SPLINE_SURFACE ( 2, 2, ( 
 ( #21594, #17939, #45472 ),
 ( #49926, #33399, #45732 ),
 ( #5648, #14277, #37593 ) ),
 .UNSPECIFIED., .F., .F., .T. ) 
 B_SPLINE_SURFACE_WITH_KNOTS ( ( 3, 3 ),
 ( 3, 3 ),
 ( -1.570796326792230024, -3.926887462493479784E-13 ),
 ( -8.405333417276831159E-12, 1.570796326803189924 ),
 .UNSPECIFIED. ) 
 GEOMETRIC_REPRESENTATION_ITEM ( )  RATIONAL_B_SPLINE_SURFACE ( (
 ( 1.000000000000000000, 0.7071067811806429626, 1.000000000000000000),
 ( 0.7071067811876210474, 0.4999999999965839548, 0.7071067811876210474),
 ( 1.000000000000000000, 0.7071067811806429626, 1.000000000000000000) ) ) 
 REPRESENTATION_ITEM ( '' )  SURFACE ( )  );
#50766=CARTESIAN_POINT ( 'NONE',  ( 71.50903575780739629, 0.9989215084293960878, -70.60223669534680369 ) ) ;
#50771=EDGE_CURVE ( 'NONE', #43577, #41820, #20483, .T. ) ;
#50775=CARTESIAN_POINT ( 'NONE',  ( 71.36799767121759430, 0.8859637708054480809, -70.70388507757908769 ) ) ;
#50777=ORIENTED_EDGE ( 'NONE', *, *, #29155, .T. ) ;
#50808=CARTESIAN_POINT ( 'NONE',  ( 71.19761362482960010, 1.388189907116970101, -70.28386057589720792 ) ) ;
#50813=CARTESIAN_POINT ( 'NONE',  ( 65.07026117056290104, 1.388189907116970101, -61.01613942410280345 ) ) ;
#50842=CARTESIAN_POINT ( 'NONE',  ( 73.03096648148358838, 1.005545696829380109, -69.10544663728329340 ) ) ;
#50844=CARTESIAN_POINT ( 'NONE',  ( 72.72759757326660690, 1.395196698723390138, -62.46966344801350601 ) ) ;
#50850=CARTESIAN_POINT ( 'NONE',  ( 64.66786723518761448, 0.9395704634982849912, -70.54765821028060202 ) ) ;
#50867=EDGE_CURVE ( 'NONE', #12484, #25175, #28455, .T. ) ;
#50882=EDGE_CURVE ( 'NONE', #9229, #26724, #51658, .T. ) ;
#50894=CARTESIAN_POINT ( 'NONE',  ( 63.54027722212589424, 1.395196698723379924, -62.46966344801359838 ) ) ;
#50906=CARTESIAN_POINT ( 'NONE',  ( 71.19526263826620038, 1.274277262446069869, -60.70118609097839624 ) ) ;
#50908=CARTESIAN_POINT ( 'NONE',  ( 72.78995442782039049, 1.368315088675930102, -62.33478283481320403 ) ) ;
#50919=SHAPE_REPRESENTATION ( 'Wheel Axle Bolt', ( #20940 ), #854 ) ;
#50920=CARTESIAN_POINT ( 'NONE',  ( 63.43393739769620510, 1.383811055320669947, -68.50657137141709541 ) ) ;
#50933=CARTESIAN_POINT ( 'NONE',  ( 63.18115153217100755, 0.8966068345641570181, -62.26318953425300862 ) ) ;
#50961=CARTESIAN_POINT ( 'NONE',  ( 63.86171360969409960, 1.406831506490820116, -61.68741386948379812 ) ) ;
#50965=CARTESIAN_POINT ( 'NONE',  ( 72.85271889401160195, 1.383136297697689976, -68.56705292396610218 ) ) ;
#50982=CARTESIAN_POINT ( 'NONE',  ( 72.48038400710301232, 1.530257664727401545, -62.44999999999999574 ) ) ;
#50997=CARTESIAN_POINT ( 'NONE',  ( 64.26031169644889474, 0.9860222121691910591, -70.23289684640710107 ) ) ;
#51003=VERTEX_POINT ( 'NONE', #32643 ) ;
#51009=CARTESIAN_POINT ( 'NONE',  ( 71.73794240842320846, 1.239065815390139935, -70.33274506191480668 ) ) ;
#51013=CARTESIAN_POINT ( 'NONE',  ( 63.34508830662979761, 1.264689361399219836, -69.01667010504620237 ) ) ;
#51021=CARTESIAN_POINT ( 'NONE',  ( 71.40428550048659417, 1.263903724274369811, -70.49199270151910923 ) ) ;
#51026=DIRECTION ( 'NONE',  ( 0.000000000000000000, 0.000000000000000000, -1.000000000000000000 ) ) ;
#51037=AXIS2_PLACEMENT_3D ( 'NONE', #44414, #48347, #8517 ) ;
#51040=AXIS2_PLACEMENT_3D ( 'NONE', #33480, #29292, #17257 ) ;
#51054=CARTESIAN_POINT ( 'NONE',  ( 63.03407832914049891, 0.8840451408750739093, -68.81103260973580404 ) ) ;
#51063=CARTESIAN_POINT ( 'NONE',  ( 71.23851365796429036, 1.390208944942409985, -70.27002685503239832 ) ) ;
#51069=CARTESIAN_POINT ( 'NONE',  ( 64.86043556304430524, 0.9234936569010840923, -60.62162712823549526 ) ) ;
#51078=CARTESIAN_POINT ( 'NONE',  ( 71.62484648860579739, 0.9098571636355720083, -70.52991329011129551 ) ) ;
#51081=DIRECTION ( 'NONE',  ( 0.000000000000000000, 0.000000000000000000, 1.000000000000000000 ) ) ;
#51085=VERTEX_POINT ( 'NONE', #4895 ) ;
#51096=ORIENTED_EDGE ( 'NONE', *, *, #51402, .T. ) ;
#51100=CARTESIAN_POINT ( 'NONE',  ( 73.07509570698499601, 0.9325382164350239922, -62.24624853760359855 ) ) ;
#51106=CARTESIAN_POINT ( 'NONE',  ( 64.76726729265020310, 1.264689361399219836, -70.43884909106650127 ) ) ;
#51117=ORIENTED_EDGE ( 'NONE', *, *, #34069, .F. ) ;
#51141=CARTESIAN_POINT ( 'NONE',  ( 64.43393739769619799, 10.88381105532070059, -62.44999999999999574 ) ) ;
#51148=DIRECTION ( 'NONE',  ( -0.000000000000000000, 1.000000000000000000, 0.000000000000000000 ) ) ;
#51158=CARTESIAN_POINT ( 'NONE',  ( 63.26785353957599511, 1.102139304147779830, -62.20100733290610151 ) ) ;
#51172=CARTESIAN_POINT ( 'NONE',  ( 70.99050876911339003, 1.383811055320669947, -60.94999999999999574 ) ) ;
#51174=CARTESIAN_POINT ( 'NONE',  ( 72.55639720057749287, 1.338417587229449923, -61.77627077996229588 ) ) ;
#51222=CARTESIAN_POINT ( 'NONE',  ( 63.25402410758490390, 0.9098571636355720083, -62.15909090909049439 ) ) ;
#51238=CARTESIAN_POINT ( 'NONE',  ( 73.06112045927889653, 1.270877794983130027, -68.75550371754310675 ) ) ;
#51256=CARTESIAN_POINT ( 'NONE',  ( 72.83393739769620367, 1.383811055320669947, -62.79342862858290886 ) ) ;
#51259=CARTESIAN_POINT ( 'NONE',  ( 72.18749078828946608, 11.23736444591397543, -68.84999999999999432 ) ) ;
#51269=CARTESIAN_POINT ( 'NONE',  ( 71.35671708621339349, 1.389801772588449946, -70.26683326709820676 ) ) ;
#51284=CARTESIAN_POINT ( 'NONE',  ( 71.61023385683570552, 1.007912009470880221, -70.53231455471861011 ) ) ;
#51296=VERTEX_POINT ( 'NONE', #14826 ) ;
#51306=DIRECTION ( 'NONE',  ( -1.000000000000000000, 0.000000000000000000, 0.000000000000000000 ) ) ;
#51314=VERTEX_POINT ( 'NONE', #47581 ) ;
#51316=CARTESIAN_POINT ( 'NONE',  ( 62.13393739769620083, -20.61618894467929763, -65.65000000000000568 ) ) ;
#51331=CARTESIAN_POINT ( 'NONE',  ( 64.85305306408208992, 1.096036836948800053, -60.67470092284240479 ) ) ;
#51347=ORIENTED_EDGE ( 'NONE', *, *, #46325, .T. ) ;
#51362=CARTESIAN_POINT ( 'NONE',  ( 73.08672326322148649, 0.8966068345641440285, -62.26318953425310099 ) ) ;
#51367=CARTESIAN_POINT ( 'NONE',  ( 64.93393739769599904, 1.396834109478120034, -70.23662692463440749 ) ) ;
#51392=AXIS2_PLACEMENT_3D ( 'NONE', #11223, #12709, #19588 ) ;
#51402=EDGE_CURVE ( 'NONE', #36774, #46160, #49440, .T. ) ;
#51404=CARTESIAN_POINT ( 'NONE',  ( 63.37726551317079782, 1.370937308141420230, -68.67294022748990301 ) ) ;
#51427=CARTESIAN_POINT ( 'NONE',  ( 71.20883305211729919, 1.369885150286779929, -60.91305399111080021 ) ) ;
#51429=CARTESIAN_POINT ( 'NONE',  ( 72.31664968728070164, 1.060191324942699964, -61.34806069345289359 ) ) ;
#51489=CARTESIAN_POINT ( 'NONE',  ( 73.16231026946078941, 0.9234936569010840923, -68.92350183465200075 ) ) ;
#51523=CARTESIAN_POINT ( 'NONE',  ( 71.44915456287860422, 1.368315088675810198, -70.30601703012600012 ) ) ;
#51531=CARTESIAN_POINT ( 'NONE',  ( 63.54027722212589424, 1.395196698723390138, -68.83033655198650536 ) ) ;
#51535=CARTESIAN_POINT ( 'NONE',  ( 64.26031169644889474, 0.9860222121691860631, -70.23289684640710107 ) ) ;
#51539=FACE_OUTER_BOUND ( 'NONE', #25885, .T. ) ;
#51541=CARTESIAN_POINT ( 'NONE',  ( 71.31398829338289147, 1.388313565858570131, -70.27734465158499688 ) ) ;
#51565=CARTESIAN_POINT ( 'NONE',  ( 63.13228119804391270, 0.8904513541338869853, -68.96413986139360475 ) ) ;
#51567=CARTESIAN_POINT ( 'NONE',  ( 65.01767771978660448, 0.8838110553206759423, -70.77727272727270247 ) ) ;
#51584=CARTESIAN_POINT ( 'NONE',  ( 64.88733809717980705, 1.187415670095769871, -60.71585052632950408 ) ) ;
#51603=CIRCLE ( 'NONE', #42408, 0.4999999999999995559 ) ;
#51617=CARTESIAN_POINT ( 'NONE',  ( 73.03096648148358838, 1.005545696829380109, -62.19455336271669665 ) ) ;
#51622=CARTESIAN_POINT ( 'NONE',  ( 64.93408011569840710, 1.389468113695450091, -70.26995969721839685 ) ) ;
#51630=ORIENTED_EDGE ( 'NONE', *, *, #6630, .F. ) ;
#51658=B_SPLINE_CURVE_WITH_KNOTS ( 'NONE', 3,
 ( #20154, #50145, #47010, #11096, #24846, #4437, #41369, #36391, #32440, #29055, #40593, #48466, #40343, #41116, #5230, #37188 ),
 .UNSPECIFIED., .F., .F.,
 ( 4, 2, 2, 2, 2, 2, 2, 4 ),
 ( -8.326672999999999728E-16, 0.07319275283556599121, 0.1391693187718509861, 0.1804046724820289882, 0.2061767685508900105, 0.2577209606886129989, 0.3401916681089700023, 0.4123535371017769680 ),
 .UNSPECIFIED. ) ;
#51659=CARTESIAN_POINT ( 'NONE',  ( 63.10556452593170462, 0.9234936569010840923, -68.92350183465200075 ) ) ;
#51679=CARTESIAN_POINT ( 'NONE',  ( 71.26748243800840044, 1.369544300367000034, -60.93595317393490518 ) ) ;
#51681=CARTESIAN_POINT ( 'NONE',  ( 72.68322664906099817, 1.025918948571989953, -61.73674522937599818 ) ) ;
#51692=ORIENTED_EDGE ( 'NONE', *, *, #49976, .F. ) ;
#51713=DIRECTION ( 'NONE',  ( 0.000000000000000000, 0.000000000000000000, 1.000000000000000000 ) ) ;
#51723=CARTESIAN_POINT ( 'NONE',  ( 63.11679429741250402, 0.8888742037077609348, -62.35931220671560027 ) ) ;
#51726=DIRECTION ( 'NONE',  ( -0.5193766129849320956, 0.000000000000000000, 0.8545454545454562734 ) ) ;
#51727=CARTESIAN_POINT ( 'NONE',  ( 64.64302830678670375, 0.9098571636355720083, -60.77008670988870165 ) ) ;
#51738=CARTESIAN_POINT ( 'NONE',  ( 72.83393739769620367, 1.383811055320669947, -68.50657137141709541 ) ) ;
#51739=CARTESIAN_POINT ( 'NONE',  ( 72.83393739769620367, 1.383811055320669947, -62.79342862858290886 ) ) ;
#51751=DIRECTION ( 'NONE',  ( -1.000000000000000000, 0.000000000000000000, 0.000000000000000000 ) ) ;
#51774=CARTESIAN_POINT ( 'NONE',  ( 72.50969334808389988, 1.026088617261680103, -69.75574693290759853 ) ) ;
#51790=CARTESIAN_POINT ( 'NONE',  ( 71.35301946752790059, 1.370853092582090094, -70.32939881202800336 ) ) ;
#51818=CARTESIAN_POINT ( 'NONE',  ( 63.00666467042349694, 0.8838110553206759423, -68.76625967790960203 ) ) ;
ENDSEC;
END-ISO-10303-21;
